ISO-10303-21;
HEADER;
/* Generated by software containing ST-Developer
 * from STEP Tools, Inc. (www.steptools.com) 
 */

FILE_DESCRIPTION(
/* description */ ('Independent equipment support assembly with bolted 600 x 500 mm welde
d perimeter frame, four adjustable legs and swivel feet. Nominal overa
ll height 518 mm. No load rating assigned.'),
/* implementation_level */ '2;1');

FILE_NAME(
/* name */ 'Socket head cap screw M8x25.step',
/* time_stamp */ '2026-11-07T17:30:39-08:00',
/* author */ (''),
/* organization */ (''),
/* preprocessor_version */ 'ST-DEVELOPER v20.2',
/* originating_system */ 'Autodesk Translation Framework v15.17.0.0',
/* authorisation */ '');

FILE_SCHEMA (('AUTOMOTIVE_DESIGN { 1 0 10303 214 3 1 1 }'));
ENDSEC;

DATA;
#10=MECHANICAL_DESIGN_GEOMETRIC_PRESENTATION_REPRESENTATION('',(#2211),#63755);
#254=CONICAL_SURFACE('',#14672,3.5,0.785398163397448);
#265=B_SPLINE_SURFACE_WITH_KNOTS('',3,3,((#26409,#26410,#26411,#26412,#26413,
#26414,#26415,#26416,#26417,#26418,#26419,#26420,#26421,#26422,#26423,#26424,
#26425,#26426,#26427,#26428,#26429,#26430,#26431,#26432,#26433,#26434,#26435,
#26436,#26437,#26438,#26439,#26440,#26441,#26442,#26443,#26444,#26445,#26446,
#26447,#26448,#26449,#26450,#26451,#26452,#26453,#26454,#26455,#26456,#26457,
#26458,#26459,#26460,#26461,#26462,#26463,#26464,#26465,#26466,#26467,#26468,
#26469,#26470,#26471,#26472,#26473,#26474,#26475,#26476,#26477,#26478,#26479,
#26480,#26481,#26482,#26483,#26484,#26485,#26486,#26487,#26488,#26489,#26490,
#26491,#26492,#26493,#26494,#26495,#26496,#26497,#26498,#26499,#26500,#26501,
#26502,#26503,#26504,#26505,#26506,#26507,#26508,#26509,#26510,#26511,#26512,
#26513,#26514,#26515,#26516,#26517,#26518,#26519,#26520,#26521,#26522,#26523,
#26524,#26525,#26526,#26527,#26528,#26529,#26530,#26531,#26532,#26533,#26534,
#26535,#26536,#26537,#26538,#26539,#26540,#26541,#26542,#26543,#26544,#26545,
#26546,#26547,#26548,#26549,#26550,#26551,#26552,#26553,#26554,#26555,#26556,
#26557,#26558,#26559,#26560,#26561,#26562,#26563,#26564,#26565,#26566),
(#26567,#26568,#26569,#26570,#26571,#26572,#26573,#26574,#26575,#26576,
#26577,#26578,#26579,#26580,#26581,#26582,#26583,#26584,#26585,#26586,#26587,
#26588,#26589,#26590,#26591,#26592,#26593,#26594,#26595,#26596,#26597,#26598,
#26599,#26600,#26601,#26602,#26603,#26604,#26605,#26606,#26607,#26608,#26609,
#26610,#26611,#26612,#26613,#26614,#26615,#26616,#26617,#26618,#26619,#26620,
#26621,#26622,#26623,#26624,#26625,#26626,#26627,#26628,#26629,#26630,#26631,
#26632,#26633,#26634,#26635,#26636,#26637,#26638,#26639,#26640,#26641,#26642,
#26643,#26644,#26645,#26646,#26647,#26648,#26649,#26650,#26651,#26652,#26653,
#26654,#26655,#26656,#26657,#26658,#26659,#26660,#26661,#26662,#26663,#26664,
#26665,#26666,#26667,#26668,#26669,#26670,#26671,#26672,#26673,#26674,#26675,
#26676,#26677,#26678,#26679,#26680,#26681,#26682,#26683,#26684,#26685,#26686,
#26687,#26688,#26689,#26690,#26691,#26692,#26693,#26694,#26695,#26696,#26697,
#26698,#26699,#26700,#26701,#26702,#26703,#26704,#26705,#26706,#26707,#26708,
#26709,#26710,#26711,#26712,#26713,#26714,#26715,#26716,#26717,#26718,#26719,
#26720,#26721,#26722,#26723,#26724),(#26725,#26726,#26727,#26728,#26729,
#26730,#26731,#26732,#26733,#26734,#26735,#26736,#26737,#26738,#26739,#26740,
#26741,#26742,#26743,#26744,#26745,#26746,#26747,#26748,#26749,#26750,#26751,
#26752,#26753,#26754,#26755,#26756,#26757,#26758,#26759,#26760,#26761,#26762,
#26763,#26764,#26765,#26766,#26767,#26768,#26769,#26770,#26771,#26772,#26773,
#26774,#26775,#26776,#26777,#26778,#26779,#26780,#26781,#26782,#26783,#26784,
#26785,#26786,#26787,#26788,#26789,#26790,#26791,#26792,#26793,#26794,#26795,
#26796,#26797,#26798,#26799,#26800,#26801,#26802,#26803,#26804,#26805,#26806,
#26807,#26808,#26809,#26810,#26811,#26812,#26813,#26814,#26815,#26816,#26817,
#26818,#26819,#26820,#26821,#26822,#26823,#26824,#26825,#26826,#26827,#26828,
#26829,#26830,#26831,#26832,#26833,#26834,#26835,#26836,#26837,#26838,#26839,
#26840,#26841,#26842,#26843,#26844,#26845,#26846,#26847,#26848,#26849,#26850,
#26851,#26852,#26853,#26854,#26855,#26856,#26857,#26858,#26859,#26860,#26861,
#26862,#26863,#26864,#26865,#26866,#26867,#26868,#26869,#26870,#26871,#26872,
#26873,#26874,#26875,#26876,#26877,#26878,#26879,#26880,#26881,#26882),
(#26883,#26884,#26885,#26886,#26887,#26888,#26889,#26890,#26891,#26892,
#26893,#26894,#26895,#26896,#26897,#26898,#26899,#26900,#26901,#26902,#26903,
#26904,#26905,#26906,#26907,#26908,#26909,#26910,#26911,#26912,#26913,#26914,
#26915,#26916,#26917,#26918,#26919,#26920,#26921,#26922,#26923,#26924,#26925,
#26926,#26927,#26928,#26929,#26930,#26931,#26932,#26933,#26934,#26935,#26936,
#26937,#26938,#26939,#26940,#26941,#26942,#26943,#26944,#26945,#26946,#26947,
#26948,#26949,#26950,#26951,#26952,#26953,#26954,#26955,#26956,#26957,#26958,
#26959,#26960,#26961,#26962,#26963,#26964,#26965,#26966,#26967,#26968,#26969,
#26970,#26971,#26972,#26973,#26974,#26975,#26976,#26977,#26978,#26979,#26980,
#26981,#26982,#26983,#26984,#26985,#26986,#26987,#26988,#26989,#26990,#26991,
#26992,#26993,#26994,#26995,#26996,#26997,#26998,#26999,#27000,#27001,#27002,
#27003,#27004,#27005,#27006,#27007,#27008,#27009,#27010,#27011,#27012,#27013,
#27014,#27015,#27016,#27017,#27018,#27019,#27020,#27021,#27022,#27023,#27024,
#27025,#27026,#27027,#27028,#27029,#27030,#27031,#27032,#27033,#27034,#27035,
#27036,#27037,#27038,#27039,#27040)),.UNSPECIFIED.,.F.,.F.,.F.,(4,4),(4,
1,1,1,1,1,1,1,1,1,1,1,1,1,1,1,1,1,1,1,1,1,1,1,1,1,1,1,1,1,1,1,1,1,1,1,1,
1,1,1,1,1,1,1,1,1,1,1,1,1,1,1,1,1,1,1,1,1,1,1,1,1,1,1,1,1,1,1,1,1,1,1,1,
1,1,1,1,1,1,1,1,1,1,1,1,1,1,1,1,1,1,1,1,1,1,1,1,1,1,1,1,1,1,1,1,1,1,1,1,
1,1,1,1,1,1,1,1,1,1,1,1,1,1,1,1,1,1,1,1,1,1,1,1,1,1,1,1,1,1,1,1,1,1,1,1,
1,1,1,1,1,1,1,1,1,1,4),(0.,0.0658467982010769),(11.6150328478184,12.61338032228,
13.6117277967416,14.6100752712031,15.6084227456647,16.6067702201263,17.6051176945879,
18.6034651690495,19.6018126435111,20.6001601179726,21.5985075924342,22.5968550668958,
23.5952025413574,24.593550015819,25.5918974902806,26.5902449647422,27.5885924392037,
28.5869399136653,29.5852873881269,30.5836348625885,31.5819823370501,32.5803298115117,
33.5786772859732,34.5770247604348,35.5753722348964,36.573719709358,37.5720671838196,
38.5704146582812,39.5687621327428,40.5671096072043,41.5654570816659,42.5638045561275,
43.5621520305891,44.5604995050507,45.5588469795123,46.5571944539738,47.5555419284354,
48.553889402897,49.5522368773586,50.5505843518202,51.5489318262818,52.5472793007434,
53.545626775205,54.5439742496665,55.5423217241281,56.5406691985897,57.5390166730513,
58.5373641475129,59.5357116219745,60.534059096436,61.5324065708976,62.5307540453592,
63.5291015198208,64.5274489942824,65.525796468744,66.5241439432056,67.5224914176671,
68.5208388921287,69.5191863665903,70.5175338410519,71.5158813155135,72.5142287899751,
73.5125762644366,74.5109237388982,75.5092712133598,76.5076186878214,77.505966162283,
78.5043136367446,79.5026611112062,80.5010085856677,81.4993560601293,82.4977035345909,
83.4960510090525,84.4943984835141,85.4927459579757,86.4910934324373,87.4894409068988,
88.4877883813604,89.486135855822,90.4844833302836,91.4828308047452,92.4811782792068,
93.4795257536684,94.4778732281299,95.4762207025915,96.4745681770531,97.4729156515147,
98.4712631259763,99.4696106004379,100.467958074899,101.466305549361,102.464653023823,
103.463000498284,104.461347972746,105.459695447207,106.458042921669,107.456390396131,
108.454737870592,109.453085345054,110.451432819515,111.449780293977,112.448127768438,
113.4464752429,114.444822717362,115.443170191823,116.441517666285,117.439865140746,
118.438212615208,119.43656008967,120.434907564131,121.433255038593,122.431602513054,
123.429949987516,124.428297461977,125.426644936439,126.424992410901,127.423339885362,
128.421687359824,129.420034834285,130.418382308747,131.416729783209,132.41507725767,
133.413424732132,134.411772206593,135.410119681055,136.408467155516,137.406814629978,
138.40516210444,139.403509578901,140.401857053363,141.400204527824,142.398552002286,
143.396899476748,144.395246951209,145.393594425671,146.391941900132,147.390289374594,
148.388636849056,149.386984323517,150.385331797979,151.38367927244,152.382026746902,
153.380374221363,154.378721695825,155.377069170287,156.375416644748,157.37376411921,
158.372111593671,159.370459068133,160.368806542595,161.367154017056,162.365501491518,
163.363848965979,164.362196440441,165.360543914902,166.358891389364),
 .UNSPECIFIED.);
#266=B_SPLINE_SURFACE_WITH_KNOTS('',3,3,((#27178,#27179,#27180,#27181,#27182,
#27183,#27184,#27185,#27186,#27187,#27188,#27189,#27190,#27191,#27192,#27193,
#27194,#27195,#27196,#27197,#27198,#27199,#27200,#27201,#27202,#27203,#27204,
#27205,#27206,#27207,#27208,#27209,#27210,#27211,#27212,#27213,#27214,#27215,
#27216,#27217,#27218,#27219,#27220,#27221,#27222,#27223,#27224,#27225,#27226,
#27227,#27228,#27229,#27230,#27231,#27232,#27233,#27234,#27235,#27236,#27237,
#27238,#27239,#27240,#27241,#27242,#27243,#27244,#27245,#27246,#27247,#27248,
#27249,#27250,#27251,#27252,#27253,#27254,#27255,#27256,#27257,#27258,#27259,
#27260,#27261,#27262,#27263,#27264,#27265,#27266,#27267,#27268,#27269,#27270,
#27271,#27272,#27273,#27274,#27275,#27276,#27277,#27278,#27279,#27280,#27281,
#27282,#27283,#27284,#27285,#27286,#27287,#27288,#27289,#27290,#27291,#27292,
#27293,#27294,#27295,#27296,#27297,#27298,#27299,#27300,#27301,#27302,#27303,
#27304,#27305,#27306,#27307,#27308,#27309,#27310,#27311,#27312,#27313,#27314,
#27315,#27316,#27317,#27318,#27319,#27320,#27321,#27322,#27323,#27324,#27325,
#27326,#27327,#27328,#27329,#27330,#27331,#27332,#27333,#27334,#27335,#27336,
#27337),(#27338,#27339,#27340,#27341,#27342,#27343,#27344,#27345,#27346,
#27347,#27348,#27349,#27350,#27351,#27352,#27353,#27354,#27355,#27356,#27357,
#27358,#27359,#27360,#27361,#27362,#27363,#27364,#27365,#27366,#27367,#27368,
#27369,#27370,#27371,#27372,#27373,#27374,#27375,#27376,#27377,#27378,#27379,
#27380,#27381,#27382,#27383,#27384,#27385,#27386,#27387,#27388,#27389,#27390,
#27391,#27392,#27393,#27394,#27395,#27396,#27397,#27398,#27399,#27400,#27401,
#27402,#27403,#27404,#27405,#27406,#27407,#27408,#27409,#27410,#27411,#27412,
#27413,#27414,#27415,#27416,#27417,#27418,#27419,#27420,#27421,#27422,#27423,
#27424,#27425,#27426,#27427,#27428,#27429,#27430,#27431,#27432,#27433,#27434,
#27435,#27436,#27437,#27438,#27439,#27440,#27441,#27442,#27443,#27444,#27445,
#27446,#27447,#27448,#27449,#27450,#27451,#27452,#27453,#27454,#27455,#27456,
#27457,#27458,#27459,#27460,#27461,#27462,#27463,#27464,#27465,#27466,#27467,
#27468,#27469,#27470,#27471,#27472,#27473,#27474,#27475,#27476,#27477,#27478,
#27479,#27480,#27481,#27482,#27483,#27484,#27485,#27486,#27487,#27488,#27489,
#27490,#27491,#27492,#27493,#27494,#27495,#27496,#27497),(#27498,#27499,
#27500,#27501,#27502,#27503,#27504,#27505,#27506,#27507,#27508,#27509,#27510,
#27511,#27512,#27513,#27514,#27515,#27516,#27517,#27518,#27519,#27520,#27521,
#27522,#27523,#27524,#27525,#27526,#27527,#27528,#27529,#27530,#27531,#27532,
#27533,#27534,#27535,#27536,#27537,#27538,#27539,#27540,#27541,#27542,#27543,
#27544,#27545,#27546,#27547,#27548,#27549,#27550,#27551,#27552,#27553,#27554,
#27555,#27556,#27557,#27558,#27559,#27560,#27561,#27562,#27563,#27564,#27565,
#27566,#27567,#27568,#27569,#27570,#27571,#27572,#27573,#27574,#27575,#27576,
#27577,#27578,#27579,#27580,#27581,#27582,#27583,#27584,#27585,#27586,#27587,
#27588,#27589,#27590,#27591,#27592,#27593,#27594,#27595,#27596,#27597,#27598,
#27599,#27600,#27601,#27602,#27603,#27604,#27605,#27606,#27607,#27608,#27609,
#27610,#27611,#27612,#27613,#27614,#27615,#27616,#27617,#27618,#27619,#27620,
#27621,#27622,#27623,#27624,#27625,#27626,#27627,#27628,#27629,#27630,#27631,
#27632,#27633,#27634,#27635,#27636,#27637,#27638,#27639,#27640,#27641,#27642,
#27643,#27644,#27645,#27646,#27647,#27648,#27649,#27650,#27651,#27652,#27653,
#27654,#27655,#27656,#27657),(#27658,#27659,#27660,#27661,#27662,#27663,
#27664,#27665,#27666,#27667,#27668,#27669,#27670,#27671,#27672,#27673,#27674,
#27675,#27676,#27677,#27678,#27679,#27680,#27681,#27682,#27683,#27684,#27685,
#27686,#27687,#27688,#27689,#27690,#27691,#27692,#27693,#27694,#27695,#27696,
#27697,#27698,#27699,#27700,#27701,#27702,#27703,#27704,#27705,#27706,#27707,
#27708,#27709,#27710,#27711,#27712,#27713,#27714,#27715,#27716,#27717,#27718,
#27719,#27720,#27721,#27722,#27723,#27724,#27725,#27726,#27727,#27728,#27729,
#27730,#27731,#27732,#27733,#27734,#27735,#27736,#27737,#27738,#27739,#27740,
#27741,#27742,#27743,#27744,#27745,#27746,#27747,#27748,#27749,#27750,#27751,
#27752,#27753,#27754,#27755,#27756,#27757,#27758,#27759,#27760,#27761,#27762,
#27763,#27764,#27765,#27766,#27767,#27768,#27769,#27770,#27771,#27772,#27773,
#27774,#27775,#27776,#27777,#27778,#27779,#27780,#27781,#27782,#27783,#27784,
#27785,#27786,#27787,#27788,#27789,#27790,#27791,#27792,#27793,#27794,#27795,
#27796,#27797,#27798,#27799,#27800,#27801,#27802,#27803,#27804,#27805,#27806,
#27807,#27808,#27809,#27810,#27811,#27812,#27813,#27814,#27815,#27816,#27817)),
 .UNSPECIFIED.,.F.,.F.,.F.,(4,4),(4,1,1,1,1,1,1,1,1,1,1,1,1,1,1,1,1,1,1,
1,1,1,1,1,1,1,1,1,1,1,1,1,1,1,1,1,1,1,1,1,1,1,1,1,1,1,1,1,1,1,1,1,1,1,1,
1,1,1,1,1,1,1,1,1,1,1,1,1,1,1,1,1,1,1,1,1,1,1,1,1,1,1,1,1,1,1,1,1,1,1,1,
1,1,1,1,1,1,1,1,1,1,1,1,1,1,1,1,1,1,1,1,1,1,1,1,1,1,1,1,1,1,1,1,1,1,1,1,
1,1,1,1,1,1,1,1,1,1,1,1,1,1,1,1,1,1,1,1,1,1,1,1,1,1,1,1,1,1,4),(0.,0.0658467982010769),
(8.30747755240114,9.30628326397092,10.3050889755407,11.3038946871105,12.3027003986802,
13.30150611025,14.3003118218198,15.2991175333896,16.2979232449593,17.2967289565291,
18.2955346680989,19.2943403796687,20.2931460912385,21.2919518028082,22.290757514378,
23.2895632259478,24.2883689375176,25.2871746490873,26.2859803606571,27.2847860722269,
28.2835917837967,29.2823974953664,30.2812032069362,31.280008918506,32.2788146300758,
33.2776203416455,34.2764260532153,35.2752317647851,36.2740374763549,37.2728431879246,
38.2716488994944,39.2704546110642,40.269260322634,41.2680660342037,42.2668717457735,
43.2656774573433,44.2644831689131,45.2632888804829,46.2620945920526,47.2609003036224,
48.2597060151922,49.258511726762,50.2573174383317,51.2561231499015,52.2549288614713,
53.2537345730411,54.2525402846108,55.2513459961806,56.2501517077504,57.2489574193202,
58.2477631308899,59.2465688424597,60.2453745540295,61.2441802655993,62.242985977169,
63.2417916887388,64.2405974003086,65.2394031118784,66.2382088234481,67.2370145350179,
68.2358202465877,69.2346259581575,70.2334316697272,71.232237381297,72.2310430928668,
73.2298488044366,74.2286545160063,75.2274602275761,76.2262659391459,77.2250716507157,
78.2238773622854,79.2226830738552,80.221488785425,81.2202944969948,82.2191002085646,
83.2179059201343,84.2167116317041,85.2155173432739,86.2143230548436,87.2131287664134,
88.2119344779832,89.210740189553,90.2095459011228,91.2083516126925,92.2071573242623,
93.2059630358321,94.2047687474019,95.2035744589716,96.2023801705414,97.2011858821112,
98.199991593681,99.1987973052507,100.197603016821,101.19640872839,102.19521443996,
103.19402015153,104.1928258631,105.191631574669,106.190437286239,107.189242997809,
108.188048709379,109.186854420948,110.185660132518,111.184465844088,112.183271555658,
113.182077267228,114.180882978797,115.179688690367,116.178494401937,117.177300113507,
118.176105825076,119.174911536646,120.173717248216,121.172522959786,122.171328671356,
123.170134382925,124.168940094495,125.167745806065,126.166551517635,127.165357229204,
128.164162940774,129.162968652344,130.161774363914,131.160580075484,132.159385787053,
133.158191498623,134.156997210193,135.155802921763,136.154608633332,137.153414344902,
138.152220056472,139.151025768042,140.149831479612,141.148637191181,142.147442902751,
143.146248614321,144.145054325891,145.14386003746,146.14266574903,147.1414714606,
148.14027717217,149.13908288374,150.137888595309,151.136694306879,152.135500018449,
153.134305730019,154.133111441588,155.131917153158,156.130722864728,157.129528576298,
158.128334287868,159.127139999437,160.125945711007,161.124751422577,162.123557134147,
163.122362845716,164.121168557286,165.119974268856),.UNSPECIFIED.);
#301=CIRCLE('',#14623,3.942);
#302=CIRCLE('',#14648,3.37175);
#303=CIRCLE('',#14673,3.942);
#304=CIRCLE('',#14674,3.);
#305=CIRCLE('',#14676,3.37175);
#306=CIRCLE('',#14686,6.5);
#307=CIRCLE('',#14688,6.5);
#647=B_SPLINE_CURVE_WITH_KNOTS('',3,(#24322,#24323,#24324,#24325,#24326,
#24327,#24328,#24329,#24330,#24331),.UNSPECIFIED.,.F.,.F.,(4,3,3,4),(-4.09293042013064,
-3.99338989784634,-2.99504242338475,-2.06863817490912),.UNSPECIFIED.);
#648=B_SPLINE_CURVE_WITH_KNOTS('',3,(#24334,#24335,#24336,#24337,#24338,
#24339,#24340),.UNSPECIFIED.,.F.,.F.,(4,3,4),(0.,0.998805711569778,1.11730040836826),
 .UNSPECIFIED.);
#649=B_SPLINE_CURVE_WITH_KNOTS('',3,(#24345,#24346,#24347,#24348,#24349,
#24350,#24351,#24352,#24353,#24354,#24355,#24356,#24357,#24358,#24359,#24360,
#24361,#24362,#24363,#24364,#24365,#24366),.UNSPECIFIED.,.F.,.F.,(4,3,3,
3,3,3,3,4),(-10.3761157273102,-9.98347474461585,-8.98512727015427,-7.98677979569268,
-6.98843232123109,-5.99008484676951,-4.99173737230793,-4.09293042013064),
 .UNSPECIFIED.);
#650=B_SPLINE_CURVE_WITH_KNOTS('',3,(#24367,#24368,#24369,#24370,#24371,
#24372,#24373,#24374,#24375,#24376,#24377,#24378,#24379,#24380,#24381,#24382,
#24383,#24384,#24385,#24386,#24387,#24388),.UNSPECIFIED.,.F.,.F.,(4,3,3,
3,3,3,3,4),(1.11730040836826,1.99761142313956,2.99641713470934,3.99522284627912,
4.99402855784889,5.99283426941867,6.99163998098846,7.40048571554784),
 .UNSPECIFIED.);
#651=B_SPLINE_CURVE_WITH_KNOTS('',3,(#24393,#24394,#24395,#24396,#24397,
#24398,#24399,#24400,#24401,#24402,#24403,#24404,#24405,#24406,#24407,#24408,
#24409,#24410,#24411,#24412,#24413,#24414),.UNSPECIFIED.,.F.,.F.,(4,3,3,
3,3,3,3,4),(-16.6593010344898,-15.9735595913854,-14.9752121169238,-13.9768646424622,
-12.9785171680006,-11.980169693539,-10.9818222190774,-10.3761157273102),
 .UNSPECIFIED.);
#652=B_SPLINE_CURVE_WITH_KNOTS('',3,(#24415,#24416,#24417,#24418,#24419,
#24420,#24421,#24422,#24423,#24424,#24425,#24426,#24427,#24428,#24429,#24430,
#24431,#24432,#24433,#24434,#24435,#24436),.UNSPECIFIED.,.F.,.F.,(4,3,3,
3,3,3,3,4),(7.40048571554784,7.99044569255823,8.989251404128,9.98805711569777,
10.9868628272675,11.9856685388373,12.9844742504071,13.6836710227274),
 .UNSPECIFIED.);
#653=B_SPLINE_CURVE_WITH_KNOTS('',3,(#24441,#24442,#24443,#24444,#24445,
#24446,#24447,#24448,#24449,#24450,#24451,#24452,#24453,#24454,#24455,#24456,
#24457,#24458,#24459,#24460,#24461,#24462),.UNSPECIFIED.,.F.,.F.,(4,3,3,
3,3,3,3,4),(-22.9424863416694,-21.9636444381549,-20.9652969636933,-19.9669494892317,
-18.9686020147701,-17.9702545403085,-16.9719070658469,-16.6593010344898),
 .UNSPECIFIED.);
#654=B_SPLINE_CURVE_WITH_KNOTS('',3,(#24463,#24464,#24465,#24466,#24467,
#24468,#24469,#24470,#24471,#24472,#24473,#24474,#24475,#24476,#24477,#24478,
#24479,#24480,#24481,#24482,#24483,#24484),.UNSPECIFIED.,.F.,.F.,(4,3,3,
3,3,3,3,4),(13.6836710227274,13.9832799619769,14.9820856735466,15.9808913851164,
16.9796970966862,17.978502808256,18.9773085198257,19.966856329907),
 .UNSPECIFIED.);
#655=B_SPLINE_CURVE_WITH_KNOTS('',3,(#24489,#24490,#24491,#24492,#24493,
#24494,#24495,#24496,#24497,#24498,#24499,#24500,#24501,#24502,#24503,#24504,
#24505,#24506,#24507,#24508,#24509,#24510,#24511,#24512,#24513),
 .UNSPECIFIED.,.F.,.F.,(4,3,3,3,3,3,3,3,4),(-29.225671648849,-28.952076759386,
-27.9537292849244,-26.9553818104628,-25.9570343360012,-24.9586868615396,
-23.960339387078,-22.9619919126165,-22.9424863416694),.UNSPECIFIED.);
#656=B_SPLINE_CURVE_WITH_KNOTS('',3,(#24514,#24515,#24516,#24517,#24518,
#24519,#24520,#24521,#24522,#24523,#24524,#24525,#24526,#24527,#24528,#24529,
#24530,#24531,#24532,#24533,#24534,#24535,#24536,#24537,#24538),
 .UNSPECIFIED.,.F.,.F.,(4,3,3,3,3,3,3,3,4),(19.966856329907,19.9761142313955,
20.9749199429653,21.9737256545351,22.9725313661048,23.9713370776746,24.9701427892444,
25.9689485008142,26.2500416370866),.UNSPECIFIED.);
#657=B_SPLINE_CURVE_WITH_KNOTS('',3,(#24543,#24544,#24545,#24546,#24547,
#24548,#24549,#24550,#24551,#24552,#24553,#24554,#24555,#24556,#24557,#24558,
#24559,#24560,#24561,#24562,#24563,#24564),.UNSPECIFIED.,.F.,.F.,(4,3,3,
3,3,3,3,4),(-35.5088569560286,-34.9421616061555,-33.9438141316939,-32.9454666572323,
-31.9471191827707,-30.9487717083091,-29.9504242338475,-29.225671648849),
 .UNSPECIFIED.);
#658=B_SPLINE_CURVE_WITH_KNOTS('',3,(#24565,#24566,#24567,#24568,#24569,
#24570,#24571,#24572,#24573,#24574,#24575,#24576,#24577,#24578,#24579,#24580,
#24581,#24582,#24583,#24584,#24585,#24586),.UNSPECIFIED.,.F.,.F.,(4,3,3,
3,3,3,3,4),(26.2500416370866,26.9677542123839,27.9665599239537,28.9653656355235,
29.9641713470933,30.9629770586631,31.9617827702328,32.5332269442662),
 .UNSPECIFIED.);
#659=B_SPLINE_CURVE_WITH_KNOTS('',3,(#24591,#24592,#24593,#24594,#24595,
#24596,#24597,#24598,#24599,#24600,#24601,#24602,#24603,#24604,#24605,#24606,
#24607,#24608,#24609,#24610,#24611,#24612),.UNSPECIFIED.,.F.,.F.,(4,3,3,
3,3,3,3,4),(-41.7920422632082,-40.932246452925,-39.9338989784634,-38.9355515040018,
-37.9372040295402,-36.9388565550787,-35.9405090806171,-35.5088569560286),
 .UNSPECIFIED.);
#660=B_SPLINE_CURVE_WITH_KNOTS('',3,(#24613,#24614,#24615,#24616,#24617,
#24618,#24619,#24620,#24621,#24622,#24623,#24624,#24625,#24626,#24627,#24628,
#24629,#24630,#24631,#24632,#24633,#24634),.UNSPECIFIED.,.F.,.F.,(4,3,3,
3,3,3,3,4),(32.5332269442662,32.9605884818026,33.9593941933724,34.9581999049422,
35.9570056165119,36.9558113280817,37.9546170396515,38.8164122514458),
 .UNSPECIFIED.);
#661=B_SPLINE_CURVE_WITH_KNOTS('',3,(#24639,#24640,#24641,#24642,#24643,
#24644,#24645,#24646,#24647,#24648,#24649,#24650,#24651,#24652,#24653,#24654,
#24655,#24656,#24657,#24658,#24659,#24660,#24661,#24662,#24663),
 .UNSPECIFIED.,.F.,.F.,(4,3,3,3,3,3,3,3,4),(-48.0752275703878,-47.9206787741561,
-46.9223312996945,-45.9239838252329,-44.9256363507713,-43.9272888763097,
-42.9289414018482,-41.9305939273866,-41.7920422632082),.UNSPECIFIED.);
#662=B_SPLINE_CURVE_WITH_KNOTS('',3,(#24664,#24665,#24666,#24667,#24668,
#24669,#24670,#24671,#24672,#24673,#24674,#24675,#24676,#24677,#24678,#24679,
#24680,#24681,#24682,#24683,#24684,#24685,#24686,#24687,#24688),
 .UNSPECIFIED.,.F.,.F.,(4,3,3,3,3,3,3,3,4),(38.8164122514458,38.9534227512213,
39.952228462791,40.9510341743608,41.9498398859306,42.9486455975004,43.9474513090701,
44.9462570206399,45.0995975586254),.UNSPECIFIED.);
#663=B_SPLINE_CURVE_WITH_KNOTS('',3,(#24693,#24694,#24695,#24696,#24697,
#24698,#24699,#24700,#24701,#24702,#24703,#24704,#24705,#24706,#24707,#24708,
#24709,#24710,#24711,#24712,#24713,#24714),.UNSPECIFIED.,.F.,.F.,(4,3,3,
3,3,3,3,4),(-54.3584128775673,-53.9107636209256,-52.912416146464,-51.9140686720024,
-50.9157211975408,-49.9173737230793,-48.9190262486177,-48.0752275703878),
 .UNSPECIFIED.);
#664=B_SPLINE_CURVE_WITH_KNOTS('',3,(#24715,#24716,#24717,#24718,#24719,
#24720,#24721,#24722,#24723,#24724,#24725,#24726,#24727,#24728,#24729,#24730,
#24731,#24732,#24733,#24734,#24735,#24736),.UNSPECIFIED.,.F.,.F.,(4,3,3,
3,3,3,3,4),(45.0995975586254,45.9450627322097,46.9438684437795,47.9426741553493,
48.941479866919,49.9402855784888,50.9390912900586,51.382782865805),
 .UNSPECIFIED.);
#665=B_SPLINE_CURVE_WITH_KNOTS('',3,(#24741,#24742,#24743,#24744,#24745,
#24746,#24747,#24748,#24749,#24750,#24751,#24752,#24753,#24754,#24755,#24756,
#24757,#24758,#24759,#24760,#24761,#24762),.UNSPECIFIED.,.F.,.F.,(4,3,3,
3,3,3,3,4),(-60.6415981847469,-59.9008484676951,-58.9025009932335,-57.9041535187719,
-56.9058060443103,-55.9074585698488,-54.9091110953872,-54.3584128775673),
 .UNSPECIFIED.);
#666=B_SPLINE_CURVE_WITH_KNOTS('',3,(#24763,#24764,#24765,#24766,#24767,
#24768,#24769,#24770,#24771,#24772,#24773,#24774,#24775,#24776,#24777,#24778,
#24779,#24780,#24781,#24782,#24783,#24784),.UNSPECIFIED.,.F.,.F.,(4,3,3,
3,3,3,3,4),(51.382782865805,51.9378970016283,52.9367027131981,53.9355084247679,
54.9343141363377,55.9331198479074,56.9319255594772,57.6659681729846),
 .UNSPECIFIED.);
#667=B_SPLINE_CURVE_WITH_KNOTS('',3,(#24789,#24790,#24791,#24792,#24793,
#24794,#24795,#24796,#24797,#24798,#24799,#24800,#24801,#24802,#24803,#24804,
#24805,#24806,#24807,#24808,#24809,#24810,#24811,#24812,#24813),
 .UNSPECIFIED.,.F.,.F.,(4,3,3,3,3,3,3,3,4),(-66.9247834919265,-66.8892807889262,
-65.8909333144646,-64.892585840003,-63.8942383655414,-62.8958908910799,
-61.8975434166182,-60.8991959421567,-60.6415981847469),.UNSPECIFIED.);
#668=B_SPLINE_CURVE_WITH_KNOTS('',3,(#24814,#24815,#24816,#24817,#24818,
#24819,#24820,#24821,#24822,#24823,#24824,#24825,#24826,#24827,#24828,#24829,
#24830,#24831,#24832,#24833,#24834,#24835,#24836,#24837,#24838),
 .UNSPECIFIED.,.F.,.F.,(4,3,3,3,3,3,3,3,4),(57.6659681729846,57.930731271047,
58.9295369826168,59.9283426941866,60.9271484057563,61.9259541173261,62.9247598288959,
63.9235655404657,63.9491534801642),.UNSPECIFIED.);
#669=B_SPLINE_CURVE_WITH_KNOTS('',3,(#24843,#24844,#24845,#24846,#24847,
#24848,#24849,#24850,#24851,#24852,#24853,#24854,#24855,#24856,#24857,#24858,
#24859,#24860,#24861,#24862,#24863,#24864),.UNSPECIFIED.,.F.,.F.,(4,3,3,
3,3,3,3,4),(-73.2079687991061,-72.8793656356957,-71.8810181612341,-70.8826706867726,
-69.8843232123109,-68.8859757378494,-67.8876282633878,-66.9247834919265),
 .UNSPECIFIED.);
#670=B_SPLINE_CURVE_WITH_KNOTS('',3,(#24865,#24866,#24867,#24868,#24869,
#24870,#24871,#24872,#24873,#24874,#24875,#24876,#24877,#24878,#24879,#24880,
#24881,#24882,#24883,#24884,#24885,#24886),.UNSPECIFIED.,.F.,.F.,(4,3,3,
3,3,3,3,4),(63.9491534801642,64.9223712520354,65.9211769636052,66.919982675175,
67.9187883867447,68.9175940983145,69.9163998098843,70.2323387873437),
 .UNSPECIFIED.);
#671=B_SPLINE_CURVE_WITH_KNOTS('',3,(#24891,#24892,#24893,#24894,#24895,
#24896,#24897,#24898,#24899,#24900,#24901,#24902,#24903,#24904,#24905,#24906,
#24907,#24908,#24909,#24910,#24911,#24912),.UNSPECIFIED.,.F.,.F.,(4,3,3,
3,3,3,3,4),(-79.4911541062857,-78.8694504824652,-77.8711030080036,-76.8727555335421,
-75.8744080590805,-74.8760605846189,-73.8777131101573,-73.2079687991061),
 .UNSPECIFIED.);
#672=B_SPLINE_CURVE_WITH_KNOTS('',3,(#24913,#24914,#24915,#24916,#24917,
#24918,#24919,#24920,#24921,#24922,#24923,#24924,#24925,#24926,#24927,#24928,
#24929,#24930,#24931,#24932,#24933,#24934),.UNSPECIFIED.,.F.,.F.,(4,3,3,
3,3,3,3,4),(70.2323387873437,70.9152055214541,71.9140112330238,72.9128169445936,
73.9116226561634,74.9104283677332,75.909234079303,76.5155240945233),
 .UNSPECIFIED.);
#673=B_SPLINE_CURVE_WITH_KNOTS('',3,(#24939,#24940,#24941,#24942,#24943,
#24944,#24945,#24946,#24947,#24948,#24949,#24950,#24951,#24952,#24953,#24954,
#24955,#24956,#24957,#24958,#24959,#24960),.UNSPECIFIED.,.F.,.F.,(4,3,3,
3,3,3,3,4),(-85.7743394134653,-84.8595353292348,-83.8611878547731,-82.8628403803116,
-81.86449290585,-80.8661454313884,-79.8677979569268,-79.4911541062857),
 .UNSPECIFIED.);
#674=B_SPLINE_CURVE_WITH_KNOTS('',3,(#24961,#24962,#24963,#24964,#24965,
#24966,#24967,#24968,#24969,#24970,#24971,#24972,#24973,#24974,#24975,#24976,
#24977,#24978,#24979,#24980,#24981,#24982),.UNSPECIFIED.,.F.,.F.,(4,3,3,
3,3,3,3,4),(76.5155240945233,76.9080397908727,77.9068455024425,78.9056512140123,
79.9044569255821,80.9032626371518,81.9020683487216,82.7987094017029),
 .UNSPECIFIED.);
#675=B_SPLINE_CURVE_WITH_KNOTS('',3,(#24987,#24988,#24989,#24990,#24991,
#24992,#24993,#24994,#24995,#24996,#24997,#24998,#24999,#25000,#25001,#25002,
#25003,#25004,#25005,#25006,#25007,#25008,#25009,#25010,#25011),
 .UNSPECIFIED.,.F.,.F.,(4,3,3,3,3,3,3,3,4),(-92.0575247206449,-91.8479676504658,
-90.8496201760042,-89.8512727015427,-88.8529252270811,-87.8545777526195,
-86.8562302781579,-85.8578828036963,-85.7743394134653),.UNSPECIFIED.);
#676=B_SPLINE_CURVE_WITH_KNOTS('',3,(#25012,#25013,#25014,#25015,#25016,
#25017,#25018,#25019,#25020,#25021,#25022,#25023,#25024,#25025,#25026,#25027,
#25028,#25029,#25030,#25031,#25032,#25033,#25034,#25035,#25036),
 .UNSPECIFIED.,.F.,.F.,(4,3,3,3,3,3,3,3,4),(82.7987094017029,82.9008740602914,
83.8996797718612,84.8984854834309,85.8972911950007,86.8960969065705,87.8949026181403,
88.8937083297101,89.0818947088825),.UNSPECIFIED.);
#677=B_SPLINE_CURVE_WITH_KNOTS('',3,(#25041,#25042,#25043,#25044,#25045,
#25046,#25047,#25048,#25049,#25050,#25051,#25052,#25053,#25054,#25055,#25056,
#25057,#25058,#25059,#25060,#25061,#25062),.UNSPECIFIED.,.F.,.F.,(4,3,3,
3,3,3,3,4),(-98.3407100278245,-97.8380524972353,-96.8397050227737,-95.8413575483122,
-94.8430100738506,-93.844662599389,-92.8463151249274,-92.0575247206449),
 .UNSPECIFIED.);
#678=B_SPLINE_CURVE_WITH_KNOTS('',3,(#25063,#25064,#25065,#25066,#25067,
#25068,#25069,#25070,#25071,#25072,#25073,#25074,#25075,#25076,#25077,#25078,
#25079,#25080,#25081,#25082,#25083,#25084),.UNSPECIFIED.,.F.,.F.,(4,3,3,
3,3,3,3,4),(89.0818947088825,89.8925140412798,90.8913197528496,91.8901254644194,
92.8889311759891,93.8877368875589,94.8865425991287,95.3650800160621),
 .UNSPECIFIED.);
#679=B_SPLINE_CURVE_WITH_KNOTS('',3,(#25089,#25090,#25091,#25092,#25093,
#25094,#25095,#25096,#25097,#25098,#25099,#25100,#25101,#25102,#25103,#25104,
#25105,#25106,#25107,#25108,#25109,#25110),.UNSPECIFIED.,.F.,.F.,(4,3,3,
3,3,3,3,4),(-104.623895335004,-103.828137344005,-102.829789869543,-101.831442395082,
-100.83309492062,-99.8347474461585,-98.8363999716969,-98.3407100278245),
 .UNSPECIFIED.);
#680=B_SPLINE_CURVE_WITH_KNOTS('',3,(#25111,#25112,#25113,#25114,#25115,
#25116,#25117,#25118,#25119,#25120,#25121,#25122,#25123,#25124,#25125,#25126,
#25127,#25128,#25129,#25130,#25131,#25132),.UNSPECIFIED.,.F.,.F.,(4,3,3,
3,3,3,3,4),(95.3650800160621,95.8853483106984,96.8841540222682,97.882959733838,
98.8817654454078,99.8805711569776,100.879376868547,101.648265323242),
 .UNSPECIFIED.);
#681=B_SPLINE_CURVE_WITH_KNOTS('',3,(#25137,#25138,#25139,#25140,#25141,
#25142,#25143,#25144,#25145,#25146,#25147,#25148,#25149,#25150,#25151,#25152,
#25153,#25154,#25155,#25156,#25157,#25158,#25159,#25160,#25161),
 .UNSPECIFIED.,.F.,.F.,(4,3,3,3,3,3,3,3,4),(-110.907080642184,-110.816569665236,
-109.818222190774,-108.819874716313,-107.821527241851,-106.82317976739,
-105.824832292928,-104.826484818466,-104.623895335004),.UNSPECIFIED.);
#682=B_SPLINE_CURVE_WITH_KNOTS('',3,(#25162,#25163,#25164,#25165,#25166,
#25167,#25168,#25169,#25170,#25171,#25172,#25173,#25174,#25175,#25176,#25177,
#25178,#25179,#25180,#25181,#25182,#25183,#25184,#25185,#25186),
 .UNSPECIFIED.,.F.,.F.,(4,3,3,3,3,3,3,3,4),(101.648265323242,101.878182580117,
102.876988291687,103.875794003257,104.874599714826,105.873405426396,106.872211137966,
107.871016849536,107.931450630421),.UNSPECIFIED.);
#683=B_SPLINE_CURVE_WITH_KNOTS('',3,(#25191,#25192,#25193,#25194,#25195,
#25196,#25197,#25198,#25199,#25200,#25201,#25202,#25203,#25204,#25205,#25206,
#25207,#25208,#25209,#25210,#25211,#25212),.UNSPECIFIED.,.F.,.F.,(4,3,3,
3,3,3,3,4),(-117.190265949363,-116.806654512005,-115.808307037544,-114.809959563082,
-113.811612088621,-112.813264614159,-111.814917139698,-110.907080642184),
 .UNSPECIFIED.);
#684=B_SPLINE_CURVE_WITH_KNOTS('',3,(#25213,#25214,#25215,#25216,#25217,
#25218,#25219,#25220,#25221,#25222,#25223,#25224,#25225,#25226,#25227,#25228,
#25229,#25230,#25231,#25232,#25233,#25234),.UNSPECIFIED.,.F.,.F.,(4,3,3,
3,3,3,3,4),(107.931450630421,108.869822561106,109.868628272675,110.867433984245,
111.866239695815,112.865045407385,113.863851118954,114.214635937601),
 .UNSPECIFIED.);
#685=B_SPLINE_CURVE_WITH_KNOTS('',3,(#25239,#25240,#25241,#25242,#25243,
#25244,#25245,#25246,#25247,#25248,#25249,#25250,#25251,#25252,#25253,#25254,
#25255,#25256,#25257,#25258,#25259,#25260),.UNSPECIFIED.,.F.,.F.,(4,3,3,
3,3,3,3,4),(-123.473451256543,-122.796739358775,-121.798391884313,-120.800044409852,
-119.80169693539,-118.803349460929,-117.805001986467,-117.190265949363),
 .UNSPECIFIED.);
#686=B_SPLINE_CURVE_WITH_KNOTS('',3,(#25261,#25262,#25263,#25264,#25265,
#25266,#25267,#25268,#25269,#25270,#25271,#25272,#25273,#25274,#25275,#25276,
#25277,#25278,#25279,#25280,#25281,#25282),.UNSPECIFIED.,.F.,.F.,(4,3,3,
3,3,3,3,4),(114.214635937601,114.862656830524,115.861462542094,116.860268253664,
117.859073965234,118.857879676803,119.856685388373,120.49782124478),
 .UNSPECIFIED.);
#687=B_SPLINE_CURVE_WITH_KNOTS('',3,(#25287,#25288,#25289,#25290,#25291,
#25292,#25293,#25294,#25295,#25296,#25297,#25298,#25299,#25300,#25301,#25302,
#25303,#25304,#25305,#25306,#25307,#25308),.UNSPECIFIED.,.F.,.F.,(4,3,3,
3,3,3,3,4),(-129.756636563722,-128.786824205544,-127.788476731083,-126.790129256621,
-125.79178178216,-124.793434307698,-123.795086833237,-123.473451256543),
 .UNSPECIFIED.);
#688=B_SPLINE_CURVE_WITH_KNOTS('',3,(#25309,#25310,#25311,#25312,#25313,
#25314,#25315,#25316,#25317,#25318,#25319,#25320,#25321,#25322,#25323,#25324,
#25325,#25326,#25327,#25328,#25329,#25330),.UNSPECIFIED.,.F.,.F.,(4,3,3,
3,3,3,3,4),(120.49782124478,120.855491099943,121.854296811513,122.853102523082,
123.851908234652,124.850713946222,125.849519657792,126.78100655196),
 .UNSPECIFIED.);
#689=B_SPLINE_CURVE_WITH_KNOTS('',3,(#25335,#25336,#25337,#25338,#25339,
#25340,#25341,#25342,#25343,#25344,#25345,#25346,#25347,#25348,#25349,#25350,
#25351,#25352,#25353,#25354,#25355,#25356,#25357,#25358,#25359),
 .UNSPECIFIED.,.F.,.F.,(4,3,3,3,3,3,3,3,4),(-136.039821870902,-135.775256526776,
-134.776909052314,-133.778561577852,-132.780214103391,-131.781866628929,
-130.783519154468,-129.785171680006,-129.756636563722),.UNSPECIFIED.);
#690=B_SPLINE_CURVE_WITH_KNOTS('',3,(#25360,#25361,#25362,#25363,#25364,
#25365,#25366,#25367,#25368,#25369,#25370,#25371,#25372,#25373,#25374,#25375,
#25376,#25377,#25378,#25379,#25380,#25381,#25382,#25383,#25384),
 .UNSPECIFIED.,.F.,.F.,(4,3,3,3,3,3,3,3,4),(126.78100655196,126.848325369362,
127.847131080931,128.845936792501,129.844742504071,130.843548215641,131.84235392721,
132.84115963878,133.06419185914),.UNSPECIFIED.);
#691=B_SPLINE_CURVE_WITH_KNOTS('',3,(#25389,#25390,#25391,#25392,#25393,
#25394,#25395,#25396,#25397,#25398,#25399,#25400,#25401,#25402,#25403,#25404,
#25405,#25406,#25407,#25408,#25409,#25410),.UNSPECIFIED.,.F.,.F.,(4,3,3,
3,3,3,3,4),(-142.323007178082,-141.765341373545,-140.766993899083,-139.768646424622,
-138.77029895016,-137.771951475699,-136.773604001237,-136.039821870902),
 .UNSPECIFIED.);
#692=B_SPLINE_CURVE_WITH_KNOTS('',3,(#25411,#25412,#25413,#25414,#25415,
#25416,#25417,#25418,#25419,#25420,#25421,#25422,#25423,#25424,#25425,#25426,
#25427,#25428,#25429,#25430,#25431,#25432),.UNSPECIFIED.,.F.,.F.,(4,3,3,
3,3,3,3,4),(133.06419185914,133.83996535035,134.83877106192,135.83757677349,
136.836382485059,137.835188196629,138.833993908199,139.347377166319),
 .UNSPECIFIED.);
#693=B_SPLINE_CURVE_WITH_KNOTS('',3,(#25437,#25438,#25439,#25440,#25441,
#25442,#25443,#25444,#25445,#25446,#25447,#25448,#25449,#25450,#25451,#25452,
#25453,#25454,#25455,#25456,#25457,#25458),.UNSPECIFIED.,.F.,.F.,(4,3,3,
3,3,3,3,4),(-148.606192485261,-147.755426220315,-146.757078745853,-145.758731271391,
-144.76038379693,-143.762036322468,-142.763688848007,-142.323007178082),
 .UNSPECIFIED.);
#694=B_SPLINE_CURVE_WITH_KNOTS('',3,(#25459,#25460,#25461,#25462,#25463,
#25464,#25465,#25466,#25467,#25468,#25469,#25470,#25471,#25472,#25473,#25474,
#25475,#25476,#25477,#25478,#25479,#25480),.UNSPECIFIED.,.F.,.F.,(4,3,3,
3,3,3,3,4),(139.347377166319,139.832799619769,140.831605331338,141.830411042908,
142.829216754478,143.828022466048,144.826828177618,145.630562473499),
 .UNSPECIFIED.);
#695=B_SPLINE_CURVE_WITH_KNOTS('',3,(#25486,#25487,#25488,#25489,#25490,
#25491,#25492,#25493,#25494,#25495),.UNSPECIFIED.,.F.,.F.,(4,1,1,1,1,1,
1,4),(160.221225333079,160.368806542595,161.367154017056,162.365501491518,
163.363848965979,164.362196440441,165.360543914902,166.358891389364),
 .UNSPECIFIED.);
#696=B_SPLINE_CURVE_WITH_KNOTS('',3,(#25498,#25499,#25500,#25501,#25502,
#25503,#25504,#25505),.UNSPECIFIED.,.F.,.F.,(4,1,1,1,1,4),(160.221225333079,
161.124751422577,162.123557134147,163.122362845716,164.121168557286,165.119974268856),
 .UNSPECIFIED.);
#697=B_SPLINE_CURVE_WITH_KNOTS('',3,(#25510,#25511,#25512,#25513,#25514,
#25515,#25516,#25517,#25518,#25519),.UNSPECIFIED.,.F.,.F.,(4,1,1,1,1,1,
1,4),(153.9380400259,154.378721695825,155.377069170287,156.375416644748,
157.37376411921,158.372111593671,159.370459068133,160.221225333079),
 .UNSPECIFIED.);
#698=B_SPLINE_CURVE_WITH_KNOTS('',3,(#25520,#25521,#25522,#25523,#25524,
#25525,#25526,#25527,#25528,#25529,#25530),.UNSPECIFIED.,.F.,.F.,(4,1,1,
1,1,1,1,1,4),(153.9380400259,154.133111441588,155.131917153158,156.130722864728,
157.129528576298,158.128334287868,159.127139999437,160.125945711007,160.221225333079),
 .UNSPECIFIED.);
#699=B_SPLINE_CURVE_WITH_KNOTS('',3,(#25535,#25536,#25537,#25538,#25539,
#25540,#25541,#25542,#25543,#25544),.UNSPECIFIED.,.F.,.F.,(4,1,1,1,1,1,
1,4),(147.65485471872,148.388636849056,149.386984323517,150.385331797979,
151.38367927244,152.382026746902,153.380374221363,153.9380400259),
 .UNSPECIFIED.);
#700=B_SPLINE_CURVE_WITH_KNOTS('',3,(#25545,#25546,#25547,#25548,#25549,
#25550,#25551,#25552,#25553,#25554),.UNSPECIFIED.,.F.,.F.,(4,1,1,1,1,1,
1,4),(147.65485471872,148.14027717217,149.13908288374,150.137888595309,
151.136694306879,152.135500018449,153.134305730019,153.9380400259),
 .UNSPECIFIED.);
#701=B_SPLINE_CURVE_WITH_KNOTS('',3,(#25559,#25560,#25561,#25562,#25563,
#25564,#25565,#25566,#25567,#25568,#25569),.UNSPECIFIED.,.F.,.F.,(4,1,1,
1,1,1,1,1,4),(141.371669411541,141.400204527824,142.398552002286,143.396899476748,
144.395246951209,145.393594425671,146.391941900132,147.390289374594,147.65485471872),
 .UNSPECIFIED.);
#702=B_SPLINE_CURVE_WITH_KNOTS('',3,(#25570,#25571,#25572,#25573,#25574,
#25575,#25576,#25577,#25578,#25579),.UNSPECIFIED.,.F.,.F.,(4,1,1,1,1,1,
1,4),(141.371669411541,142.147442902751,143.146248614321,144.145054325891,
145.14386003746,146.14266574903,147.1414714606,147.65485471872),
 .UNSPECIFIED.);
#703=B_SPLINE_CURVE_WITH_KNOTS('',3,(#25584,#25585,#25586,#25587,#25588,
#25589,#25590,#25591,#25592,#25593),.UNSPECIFIED.,.F.,.F.,(4,1,1,1,1,1,
1,4),(135.088484104361,135.410119681055,136.408467155516,137.406814629978,
138.40516210444,139.403509578901,140.401857053363,141.371669411541),
 .UNSPECIFIED.);
#704=B_SPLINE_CURVE_WITH_KNOTS('',3,(#25594,#25595,#25596,#25597,#25598,
#25599,#25600,#25601,#25602,#25603,#25604),.UNSPECIFIED.,.F.,.F.,(4,1,1,
1,1,1,1,1,4),(135.088484104361,135.155802921763,136.154608633332,137.153414344902,
138.152220056472,139.151025768042,140.149831479612,141.148637191181,141.371669411541),
 .UNSPECIFIED.);
#705=B_SPLINE_CURVE_WITH_KNOTS('',3,(#25609,#25610,#25611,#25612,#25613,
#25614,#25615,#25616,#25617,#25618),.UNSPECIFIED.,.F.,.F.,(4,1,1,1,1,1,
1,4),(128.805298797182,129.420034834285,130.418382308747,131.416729783209,
132.41507725767,133.413424732132,134.411772206593,135.088484104361),
 .UNSPECIFIED.);
#706=B_SPLINE_CURVE_WITH_KNOTS('',3,(#25619,#25620,#25621,#25622,#25623,
#25624,#25625,#25626,#25627,#25628),.UNSPECIFIED.,.F.,.F.,(4,1,1,1,1,1,
1,4),(128.805298797182,129.162968652344,130.161774363914,131.160580075484,
132.159385787053,133.158191498623,134.156997210193,135.088484104361),
 .UNSPECIFIED.);
#707=B_SPLINE_CURVE_WITH_KNOTS('',3,(#25633,#25634,#25635,#25636,#25637,
#25638,#25639,#25640,#25641,#25642),.UNSPECIFIED.,.F.,.F.,(4,1,1,1,1,1,
1,4),(122.522113490002,123.429949987516,124.428297461977,125.426644936439,
126.424992410901,127.423339885362,128.421687359824,128.805298797182),
 .UNSPECIFIED.);
#708=B_SPLINE_CURVE_WITH_KNOTS('',3,(#25643,#25644,#25645,#25646,#25647,
#25648,#25649,#25650,#25651,#25652),.UNSPECIFIED.,.F.,.F.,(4,1,1,1,1,1,
1,4),(122.522113490002,123.170134382925,124.168940094495,125.167745806065,
126.166551517635,127.165357229204,128.164162940774,128.805298797182),
 .UNSPECIFIED.);
#709=B_SPLINE_CURVE_WITH_KNOTS('',3,(#25657,#25658,#25659,#25660,#25661,
#25662,#25663,#25664,#25665,#25666,#25667),.UNSPECIFIED.,.F.,.F.,(4,1,1,
1,1,1,1,1,4),(116.238928182822,116.441517666285,117.439865140746,118.438212615208,
119.43656008967,120.434907564131,121.433255038593,122.431602513054,122.522113490002),
 .UNSPECIFIED.);
#710=B_SPLINE_CURVE_WITH_KNOTS('',3,(#25668,#25669,#25670,#25671,#25672,
#25673,#25674,#25675,#25676,#25677),.UNSPECIFIED.,.F.,.F.,(4,1,1,1,1,1,
1,4),(116.238928182822,117.177300113507,118.176105825076,119.174911536646,
120.173717248216,121.172522959786,122.171328671356,122.522113490002),
 .UNSPECIFIED.);
#711=B_SPLINE_CURVE_WITH_KNOTS('',3,(#25682,#25683,#25684,#25685,#25686,
#25687,#25688,#25689,#25690,#25691),.UNSPECIFIED.,.F.,.F.,(4,1,1,1,1,1,
1,4),(109.955742875643,110.451432819515,111.449780293977,112.448127768438,
113.4464752429,114.444822717362,115.443170191823,116.238928182822),
 .UNSPECIFIED.);
#712=B_SPLINE_CURVE_WITH_KNOTS('',3,(#25692,#25693,#25694,#25695,#25696,
#25697,#25698,#25699,#25700,#25701,#25702),.UNSPECIFIED.,.F.,.F.,(4,1,1,
1,1,1,1,1,4),(109.955742875643,110.185660132518,111.184465844088,112.183271555658,
113.182077267228,114.180882978797,115.179688690367,116.178494401937,116.238928182822),
 .UNSPECIFIED.);
#713=B_SPLINE_CURVE_WITH_KNOTS('',3,(#25707,#25708,#25709,#25710,#25711,
#25712,#25713,#25714,#25715,#25716),.UNSPECIFIED.,.F.,.F.,(4,1,1,1,1,1,
1,4),(103.672557568463,104.461347972746,105.459695447207,106.458042921669,
107.456390396131,108.454737870592,109.453085345054,109.955742875643),
 .UNSPECIFIED.);
#714=B_SPLINE_CURVE_WITH_KNOTS('',3,(#25717,#25718,#25719,#25720,#25721,
#25722,#25723,#25724,#25725,#25726),.UNSPECIFIED.,.F.,.F.,(4,1,1,1,1,1,
1,4),(103.672557568463,104.1928258631,105.191631574669,106.190437286239,
107.189242997809,108.188048709379,109.186854420948,109.955742875643),
 .UNSPECIFIED.);
#715=B_SPLINE_CURVE_WITH_KNOTS('',3,(#25731,#25732,#25733,#25734,#25735,
#25736,#25737,#25738,#25739,#25740,#25741),.UNSPECIFIED.,.F.,.F.,(4,1,1,
1,1,1,1,1,4),(97.3893722612837,97.4729156515147,98.4712631259763,99.4696106004379,
100.467958074899,101.466305549361,102.464653023823,103.463000498284,103.672557568463),
 .UNSPECIFIED.);
#716=B_SPLINE_CURVE_WITH_KNOTS('',3,(#25742,#25743,#25744,#25745,#25746,
#25747,#25748,#25749,#25750,#25751),.UNSPECIFIED.,.F.,.F.,(4,1,1,1,1,1,
1,4),(97.3893722612837,98.199991593681,99.1987973052507,100.197603016821,
101.19640872839,102.19521443996,103.19402015153,103.672557568463),
 .UNSPECIFIED.);
#717=B_SPLINE_CURVE_WITH_KNOTS('',3,(#25756,#25757,#25758,#25759,#25760,
#25761,#25762,#25763,#25764,#25765),.UNSPECIFIED.,.F.,.F.,(4,1,1,1,1,1,
1,4),(91.1061869541041,91.4828308047452,92.4811782792068,93.4795257536684,
94.4778732281299,95.4762207025915,96.4745681770531,97.3893722612837),
 .UNSPECIFIED.);
#718=B_SPLINE_CURVE_WITH_KNOTS('',3,(#25766,#25767,#25768,#25769,#25770,
#25771,#25772,#25773,#25774,#25775,#25776),.UNSPECIFIED.,.F.,.F.,(4,1,1,
1,1,1,1,1,4),(91.1061869541041,91.2083516126925,92.2071573242623,93.2059630358321,
94.2047687474019,95.2035744589716,96.2023801705414,97.2011858821112,97.3893722612837),
 .UNSPECIFIED.);
#719=B_SPLINE_CURVE_WITH_KNOTS('',3,(#25781,#25782,#25783,#25784,#25785,
#25786,#25787,#25788,#25789,#25790),.UNSPECIFIED.,.F.,.F.,(4,1,1,1,1,1,
1,4),(84.8230016469245,85.4927459579757,86.4910934324373,87.4894409068988,
88.4877883813604,89.486135855822,90.4844833302836,91.1061869541041),
 .UNSPECIFIED.);
#720=B_SPLINE_CURVE_WITH_KNOTS('',3,(#25791,#25792,#25793,#25794,#25795,
#25796,#25797,#25798,#25799,#25800),.UNSPECIFIED.,.F.,.F.,(4,1,1,1,1,1,
1,4),(84.8230016469245,85.2155173432739,86.2143230548436,87.2131287664134,
88.2119344779832,89.210740189553,90.2095459011228,91.1061869541041),
 .UNSPECIFIED.);
#721=B_SPLINE_CURVE_WITH_KNOTS('',3,(#25805,#25806,#25807,#25808,#25809,
#25810,#25811,#25812,#25813,#25814),.UNSPECIFIED.,.F.,.F.,(4,1,1,1,1,1,
1,4),(78.5398163397449,79.5026611112062,80.5010085856677,81.4993560601293,
82.4977035345909,83.4960510090525,84.4943984835141,84.8230016469245),
 .UNSPECIFIED.);
#722=B_SPLINE_CURVE_WITH_KNOTS('',3,(#25815,#25816,#25817,#25818,#25819,
#25820,#25821,#25822,#25823,#25824),.UNSPECIFIED.,.F.,.F.,(4,1,1,1,1,1,
1,4),(78.5398163397449,79.2226830738552,80.221488785425,81.2202944969948,
82.2191002085646,83.2179059201343,84.2167116317041,84.8230016469245),
 .UNSPECIFIED.);
#723=B_SPLINE_CURVE_WITH_KNOTS('',3,(#25829,#25830,#25831,#25832,#25833,
#25834,#25835,#25836,#25837,#25838,#25839),.UNSPECIFIED.,.F.,.F.,(4,1,1,
1,1,1,1,1,4),(72.2566310325653,72.5142287899751,73.5125762644366,74.5109237388982,
75.5092712133598,76.5076186878214,77.505966162283,78.5043136367446,78.5398163397449),
 .UNSPECIFIED.);
#724=B_SPLINE_CURVE_WITH_KNOTS('',3,(#25840,#25841,#25842,#25843,#25844,
#25845,#25846,#25847,#25848,#25849),.UNSPECIFIED.,.F.,.F.,(4,1,1,1,1,1,
1,4),(72.2566310325653,73.2298488044366,74.2286545160063,75.2274602275761,
76.2262659391459,77.2250716507157,78.2238773622854,78.5398163397449),
 .UNSPECIFIED.);
#725=B_SPLINE_CURVE_WITH_KNOTS('',3,(#25854,#25855,#25856,#25857,#25858,
#25859,#25860,#25861,#25862,#25863),.UNSPECIFIED.,.F.,.F.,(4,1,1,1,1,1,
1,4),(65.9734457253857,66.5241439432056,67.5224914176671,68.5208388921287,
69.5191863665903,70.5175338410519,71.5158813155135,72.2566310325653),
 .UNSPECIFIED.);
#726=B_SPLINE_CURVE_WITH_KNOTS('',3,(#25864,#25865,#25866,#25867,#25868,
#25869,#25870,#25871,#25872,#25873,#25874),.UNSPECIFIED.,.F.,.F.,(4,1,1,
1,1,1,1,1,4),(65.9734457253857,66.2382088234481,67.2370145350179,68.2358202465877,
69.2346259581575,70.2334316697272,71.232237381297,72.2310430928668,72.2566310325653),
 .UNSPECIFIED.);
#727=B_SPLINE_CURVE_WITH_KNOTS('',3,(#25879,#25880,#25881,#25882,#25883,
#25884,#25885,#25886,#25887,#25888),.UNSPECIFIED.,.F.,.F.,(4,1,1,1,1,1,
1,4),(59.6902604182061,60.534059096436,61.5324065708976,62.5307540453592,
63.5291015198208,64.5274489942824,65.525796468744,65.9734457253857),
 .UNSPECIFIED.);
#728=B_SPLINE_CURVE_WITH_KNOTS('',3,(#25889,#25890,#25891,#25892,#25893,
#25894,#25895,#25896,#25897,#25898),.UNSPECIFIED.,.F.,.F.,(4,1,1,1,1,1,
1,4),(59.6902604182061,60.2453745540295,61.2441802655993,62.242985977169,
63.2417916887388,64.2405974003086,65.2394031118784,65.9734457253857),
 .UNSPECIFIED.);
#729=B_SPLINE_CURVE_WITH_KNOTS('',3,(#25903,#25904,#25905,#25906,#25907,
#25908,#25909,#25910,#25911,#25912,#25913),.UNSPECIFIED.,.F.,.F.,(4,1,1,
1,1,1,1,1,4),(53.4070751110265,53.545626775205,54.5439742496665,55.5423217241281,
56.5406691985897,57.5390166730513,58.5373641475129,59.5357116219745,59.6902604182061),
 .UNSPECIFIED.);
#730=B_SPLINE_CURVE_WITH_KNOTS('',3,(#25914,#25915,#25916,#25917,#25918,
#25919,#25920,#25921,#25922,#25923),.UNSPECIFIED.,.F.,.F.,(4,1,1,1,1,1,
1,4),(53.4070751110265,54.2525402846108,55.2513459961806,56.2501517077504,
57.2489574193202,58.2477631308899,59.2465688424597,59.6902604182061),
 .UNSPECIFIED.);
#731=B_SPLINE_CURVE_WITH_KNOTS('',3,(#25928,#25929,#25930,#25931,#25932,
#25933,#25934,#25935,#25936,#25937),.UNSPECIFIED.,.F.,.F.,(4,1,1,1,1,1,
1,4),(47.1238898038469,47.5555419284354,48.553889402897,49.5522368773586,
50.5505843518202,51.5489318262818,52.5472793007434,53.4070751110265),
 .UNSPECIFIED.);
#732=B_SPLINE_CURVE_WITH_KNOTS('',3,(#25938,#25939,#25940,#25941,#25942,
#25943,#25944,#25945,#25946,#25947,#25948),.UNSPECIFIED.,.F.,.F.,(4,1,1,
1,1,1,1,1,4),(47.1238898038469,47.2609003036224,48.2597060151922,49.258511726762,
50.2573174383317,51.2561231499015,52.2549288614713,53.2537345730411,53.4070751110265),
 .UNSPECIFIED.);
#733=B_SPLINE_CURVE_WITH_KNOTS('',3,(#25953,#25954,#25955,#25956,#25957,
#25958,#25959,#25960,#25961,#25962),.UNSPECIFIED.,.F.,.F.,(4,1,1,1,1,1,
1,4),(40.8407044966673,41.5654570816659,42.5638045561275,43.5621520305891,
44.5604995050507,45.5588469795123,46.5571944539738,47.1238898038469),
 .UNSPECIFIED.);
#734=B_SPLINE_CURVE_WITH_KNOTS('',3,(#25963,#25964,#25965,#25966,#25967,
#25968,#25969,#25970,#25971,#25972),.UNSPECIFIED.,.F.,.F.,(4,1,1,1,1,1,
1,4),(40.8407044966673,41.2680660342037,42.2668717457735,43.2656774573433,
44.2644831689131,45.2632888804829,46.2620945920526,47.1238898038469),
 .UNSPECIFIED.);
#735=B_SPLINE_CURVE_WITH_KNOTS('',3,(#25977,#25978,#25979,#25980,#25981,
#25982,#25983,#25984,#25985,#25986,#25987),.UNSPECIFIED.,.F.,.F.,(4,1,1,
1,1,1,1,1,4),(34.5575191894877,34.5770247604348,35.5753722348964,36.573719709358,
37.5720671838196,38.5704146582812,39.5687621327428,40.5671096072043,40.8407044966673),
 .UNSPECIFIED.);
#736=B_SPLINE_CURVE_WITH_KNOTS('',3,(#25988,#25989,#25990,#25991,#25992,
#25993,#25994,#25995,#25996,#25997),.UNSPECIFIED.,.F.,.F.,(4,1,1,1,1,1,
1,4),(34.5575191894877,35.2752317647851,36.2740374763549,37.2728431879246,
38.2716488994944,39.2704546110642,40.269260322634,40.8407044966673),
 .UNSPECIFIED.);
#737=B_SPLINE_CURVE_WITH_KNOTS('',3,(#26002,#26003,#26004,#26005,#26006,
#26007,#26008,#26009,#26010,#26011),.UNSPECIFIED.,.F.,.F.,(4,1,1,1,1,1,
1,4),(28.2743338823082,28.5869399136653,29.5852873881269,30.5836348625885,
31.5819823370501,32.5803298115117,33.5786772859732,34.5575191894877),
 .UNSPECIFIED.);
#738=B_SPLINE_CURVE_WITH_KNOTS('',3,(#26012,#26013,#26014,#26015,#26016,
#26017,#26018,#26019,#26020,#26021,#26022),.UNSPECIFIED.,.F.,.F.,(4,1,1,
1,1,1,1,1,4),(28.2743338823082,28.2835917837967,29.2823974953664,30.2812032069362,
31.280008918506,32.2788146300758,33.2776203416455,34.2764260532153,34.5575191894877),
 .UNSPECIFIED.);
#739=B_SPLINE_CURVE_WITH_KNOTS('',3,(#26027,#26028,#26029,#26030,#26031,
#26032,#26033,#26034,#26035,#26036),.UNSPECIFIED.,.F.,.F.,(4,1,1,1,1,1,
1,4),(21.9911485751286,22.5968550668958,23.5952025413574,24.593550015819,
25.5918974902806,26.5902449647422,27.5885924392037,28.2743338823082),
 .UNSPECIFIED.);
#740=B_SPLINE_CURVE_WITH_KNOTS('',3,(#26037,#26038,#26039,#26040,#26041,
#26042,#26043,#26044,#26045,#26046),.UNSPECIFIED.,.F.,.F.,(4,1,1,1,1,1,
1,4),(21.9911485751286,22.290757514378,23.2895632259478,24.2883689375176,
25.2871746490873,26.2859803606571,27.2847860722269,28.2743338823082),
 .UNSPECIFIED.);
#741=B_SPLINE_CURVE_WITH_KNOTS('',3,(#26051,#26052,#26053,#26054,#26055,
#26056,#26057,#26058,#26059,#26060),.UNSPECIFIED.,.F.,.F.,(4,1,1,1,1,1,
1,4),(15.707963267949,16.6067702201263,17.6051176945879,18.6034651690495,
19.6018126435111,20.6001601179726,21.5985075924342,21.9911485751286),
 .UNSPECIFIED.);
#742=B_SPLINE_CURVE_WITH_KNOTS('',3,(#26061,#26062,#26063,#26064,#26065,
#26066,#26067,#26068,#26069,#26070),.UNSPECIFIED.,.F.,.F.,(4,1,1,1,1,1,
1,4),(15.707963267949,16.2979232449593,17.2967289565291,18.2955346680989,
19.2943403796687,20.2931460912385,21.2919518028082,21.9911485751286),
 .UNSPECIFIED.);
#743=B_SPLINE_CURVE_WITH_KNOTS('',3,(#26073,#26074,#26075,#26076,#26077,
#26078,#26079,#26080,#26081,#26082,#26083,#26084,#26085,#26086,#26087,#26088,
#26089,#26090,#26091,#26092,#26093,#26094,#26095,#26096,#26097,#26098,#26099,
#26100,#26101,#26102,#26103,#26104,#26105,#26106,#26107,#26108,#26109,#26110,
#26111,#26112,#26113,#26114,#26115,#26116,#26117,#26118,#26119,#26120,#26121,
#26122,#26123,#26124,#26125,#26126,#26127,#26128,#26129,#26130,#26131,#26132,
#26133,#26134,#26135,#26136,#26137,#26138,#26139,#26140,#26141,#26142,#26143,
#26144,#26145,#26146,#26147,#26148,#26149,#26150,#26151,#26152,#26153,#26154,
#26155,#26156,#26157,#26158,#26159,#26160,#26161,#26162,#26163,#26164,#26165,
#26166,#26167,#26168,#26169,#26170,#26171,#26172,#26173,#26174,#26175,#26176,
#26177,#26178,#26179,#26180,#26181,#26182,#26183,#26184,#26185,#26186,#26187,
#26188,#26189,#26190,#26191,#26192,#26193,#26194,#26195,#26196,#26197,#26198,
#26199,#26200,#26201,#26202,#26203,#26204,#26205,#26206,#26207,#26208,#26209,
#26210,#26211,#26212,#26213,#26214,#26215,#26216,#26217,#26218,#26219,#26220,
#26221,#26222,#26223,#26224,#26225,#26226,#26227,#26228,#26229,#26230,#26231,
#26232,#26233,#26234,#26235,#26236,#26237,#26238,#26239,#26240,#26241,#26242,
#26243,#26244,#26245,#26246,#26247,#26248,#26249,#26250,#26251,#26252,#26253,
#26254,#26255,#26256,#26257,#26258,#26259,#26260,#26261,#26262,#26263,#26264,
#26265,#26266,#26267,#26268,#26269,#26270,#26271,#26272,#26273,#26274,#26275,
#26276,#26277,#26278,#26279,#26280,#26281,#26282,#26283,#26284,#26285,#26286,
#26287,#26288,#26289,#26290,#26291,#26292,#26293,#26294,#26295,#26296,#26297,
#26298,#26299,#26300,#26301,#26302,#26303,#26304),.UNSPECIFIED.,.F.,.F.,
(4,3,3,3,3,3,3,3,3,3,3,3,3,3,3,3,3,3,3,3,3,3,3,3,3,3,3,3,3,3,3,3,3,3,3,
3,3,3,3,3,3,3,3,3,3,3,3,3,3,3,3,3,3,3,3,3,3,3,3,3,3,3,3,3,3,3,3,3,3,3,3,
3,3,3,3,3,3,4),(-2.07787844821581,-2.04563640817454,-2.01260600406739,-1.99390262471517,
-1.97880815407869,-1.97343611688677,-1.93978265453417,-1.90587423526444,
-1.88438455677208,-1.87589993511254,-1.87071648916707,-1.83652656870669,
-1.80253536734925,-1.7682460873374,-1.75110144733148,-1.74333138277347,
-1.73705920337893,-1.73395680732556,-1.70122489773177,-1.66760788468754,
-1.63163034935991,-1.61589017765406,-1.60492981834386,-1.60020318232811,
-1.56577415958123,-1.53098947454713,-1.49635100238812,-1.4672101523077,
-1.46216466120046,-1.42716054566692,-1.39267814268788,-1.37978760206645,
-1.34531390132733,-1.33245646351828,-1.32592267957129,-1.32082668753048,
-1.28679878189102,-1.2516716099619,-1.21635641577775,-1.19129075085948,
-1.18499879133774,-1.18014246087519,-1.1446795062145,-1.10922024591651,
-1.07424600071327,-1.04503854857244,-1.03811338002803,-1.0158310964316,
-0.981392848951218,-0.946133107350497,-0.910369520876374,-0.899628872347486,
-0.89368994999567,-0.857962841308724,-0.82181130706931,-0.785718553763474,
-0.767732714465289,-0.754402261382112,-0.748013249342093,-0.711600160631613,
-0.675777877337977,-0.641831839377992,-0.620163722971144,-0.609175591942721,
-0.603763283335243,-0.56872451739821,-0.532416642828612,-0.495724942594248,
-0.470652071878519,-0.458093605572563,-0.451831603827856,-0.415093157349795,
-0.378123471546787,-0.341518871530435,-0.318330424199427,-0.308274893383926,
-0.301672805800084,-0.295141976868419),.UNSPECIFIED.);
#744=B_SPLINE_CURVE_WITH_KNOTS('',3,(#26306,#26307,#26308,#26309,#26310,
#26311,#26312,#26313,#26314,#26315,#26316,#26317,#26318,#26319,#26320,#26321,
#26322,#26323,#26324,#26325,#26326,#26327,#26328,#26329,#26330,#26331,#26332,
#26333,#26334,#26335,#26336,#26337,#26338,#26339,#26340,#26341,#26342,#26343,
#26344,#26345,#26346,#26347,#26348,#26349,#26350,#26351,#26352,#26353,#26354,
#26355,#26356,#26357,#26358,#26359,#26360,#26361,#26362,#26363,#26364,#26365,
#26366,#26367,#26368,#26369,#26370,#26371,#26372),.UNSPECIFIED.,.F.,.F.,
(4,3,3,3,3,3,3,3,3,3,3,3,3,3,3,3,3,3,3,3,3,3,4),(-0.560387248253829,-0.523489675423405,
-0.486909280826814,-0.451409765500931,-0.428581929912694,-0.422644096024468,
-0.417538776764712,-0.382486843658728,-0.360098423147984,-0.324342694600126,
-0.288456460870319,-0.277039646852259,-0.272658549855339,-0.23782854730266,
-0.202954723102529,-0.168490668078001,-0.147429334568251,-0.135539740506508,
-0.130645012249701,-0.0971180289394068,-0.0640503905793665,-0.0319885771286076,
0.),.UNSPECIFIED.);
#745=B_SPLINE_CURVE_WITH_KNOTS('',3,(#26375,#26376,#26377,#26378,#26379,
#26380,#26381,#26382,#26383,#26384,#26385,#26386,#26387,#26388,#26389,#26390,
#26391,#26392,#26393,#26394,#26395,#26396,#26397,#26398,#26399,#26400,#26401,
#26402,#26403,#26404,#26405),.UNSPECIFIED.,.F.,.F.,(4,3,3,3,3,3,3,3,3,3,
4),(-0.295141976868419,-0.258118008913044,-0.221832521729933,-0.184905796964689,
-0.161792572344103,-0.155196944416255,-0.149950158553442,-0.112462618915081,
-0.0749997768837546,-0.0374998884418773,0.),.UNSPECIFIED.);
#746=B_SPLINE_CURVE_WITH_KNOTS('',3,(#27042,#27043,#27044,#27045,#27046,
#27047,#27048,#27049),.UNSPECIFIED.,.F.,.F.,(4,1,1,1,1,4),(11.6150328478184,
12.61338032228,13.6117277967416,14.6100752712031,15.6084227456647,15.707963267949),
 .UNSPECIFIED.);
#747=B_SPLINE_CURVE_WITH_KNOTS('',3,(#27050,#27051,#27052,#27053,#27054,
#27055,#27056,#27057,#27058,#27059,#27060,#27061,#27062,#27063,#27064,#27065,
#27066,#27067,#27068,#27069,#27070,#27071,#27072,#27073,#27074,#27075,#27076,
#27077,#27078,#27079,#27080,#27081,#27082,#27083,#27084,#27085,#27086,#27087,
#27088,#27089,#27090,#27091,#27092,#27093,#27094,#27095,#27096,#27097,#27098,
#27099,#27100,#27101,#27102,#27103,#27104,#27105,#27106,#27107,#27108,#27109,
#27110,#27111,#27112,#27113,#27114,#27115,#27116,#27117,#27118,#27119,#27120,
#27121,#27122,#27123,#27124,#27125,#27126,#27127,#27128,#27129,#27130,#27131,
#27132,#27133,#27134,#27135,#27136,#27137,#27138,#27139,#27140,#27141,#27142,
#27143,#27144,#27145,#27146),.UNSPECIFIED.,.F.,.F.,(4,3,3,3,3,3,3,3,3,3,
3,3,3,3,3,3,3,3,3,3,3,3,3,3,3,3,3,3,3,3,3,3,4),(-0.75940314415766,-0.731099230044352,
-0.694405090916541,-0.673021753795954,-0.659792230351525,-0.653579099280099,
-0.615915673993481,-0.58296017686769,-0.568542146875157,-0.56016187063185,
-0.554528541316208,-0.518574457756444,-0.482794928028838,-0.44802285832865,
-0.424085067993276,-0.41225754927003,-0.407433722504049,-0.373002009397425,
-0.352271696987154,-0.317344582417244,-0.282174956583422,-0.274866834214802,
-0.269904808501567,-0.23562822660491,-0.201185303792214,-0.167047167238569,
-0.146166271333748,-0.135071182701311,-0.130169248221992,-0.0967451917617864,
-0.0637506042838665,-0.03178494031496,0.),.UNSPECIFIED.);
#748=B_SPLINE_CURVE_WITH_KNOTS('',3,(#27147,#27148,#27149,#27150,#27151,
#27152,#27153,#27154,#27155,#27156,#27157,#27158,#27159,#27160,#27161,#27162,
#27163,#27164,#27165),.UNSPECIFIED.,.F.,.F.,(4,3,3,3,3,3,4),(-153.229510295036,
-152.747163592623,-151.748816118161,-150.750468643699,-149.752121169238,
-148.753773694776,-148.606192485261),.UNSPECIFIED.);
#749=B_SPLINE_CURVE_WITH_KNOTS('',3,(#27168,#27169,#27170,#27171,#27172,
#27173,#27174,#27175,#27176),.UNSPECIFIED.,.F.,.F.,(4,1,1,1,1,1,4),(10.3761157273103,
11.3038946871105,12.3027003986802,13.30150611025,14.3003118218198,15.2991175333896,
15.707963267949),.UNSPECIFIED.);
#750=B_SPLINE_CURVE_WITH_KNOTS('',3,(#27818,#27819,#27820,#27821,#27822,
#27823,#27824,#27825,#27826,#27827,#27828,#27829,#27830,#27831,#27832,#27833,
#27834,#27835,#27836,#27837,#27838,#27839),.UNSPECIFIED.,.F.,.F.,(4,3,3,
3,3,3,3,4),(145.630562473499,145.825633889187,146.824439600757,147.823245312327,
148.822051023897,149.820856735466,150.819662447036,151.160872120127),
 .UNSPECIFIED.);
#751=B_SPLINE_CURVE_WITH_KNOTS('',3,(#27840,#27841,#27842,#27843,#27844,
#27845,#27846,#27847,#27848,#27849,#27850,#27851,#27852,#27853,#27854,#27855,
#27856,#27857,#27858,#27859,#27860,#27861,#27862,#27863,#27864,#27865,#27866,
#27867,#27868,#27869,#27870,#27871,#27872,#27873,#27874,#27875,#27876,#27877,
#27878,#27879,#27880,#27881,#27882,#27883,#27884,#27885,#27886,#27887,#27888,
#27889,#27890,#27891,#27892,#27893,#27894,#27895,#27896,#27897,#27898,#27899,
#27900,#27901,#27902,#27903,#27904,#27905,#27906,#27907,#27908,#27909,#27910,
#27911,#27912,#27913,#27914,#27915,#27916,#27917,#27918,#27919,#27920,#27921,
#27922,#27923,#27924,#27925,#27926,#27927,#27928,#27929,#27930,#27931,#27932,
#27933,#27934,#27935,#27936),.UNSPECIFIED.,.F.,.F.,(4,3,3,3,3,3,3,3,3,3,
3,3,3,3,3,3,3,3,3,3,3,3,3,3,3,3,3,3,3,3,3,3,4),(-0.761903739928579,-0.737714840814909,
-0.705408016786385,-0.685226614670373,-0.676627161339419,-0.668738660960247,
-0.635678094311993,-0.604031530389268,-0.590186158673076,-0.583843379993958,
-0.578312161070379,-0.543995147795815,-0.509206617715678,-0.474634013675463,
-0.451601905989146,-0.445054542245308,-0.439067220218037,-0.403526955466083,
-0.382505582930195,-0.348068670802762,-0.312989133154698,-0.301425205487243,
-0.296110141258073,-0.261171717718659,-0.225140081955213,-0.188826370911274,
-0.165223074547365,-0.15245028863213,-0.147771515823046,-0.110734161208511,
-0.0736990584503352,-0.0368495292251676,0.),.UNSPECIFIED.);
#1662=CYLINDRICAL_SURFACE('',#14622,3.942);
#1663=CYLINDRICAL_SURFACE('',#14624,3.942);
#1664=CYLINDRICAL_SURFACE('',#14625,3.942);
#1665=CYLINDRICAL_SURFACE('',#14626,3.942);
#1666=CYLINDRICAL_SURFACE('',#14627,3.942);
#1667=CYLINDRICAL_SURFACE('',#14628,3.942);
#1668=CYLINDRICAL_SURFACE('',#14629,3.942);
#1669=CYLINDRICAL_SURFACE('',#14630,3.942);
#1670=CYLINDRICAL_SURFACE('',#14631,3.942);
#1671=CYLINDRICAL_SURFACE('',#14632,3.942);
#1672=CYLINDRICAL_SURFACE('',#14633,3.942);
#1673=CYLINDRICAL_SURFACE('',#14634,3.942);
#1674=CYLINDRICAL_SURFACE('',#14635,3.942);
#1675=CYLINDRICAL_SURFACE('',#14636,3.942);
#1676=CYLINDRICAL_SURFACE('',#14637,3.942);
#1677=CYLINDRICAL_SURFACE('',#14638,3.942);
#1678=CYLINDRICAL_SURFACE('',#14639,3.942);
#1679=CYLINDRICAL_SURFACE('',#14640,3.942);
#1680=CYLINDRICAL_SURFACE('',#14641,3.942);
#1681=CYLINDRICAL_SURFACE('',#14642,3.942);
#1682=CYLINDRICAL_SURFACE('',#14643,3.942);
#1683=CYLINDRICAL_SURFACE('',#14644,3.942);
#1684=CYLINDRICAL_SURFACE('',#14645,3.942);
#1685=CYLINDRICAL_SURFACE('',#14646,3.942);
#1686=CYLINDRICAL_SURFACE('',#14647,3.37175);
#1687=CYLINDRICAL_SURFACE('',#14649,3.37175);
#1688=CYLINDRICAL_SURFACE('',#14650,3.37175);
#1689=CYLINDRICAL_SURFACE('',#14651,3.37175);
#1690=CYLINDRICAL_SURFACE('',#14652,3.37175);
#1691=CYLINDRICAL_SURFACE('',#14653,3.37175);
#1692=CYLINDRICAL_SURFACE('',#14654,3.37175);
#1693=CYLINDRICAL_SURFACE('',#14655,3.37175);
#1694=CYLINDRICAL_SURFACE('',#14656,3.37175);
#1695=CYLINDRICAL_SURFACE('',#14657,3.37175);
#1696=CYLINDRICAL_SURFACE('',#14658,3.37175);
#1697=CYLINDRICAL_SURFACE('',#14659,3.37175);
#1698=CYLINDRICAL_SURFACE('',#14660,3.37175);
#1699=CYLINDRICAL_SURFACE('',#14661,3.37175);
#1700=CYLINDRICAL_SURFACE('',#14662,3.37175);
#1701=CYLINDRICAL_SURFACE('',#14663,3.37175);
#1702=CYLINDRICAL_SURFACE('',#14664,3.37175);
#1703=CYLINDRICAL_SURFACE('',#14665,3.37175);
#1704=CYLINDRICAL_SURFACE('',#14666,3.37175);
#1705=CYLINDRICAL_SURFACE('',#14667,3.37175);
#1706=CYLINDRICAL_SURFACE('',#14668,3.37175);
#1707=CYLINDRICAL_SURFACE('',#14669,3.37175);
#1708=CYLINDRICAL_SURFACE('',#14670,3.37175);
#1709=CYLINDRICAL_SURFACE('',#14671,3.37175);
#1710=CYLINDRICAL_SURFACE('',#14675,3.37175);
#1711=CYLINDRICAL_SURFACE('',#14677,3.942);
#1712=CYLINDRICAL_SURFACE('',#14687,6.5);
#2179=SHAPE_REPRESENTATION_RELATIONSHIP('SRR','None',#63863,#2195);
#2195=ADVANCED_BREP_SHAPE_REPRESENTATION('',(#2227),#63741);
#2211=STYLED_ITEM('',(#63960),#2227);
#2227=MANIFOLD_SOLID_BREP('Body1',#14312);
#2252=FACE_BOUND('',#3242,.T.);
#2253=FACE_BOUND('',#3245,.T.);
#2409=FACE_OUTER_BOUND('',#3181,.T.);
#2410=FACE_OUTER_BOUND('',#3182,.T.);
#2411=FACE_OUTER_BOUND('',#3183,.T.);
#2412=FACE_OUTER_BOUND('',#3184,.T.);
#2413=FACE_OUTER_BOUND('',#3185,.T.);
#2414=FACE_OUTER_BOUND('',#3186,.T.);
#2415=FACE_OUTER_BOUND('',#3187,.T.);
#2416=FACE_OUTER_BOUND('',#3188,.T.);
#2417=FACE_OUTER_BOUND('',#3189,.T.);
#2418=FACE_OUTER_BOUND('',#3190,.T.);
#2419=FACE_OUTER_BOUND('',#3191,.T.);
#2420=FACE_OUTER_BOUND('',#3192,.T.);
#2421=FACE_OUTER_BOUND('',#3193,.T.);
#2422=FACE_OUTER_BOUND('',#3194,.T.);
#2423=FACE_OUTER_BOUND('',#3195,.T.);
#2424=FACE_OUTER_BOUND('',#3196,.T.);
#2425=FACE_OUTER_BOUND('',#3197,.T.);
#2426=FACE_OUTER_BOUND('',#3198,.T.);
#2427=FACE_OUTER_BOUND('',#3199,.T.);
#2428=FACE_OUTER_BOUND('',#3200,.T.);
#2429=FACE_OUTER_BOUND('',#3201,.T.);
#2430=FACE_OUTER_BOUND('',#3202,.T.);
#2431=FACE_OUTER_BOUND('',#3203,.T.);
#2432=FACE_OUTER_BOUND('',#3204,.T.);
#2433=FACE_OUTER_BOUND('',#3205,.T.);
#2434=FACE_OUTER_BOUND('',#3206,.T.);
#2435=FACE_OUTER_BOUND('',#3207,.T.);
#2436=FACE_OUTER_BOUND('',#3208,.T.);
#2437=FACE_OUTER_BOUND('',#3209,.T.);
#2438=FACE_OUTER_BOUND('',#3210,.T.);
#2439=FACE_OUTER_BOUND('',#3211,.T.);
#2440=FACE_OUTER_BOUND('',#3212,.T.);
#2441=FACE_OUTER_BOUND('',#3213,.T.);
#2442=FACE_OUTER_BOUND('',#3214,.T.);
#2443=FACE_OUTER_BOUND('',#3215,.T.);
#2444=FACE_OUTER_BOUND('',#3216,.T.);
#2445=FACE_OUTER_BOUND('',#3217,.T.);
#2446=FACE_OUTER_BOUND('',#3218,.T.);
#2447=FACE_OUTER_BOUND('',#3219,.T.);
#2448=FACE_OUTER_BOUND('',#3220,.T.);
#2449=FACE_OUTER_BOUND('',#3221,.T.);
#2450=FACE_OUTER_BOUND('',#3222,.T.);
#2451=FACE_OUTER_BOUND('',#3223,.T.);
#2452=FACE_OUTER_BOUND('',#3224,.T.);
#2453=FACE_OUTER_BOUND('',#3225,.T.);
#2454=FACE_OUTER_BOUND('',#3226,.T.);
#2455=FACE_OUTER_BOUND('',#3227,.T.);
#2456=FACE_OUTER_BOUND('',#3228,.T.);
#2457=FACE_OUTER_BOUND('',#3229,.T.);
#2458=FACE_OUTER_BOUND('',#3230,.T.);
#2459=FACE_OUTER_BOUND('',#3231,.T.);
#2460=FACE_OUTER_BOUND('',#3232,.T.);
#2461=FACE_OUTER_BOUND('',#3233,.T.);
#2462=FACE_OUTER_BOUND('',#3234,.T.);
#2463=FACE_OUTER_BOUND('',#3235,.T.);
#2464=FACE_OUTER_BOUND('',#3236,.T.);
#2465=FACE_OUTER_BOUND('',#3237,.T.);
#2466=FACE_OUTER_BOUND('',#3238,.T.);
#2467=FACE_OUTER_BOUND('',#3239,.T.);
#2468=FACE_OUTER_BOUND('',#3240,.T.);
#2469=FACE_OUTER_BOUND('',#3241,.T.);
#2470=FACE_OUTER_BOUND('',#3243,.T.);
#2471=FACE_OUTER_BOUND('',#3244,.T.);
#2472=FACE_OUTER_BOUND('',#3246,.T.);
#3181=EDGE_LOOP('',(#9727,#9728,#9729,#9730));
#3182=EDGE_LOOP('',(#9731,#9732,#9733,#9734));
#3183=EDGE_LOOP('',(#9735,#9736,#9737,#9738));
#3184=EDGE_LOOP('',(#9739,#9740,#9741,#9742));
#3185=EDGE_LOOP('',(#9743,#9744,#9745,#9746));
#3186=EDGE_LOOP('',(#9747,#9748,#9749,#9750));
#3187=EDGE_LOOP('',(#9751,#9752,#9753,#9754));
#3188=EDGE_LOOP('',(#9755,#9756,#9757,#9758));
#3189=EDGE_LOOP('',(#9759,#9760,#9761,#9762));
#3190=EDGE_LOOP('',(#9763,#9764,#9765,#9766));
#3191=EDGE_LOOP('',(#9767,#9768,#9769,#9770));
#3192=EDGE_LOOP('',(#9771,#9772,#9773,#9774));
#3193=EDGE_LOOP('',(#9775,#9776,#9777,#9778));
#3194=EDGE_LOOP('',(#9779,#9780,#9781,#9782));
#3195=EDGE_LOOP('',(#9783,#9784,#9785,#9786));
#3196=EDGE_LOOP('',(#9787,#9788,#9789,#9790));
#3197=EDGE_LOOP('',(#9791,#9792,#9793,#9794));
#3198=EDGE_LOOP('',(#9795,#9796,#9797,#9798));
#3199=EDGE_LOOP('',(#9799,#9800,#9801,#9802));
#3200=EDGE_LOOP('',(#9803,#9804,#9805,#9806));
#3201=EDGE_LOOP('',(#9807,#9808,#9809,#9810));
#3202=EDGE_LOOP('',(#9811,#9812,#9813,#9814));
#3203=EDGE_LOOP('',(#9815,#9816,#9817,#9818));
#3204=EDGE_LOOP('',(#9819,#9820,#9821,#9822));
#3205=EDGE_LOOP('',(#9823,#9824,#9825,#9826));
#3206=EDGE_LOOP('',(#9827,#9828,#9829,#9830));
#3207=EDGE_LOOP('',(#9831,#9832,#9833,#9834));
#3208=EDGE_LOOP('',(#9835,#9836,#9837,#9838));
#3209=EDGE_LOOP('',(#9839,#9840,#9841,#9842));
#3210=EDGE_LOOP('',(#9843,#9844,#9845,#9846));
#3211=EDGE_LOOP('',(#9847,#9848,#9849,#9850));
#3212=EDGE_LOOP('',(#9851,#9852,#9853,#9854));
#3213=EDGE_LOOP('',(#9855,#9856,#9857,#9858));
#3214=EDGE_LOOP('',(#9859,#9860,#9861,#9862));
#3215=EDGE_LOOP('',(#9863,#9864,#9865,#9866));
#3216=EDGE_LOOP('',(#9867,#9868,#9869,#9870));
#3217=EDGE_LOOP('',(#9871,#9872,#9873,#9874));
#3218=EDGE_LOOP('',(#9875,#9876,#9877,#9878));
#3219=EDGE_LOOP('',(#9879,#9880,#9881,#9882));
#3220=EDGE_LOOP('',(#9883,#9884,#9885,#9886));
#3221=EDGE_LOOP('',(#9887,#9888,#9889,#9890));
#3222=EDGE_LOOP('',(#9891,#9892,#9893,#9894));
#3223=EDGE_LOOP('',(#9895,#9896,#9897,#9898));
#3224=EDGE_LOOP('',(#9899,#9900,#9901,#9902));
#3225=EDGE_LOOP('',(#9903,#9904,#9905,#9906));
#3226=EDGE_LOOP('',(#9907,#9908,#9909,#9910));
#3227=EDGE_LOOP('',(#9911,#9912,#9913,#9914));
#3228=EDGE_LOOP('',(#9915,#9916,#9917,#9918));
#3229=EDGE_LOOP('',(#9919,#9920,#9921,#9922,#9923,#9924,#9925,#9926));
#3230=EDGE_LOOP('',(#9927,#9928,#9929,#9930,#9931,#9932,#9933,#9934,#9935,
#9936,#9937,#9938,#9939,#9940,#9941,#9942,#9943,#9944,#9945,#9946,#9947,
#9948,#9949,#9950,#9951,#9952,#9953,#9954,#9955,#9956,#9957,#9958,#9959,
#9960,#9961,#9962,#9963,#9964,#9965,#9966,#9967,#9968,#9969,#9970,#9971,
#9972,#9973,#9974,#9975,#9976,#9977,#9978));
#3231=EDGE_LOOP('',(#9979,#9980,#9981,#9982));
#3232=EDGE_LOOP('',(#9983,#9984,#9985,#9986,#9987,#9988,#9989,#9990,#9991,
#9992,#9993,#9994,#9995,#9996,#9997,#9998,#9999,#10000,#10001,#10002,#10003,
#10004,#10005,#10006,#10007,#10008,#10009,#10010,#10011,#10012,#10013,#10014,
#10015,#10016,#10017,#10018,#10019,#10020,#10021,#10022,#10023,#10024,#10025,
#10026,#10027,#10028,#10029,#10030,#10031,#10032,#10033,#10034,#10035));
#3233=EDGE_LOOP('',(#10036,#10037,#10038,#10039));
#3234=EDGE_LOOP('',(#10040,#10041,#10042,#10043));
#3235=EDGE_LOOP('',(#10044,#10045,#10046,#10047));
#3236=EDGE_LOOP('',(#10048,#10049,#10050,#10051));
#3237=EDGE_LOOP('',(#10052,#10053,#10054,#10055));
#3238=EDGE_LOOP('',(#10056,#10057,#10058,#10059));
#3239=EDGE_LOOP('',(#10060,#10061,#10062,#10063));
#3240=EDGE_LOOP('',(#10064,#10065,#10066,#10067,#10068,#10069));
#3241=EDGE_LOOP('',(#10070));
#3242=EDGE_LOOP('',(#10071,#10072,#10073,#10074));
#3243=EDGE_LOOP('',(#10075,#10076,#10077,#10078));
#3244=EDGE_LOOP('',(#10079));
#3245=EDGE_LOOP('',(#10080,#10081,#10082,#10083,#10084,#10085));
#3246=EDGE_LOOP('',(#10086));
#4010=LINE('',#24320,#4846);
#4011=LINE('',#24344,#4847);
#4012=LINE('',#24392,#4848);
#4013=LINE('',#24440,#4849);
#4014=LINE('',#24488,#4850);
#4015=LINE('',#24542,#4851);
#4016=LINE('',#24590,#4852);
#4017=LINE('',#24638,#4853);
#4018=LINE('',#24692,#4854);
#4019=LINE('',#24740,#4855);
#4020=LINE('',#24788,#4856);
#4021=LINE('',#24842,#4857);
#4022=LINE('',#24890,#4858);
#4023=LINE('',#24938,#4859);
#4024=LINE('',#24986,#4860);
#4025=LINE('',#25040,#4861);
#4026=LINE('',#25088,#4862);
#4027=LINE('',#25136,#4863);
#4028=LINE('',#25190,#4864);
#4029=LINE('',#25238,#4865);
#4030=LINE('',#25286,#4866);
#4031=LINE('',#25334,#4867);
#4032=LINE('',#25388,#4868);
#4033=LINE('',#25436,#4869);
#4034=LINE('',#25484,#4870);
#4035=LINE('',#25509,#4871);
#4036=LINE('',#25534,#4872);
#4037=LINE('',#25558,#4873);
#4038=LINE('',#25583,#4874);
#4039=LINE('',#25608,#4875);
#4040=LINE('',#25632,#4876);
#4041=LINE('',#25656,#4877);
#4042=LINE('',#25681,#4878);
#4043=LINE('',#25706,#4879);
#4044=LINE('',#25730,#4880);
#4045=LINE('',#25755,#4881);
#4046=LINE('',#25780,#4882);
#4047=LINE('',#25804,#4883);
#4048=LINE('',#25828,#4884);
#4049=LINE('',#25853,#4885);
#4050=LINE('',#25878,#4886);
#4051=LINE('',#25902,#4887);
#4052=LINE('',#25927,#4888);
#4053=LINE('',#25952,#4889);
#4054=LINE('',#25976,#4890);
#4055=LINE('',#26001,#4891);
#4056=LINE('',#26026,#4892);
#4057=LINE('',#26050,#4893);
#4058=LINE('',#26407,#4894);
#4059=LINE('',#27941,#4895);
#4060=LINE('',#27943,#4896);
#4061=LINE('',#27945,#4897);
#4062=LINE('',#27946,#4898);
#4063=LINE('',#27949,#4899);
#4064=LINE('',#27951,#4900);
#4065=LINE('',#27952,#4901);
#4066=LINE('',#27955,#4902);
#4067=LINE('',#27957,#4903);
#4068=LINE('',#27958,#4904);
#4069=LINE('',#27961,#4905);
#4070=LINE('',#27963,#4906);
#4071=LINE('',#27964,#4907);
#4072=LINE('',#27967,#4908);
#4073=LINE('',#27969,#4909);
#4074=LINE('',#27970,#4910);
#4075=LINE('',#27972,#4911);
#4076=LINE('',#27973,#4912);
#4077=LINE('',#27980,#4913);
#4846=VECTOR('',#15881,4.);
#4847=VECTOR('',#15886,4.);
#4848=VECTOR('',#15889,4.);
#4849=VECTOR('',#15892,4.);
#4850=VECTOR('',#15895,4.);
#4851=VECTOR('',#15898,4.);
#4852=VECTOR('',#15901,4.);
#4853=VECTOR('',#15904,4.);
#4854=VECTOR('',#15907,4.);
#4855=VECTOR('',#15910,4.);
#4856=VECTOR('',#15913,4.);
#4857=VECTOR('',#15916,4.);
#4858=VECTOR('',#15919,4.);
#4859=VECTOR('',#15922,4.);
#4860=VECTOR('',#15925,4.);
#4861=VECTOR('',#15928,4.);
#4862=VECTOR('',#15931,4.);
#4863=VECTOR('',#15934,4.);
#4864=VECTOR('',#15937,4.);
#4865=VECTOR('',#15940,4.);
#4866=VECTOR('',#15943,4.);
#4867=VECTOR('',#15946,4.);
#4868=VECTOR('',#15949,4.);
#4869=VECTOR('',#15952,4.);
#4870=VECTOR('',#15955,3.37175);
#4871=VECTOR('',#15960,3.37175);
#4872=VECTOR('',#15963,3.37175);
#4873=VECTOR('',#15966,3.37175);
#4874=VECTOR('',#15969,3.37175);
#4875=VECTOR('',#15972,3.37175);
#4876=VECTOR('',#15975,3.37175);
#4877=VECTOR('',#15978,3.37175);
#4878=VECTOR('',#15981,3.37175);
#4879=VECTOR('',#15984,3.37175);
#4880=VECTOR('',#15987,3.37175);
#4881=VECTOR('',#15990,3.37175);
#4882=VECTOR('',#15993,3.37175);
#4883=VECTOR('',#15996,3.37175);
#4884=VECTOR('',#15999,3.37175);
#4885=VECTOR('',#16002,3.37175);
#4886=VECTOR('',#16005,3.37175);
#4887=VECTOR('',#16008,3.37175);
#4888=VECTOR('',#16011,3.37175);
#4889=VECTOR('',#16014,3.37175);
#4890=VECTOR('',#16017,3.37175);
#4891=VECTOR('',#16020,3.37175);
#4892=VECTOR('',#16023,3.37175);
#4893=VECTOR('',#16026,3.37175);
#4894=VECTOR('',#16031,3.5);
#4895=VECTOR('',#16042,10.);
#4896=VECTOR('',#16043,10.);
#4897=VECTOR('',#16044,10.);
#4898=VECTOR('',#16045,10.);
#4899=VECTOR('',#16048,10.);
#4900=VECTOR('',#16049,10.);
#4901=VECTOR('',#16050,10.);
#4902=VECTOR('',#16053,10.);
#4903=VECTOR('',#16054,10.);
#4904=VECTOR('',#16055,10.);
#4905=VECTOR('',#16058,10.);
#4906=VECTOR('',#16059,10.);
#4907=VECTOR('',#16060,10.);
#4908=VECTOR('',#16063,10.);
#4909=VECTOR('',#16064,10.);
#4910=VECTOR('',#16065,10.);
#4911=VECTOR('',#16068,10.);
#4912=VECTOR('',#16069,10.);
#4913=VECTOR('',#16078,6.5);
#5758=VERTEX_POINT('',#24318);
#5759=VERTEX_POINT('',#24319);
#5760=VERTEX_POINT('',#24321);
#5761=VERTEX_POINT('',#24332);
#5762=VERTEX_POINT('',#24342);
#5763=VERTEX_POINT('',#24343);
#5764=VERTEX_POINT('',#24390);
#5765=VERTEX_POINT('',#24391);
#5766=VERTEX_POINT('',#24438);
#5767=VERTEX_POINT('',#24439);
#5768=VERTEX_POINT('',#24486);
#5769=VERTEX_POINT('',#24487);
#5770=VERTEX_POINT('',#24540);
#5771=VERTEX_POINT('',#24541);
#5772=VERTEX_POINT('',#24588);
#5773=VERTEX_POINT('',#24589);
#5774=VERTEX_POINT('',#24636);
#5775=VERTEX_POINT('',#24637);
#5776=VERTEX_POINT('',#24690);
#5777=VERTEX_POINT('',#24691);
#5778=VERTEX_POINT('',#24738);
#5779=VERTEX_POINT('',#24739);
#5780=VERTEX_POINT('',#24786);
#5781=VERTEX_POINT('',#24787);
#5782=VERTEX_POINT('',#24840);
#5783=VERTEX_POINT('',#24841);
#5784=VERTEX_POINT('',#24888);
#5785=VERTEX_POINT('',#24889);
#5786=VERTEX_POINT('',#24936);
#5787=VERTEX_POINT('',#24937);
#5788=VERTEX_POINT('',#24984);
#5789=VERTEX_POINT('',#24985);
#5790=VERTEX_POINT('',#25038);
#5791=VERTEX_POINT('',#25039);
#5792=VERTEX_POINT('',#25086);
#5793=VERTEX_POINT('',#25087);
#5794=VERTEX_POINT('',#25134);
#5795=VERTEX_POINT('',#25135);
#5796=VERTEX_POINT('',#25188);
#5797=VERTEX_POINT('',#25189);
#5798=VERTEX_POINT('',#25236);
#5799=VERTEX_POINT('',#25237);
#5800=VERTEX_POINT('',#25284);
#5801=VERTEX_POINT('',#25285);
#5802=VERTEX_POINT('',#25332);
#5803=VERTEX_POINT('',#25333);
#5804=VERTEX_POINT('',#25386);
#5805=VERTEX_POINT('',#25387);
#5806=VERTEX_POINT('',#25434);
#5807=VERTEX_POINT('',#25435);
#5808=VERTEX_POINT('',#25482);
#5809=VERTEX_POINT('',#25483);
#5810=VERTEX_POINT('',#25485);
#5811=VERTEX_POINT('',#25496);
#5812=VERTEX_POINT('',#25507);
#5813=VERTEX_POINT('',#25508);
#5814=VERTEX_POINT('',#25532);
#5815=VERTEX_POINT('',#25533);
#5816=VERTEX_POINT('',#25556);
#5817=VERTEX_POINT('',#25557);
#5818=VERTEX_POINT('',#25581);
#5819=VERTEX_POINT('',#25582);
#5820=VERTEX_POINT('',#25606);
#5821=VERTEX_POINT('',#25607);
#5822=VERTEX_POINT('',#25630);
#5823=VERTEX_POINT('',#25631);
#5824=VERTEX_POINT('',#25654);
#5825=VERTEX_POINT('',#25655);
#5826=VERTEX_POINT('',#25679);
#5827=VERTEX_POINT('',#25680);
#5828=VERTEX_POINT('',#25704);
#5829=VERTEX_POINT('',#25705);
#5830=VERTEX_POINT('',#25728);
#5831=VERTEX_POINT('',#25729);
#5832=VERTEX_POINT('',#25753);
#5833=VERTEX_POINT('',#25754);
#5834=VERTEX_POINT('',#25778);
#5835=VERTEX_POINT('',#25779);
#5836=VERTEX_POINT('',#25802);
#5837=VERTEX_POINT('',#25803);
#5838=VERTEX_POINT('',#25826);
#5839=VERTEX_POINT('',#25827);
#5840=VERTEX_POINT('',#25851);
#5841=VERTEX_POINT('',#25852);
#5842=VERTEX_POINT('',#25876);
#5843=VERTEX_POINT('',#25877);
#5844=VERTEX_POINT('',#25900);
#5845=VERTEX_POINT('',#25901);
#5846=VERTEX_POINT('',#25925);
#5847=VERTEX_POINT('',#25926);
#5848=VERTEX_POINT('',#25950);
#5849=VERTEX_POINT('',#25951);
#5850=VERTEX_POINT('',#25974);
#5851=VERTEX_POINT('',#25975);
#5852=VERTEX_POINT('',#25999);
#5853=VERTEX_POINT('',#26000);
#5854=VERTEX_POINT('',#26024);
#5855=VERTEX_POINT('',#26025);
#5856=VERTEX_POINT('',#26048);
#5857=VERTEX_POINT('',#26049);
#5858=VERTEX_POINT('',#26072);
#5859=VERTEX_POINT('',#26305);
#5860=VERTEX_POINT('',#26373);
#5861=VERTEX_POINT('',#26406);
#5862=VERTEX_POINT('',#27041);
#5863=VERTEX_POINT('',#27167);
#5864=VERTEX_POINT('',#27939);
#5865=VERTEX_POINT('',#27940);
#5866=VERTEX_POINT('',#27942);
#5867=VERTEX_POINT('',#27944);
#5868=VERTEX_POINT('',#27948);
#5869=VERTEX_POINT('',#27950);
#5870=VERTEX_POINT('',#27954);
#5871=VERTEX_POINT('',#27956);
#5872=VERTEX_POINT('',#27960);
#5873=VERTEX_POINT('',#27962);
#5874=VERTEX_POINT('',#27966);
#5875=VERTEX_POINT('',#27968);
#5876=VERTEX_POINT('',#27976);
#5877=VERTEX_POINT('',#27979);
#7286=EDGE_CURVE('',#5758,#5759,#4010,.T.);
#7287=EDGE_CURVE('',#5758,#5760,#647,.T.);
#7288=EDGE_CURVE('',#5760,#5761,#301,.F.);
#7289=EDGE_CURVE('',#5761,#5759,#648,.T.);
#7290=EDGE_CURVE('',#5762,#5763,#4011,.T.);
#7291=EDGE_CURVE('',#5762,#5758,#649,.T.);
#7292=EDGE_CURVE('',#5759,#5763,#650,.T.);
#7293=EDGE_CURVE('',#5764,#5765,#4012,.T.);
#7294=EDGE_CURVE('',#5764,#5762,#651,.T.);
#7295=EDGE_CURVE('',#5763,#5765,#652,.T.);
#7296=EDGE_CURVE('',#5766,#5767,#4013,.T.);
#7297=EDGE_CURVE('',#5766,#5764,#653,.T.);
#7298=EDGE_CURVE('',#5765,#5767,#654,.T.);
#7299=EDGE_CURVE('',#5768,#5769,#4014,.T.);
#7300=EDGE_CURVE('',#5768,#5766,#655,.T.);
#7301=EDGE_CURVE('',#5767,#5769,#656,.T.);
#7302=EDGE_CURVE('',#5770,#5771,#4015,.T.);
#7303=EDGE_CURVE('',#5770,#5768,#657,.T.);
#7304=EDGE_CURVE('',#5769,#5771,#658,.T.);
#7305=EDGE_CURVE('',#5772,#5773,#4016,.T.);
#7306=EDGE_CURVE('',#5772,#5770,#659,.T.);
#7307=EDGE_CURVE('',#5771,#5773,#660,.T.);
#7308=EDGE_CURVE('',#5774,#5775,#4017,.T.);
#7309=EDGE_CURVE('',#5774,#5772,#661,.T.);
#7310=EDGE_CURVE('',#5773,#5775,#662,.T.);
#7311=EDGE_CURVE('',#5776,#5777,#4018,.T.);
#7312=EDGE_CURVE('',#5776,#5774,#663,.T.);
#7313=EDGE_CURVE('',#5775,#5777,#664,.T.);
#7314=EDGE_CURVE('',#5778,#5779,#4019,.T.);
#7315=EDGE_CURVE('',#5778,#5776,#665,.T.);
#7316=EDGE_CURVE('',#5777,#5779,#666,.T.);
#7317=EDGE_CURVE('',#5780,#5781,#4020,.T.);
#7318=EDGE_CURVE('',#5780,#5778,#667,.T.);
#7319=EDGE_CURVE('',#5779,#5781,#668,.T.);
#7320=EDGE_CURVE('',#5782,#5783,#4021,.T.);
#7321=EDGE_CURVE('',#5782,#5780,#669,.T.);
#7322=EDGE_CURVE('',#5781,#5783,#670,.T.);
#7323=EDGE_CURVE('',#5784,#5785,#4022,.T.);
#7324=EDGE_CURVE('',#5784,#5782,#671,.T.);
#7325=EDGE_CURVE('',#5783,#5785,#672,.T.);
#7326=EDGE_CURVE('',#5786,#5787,#4023,.T.);
#7327=EDGE_CURVE('',#5786,#5784,#673,.T.);
#7328=EDGE_CURVE('',#5785,#5787,#674,.T.);
#7329=EDGE_CURVE('',#5788,#5789,#4024,.T.);
#7330=EDGE_CURVE('',#5788,#5786,#675,.T.);
#7331=EDGE_CURVE('',#5787,#5789,#676,.T.);
#7332=EDGE_CURVE('',#5790,#5791,#4025,.T.);
#7333=EDGE_CURVE('',#5790,#5788,#677,.T.);
#7334=EDGE_CURVE('',#5789,#5791,#678,.T.);
#7335=EDGE_CURVE('',#5792,#5793,#4026,.T.);
#7336=EDGE_CURVE('',#5792,#5790,#679,.T.);
#7337=EDGE_CURVE('',#5791,#5793,#680,.T.);
#7338=EDGE_CURVE('',#5794,#5795,#4027,.T.);
#7339=EDGE_CURVE('',#5794,#5792,#681,.T.);
#7340=EDGE_CURVE('',#5793,#5795,#682,.T.);
#7341=EDGE_CURVE('',#5796,#5797,#4028,.T.);
#7342=EDGE_CURVE('',#5796,#5794,#683,.T.);
#7343=EDGE_CURVE('',#5795,#5797,#684,.T.);
#7344=EDGE_CURVE('',#5798,#5799,#4029,.T.);
#7345=EDGE_CURVE('',#5798,#5796,#685,.T.);
#7346=EDGE_CURVE('',#5797,#5799,#686,.T.);
#7347=EDGE_CURVE('',#5800,#5801,#4030,.T.);
#7348=EDGE_CURVE('',#5800,#5798,#687,.T.);
#7349=EDGE_CURVE('',#5799,#5801,#688,.T.);
#7350=EDGE_CURVE('',#5802,#5803,#4031,.T.);
#7351=EDGE_CURVE('',#5802,#5800,#689,.T.);
#7352=EDGE_CURVE('',#5801,#5803,#690,.T.);
#7353=EDGE_CURVE('',#5804,#5805,#4032,.T.);
#7354=EDGE_CURVE('',#5804,#5802,#691,.T.);
#7355=EDGE_CURVE('',#5803,#5805,#692,.T.);
#7356=EDGE_CURVE('',#5806,#5807,#4033,.T.);
#7357=EDGE_CURVE('',#5806,#5804,#693,.T.);
#7358=EDGE_CURVE('',#5805,#5807,#694,.T.);
#7359=EDGE_CURVE('',#5808,#5809,#4034,.T.);
#7360=EDGE_CURVE('',#5808,#5810,#695,.T.);
#7361=EDGE_CURVE('',#5810,#5811,#302,.T.);
#7362=EDGE_CURVE('',#5809,#5811,#696,.T.);
#7363=EDGE_CURVE('',#5812,#5813,#4035,.T.);
#7364=EDGE_CURVE('',#5812,#5808,#697,.T.);
#7365=EDGE_CURVE('',#5813,#5809,#698,.T.);
#7366=EDGE_CURVE('',#5814,#5815,#4036,.T.);
#7367=EDGE_CURVE('',#5814,#5812,#699,.T.);
#7368=EDGE_CURVE('',#5815,#5813,#700,.T.);
#7369=EDGE_CURVE('',#5816,#5817,#4037,.T.);
#7370=EDGE_CURVE('',#5816,#5814,#701,.T.);
#7371=EDGE_CURVE('',#5817,#5815,#702,.T.);
#7372=EDGE_CURVE('',#5818,#5819,#4038,.T.);
#7373=EDGE_CURVE('',#5818,#5816,#703,.T.);
#7374=EDGE_CURVE('',#5819,#5817,#704,.T.);
#7375=EDGE_CURVE('',#5820,#5821,#4039,.T.);
#7376=EDGE_CURVE('',#5820,#5818,#705,.T.);
#7377=EDGE_CURVE('',#5821,#5819,#706,.T.);
#7378=EDGE_CURVE('',#5822,#5823,#4040,.T.);
#7379=EDGE_CURVE('',#5822,#5820,#707,.T.);
#7380=EDGE_CURVE('',#5823,#5821,#708,.T.);
#7381=EDGE_CURVE('',#5824,#5825,#4041,.T.);
#7382=EDGE_CURVE('',#5824,#5822,#709,.T.);
#7383=EDGE_CURVE('',#5825,#5823,#710,.T.);
#7384=EDGE_CURVE('',#5826,#5827,#4042,.T.);
#7385=EDGE_CURVE('',#5826,#5824,#711,.T.);
#7386=EDGE_CURVE('',#5827,#5825,#712,.T.);
#7387=EDGE_CURVE('',#5828,#5829,#4043,.T.);
#7388=EDGE_CURVE('',#5828,#5826,#713,.T.);
#7389=EDGE_CURVE('',#5829,#5827,#714,.T.);
#7390=EDGE_CURVE('',#5830,#5831,#4044,.T.);
#7391=EDGE_CURVE('',#5830,#5828,#715,.T.);
#7392=EDGE_CURVE('',#5831,#5829,#716,.T.);
#7393=EDGE_CURVE('',#5832,#5833,#4045,.T.);
#7394=EDGE_CURVE('',#5832,#5830,#717,.T.);
#7395=EDGE_CURVE('',#5833,#5831,#718,.T.);
#7396=EDGE_CURVE('',#5834,#5835,#4046,.T.);
#7397=EDGE_CURVE('',#5834,#5832,#719,.T.);
#7398=EDGE_CURVE('',#5835,#5833,#720,.T.);
#7399=EDGE_CURVE('',#5836,#5837,#4047,.T.);
#7400=EDGE_CURVE('',#5836,#5834,#721,.T.);
#7401=EDGE_CURVE('',#5837,#5835,#722,.T.);
#7402=EDGE_CURVE('',#5838,#5839,#4048,.T.);
#7403=EDGE_CURVE('',#5838,#5836,#723,.T.);
#7404=EDGE_CURVE('',#5839,#5837,#724,.T.);
#7405=EDGE_CURVE('',#5840,#5841,#4049,.T.);
#7406=EDGE_CURVE('',#5840,#5838,#725,.T.);
#7407=EDGE_CURVE('',#5841,#5839,#726,.T.);
#7408=EDGE_CURVE('',#5842,#5843,#4050,.T.);
#7409=EDGE_CURVE('',#5842,#5840,#727,.T.);
#7410=EDGE_CURVE('',#5843,#5841,#728,.T.);
#7411=EDGE_CURVE('',#5844,#5845,#4051,.T.);
#7412=EDGE_CURVE('',#5844,#5842,#729,.T.);
#7413=EDGE_CURVE('',#5845,#5843,#730,.T.);
#7414=EDGE_CURVE('',#5846,#5847,#4052,.T.);
#7415=EDGE_CURVE('',#5846,#5844,#731,.T.);
#7416=EDGE_CURVE('',#5847,#5845,#732,.T.);
#7417=EDGE_CURVE('',#5848,#5849,#4053,.T.);
#7418=EDGE_CURVE('',#5848,#5846,#733,.T.);
#7419=EDGE_CURVE('',#5849,#5847,#734,.T.);
#7420=EDGE_CURVE('',#5850,#5851,#4054,.T.);
#7421=EDGE_CURVE('',#5850,#5848,#735,.T.);
#7422=EDGE_CURVE('',#5851,#5849,#736,.T.);
#7423=EDGE_CURVE('',#5852,#5853,#4055,.T.);
#7424=EDGE_CURVE('',#5852,#5850,#737,.T.);
#7425=EDGE_CURVE('',#5853,#5851,#738,.T.);
#7426=EDGE_CURVE('',#5854,#5855,#4056,.T.);
#7427=EDGE_CURVE('',#5854,#5852,#739,.T.);
#7428=EDGE_CURVE('',#5855,#5853,#740,.T.);
#7429=EDGE_CURVE('',#5856,#5857,#4057,.T.);
#7430=EDGE_CURVE('',#5856,#5854,#741,.T.);
#7431=EDGE_CURVE('',#5857,#5855,#742,.T.);
#7432=EDGE_CURVE('',#5811,#5858,#743,.T.);
#7433=EDGE_CURVE('',#5859,#5810,#744,.T.);
#7434=EDGE_CURVE('',#5860,#5859,#303,.T.);
#7435=EDGE_CURVE('',#5858,#5860,#745,.T.);
#7436=EDGE_CURVE('',#5858,#5861,#4058,.T.);
#7437=EDGE_CURVE('',#5861,#5861,#304,.T.);
#7438=EDGE_CURVE('',#5862,#5856,#746,.T.);
#7439=EDGE_CURVE('',#5760,#5862,#747,.T.);
#7440=EDGE_CURVE('',#5859,#5806,#748,.T.);
#7441=EDGE_CURVE('',#5863,#5857,#749,.T.);
#7442=EDGE_CURVE('',#5862,#5863,#305,.T.);
#7443=EDGE_CURVE('',#5807,#5860,#750,.T.);
#7444=EDGE_CURVE('',#5863,#5761,#751,.T.);
#7445=EDGE_CURVE('',#5864,#5865,#4059,.T.);
#7446=EDGE_CURVE('',#5864,#5866,#4060,.T.);
#7447=EDGE_CURVE('',#5866,#5867,#4061,.T.);
#7448=EDGE_CURVE('',#5865,#5867,#4062,.T.);
#7449=EDGE_CURVE('',#5868,#5864,#4063,.T.);
#7450=EDGE_CURVE('',#5868,#5869,#4064,.T.);
#7451=EDGE_CURVE('',#5869,#5866,#4065,.T.);
#7452=EDGE_CURVE('',#5870,#5868,#4066,.T.);
#7453=EDGE_CURVE('',#5870,#5871,#4067,.T.);
#7454=EDGE_CURVE('',#5871,#5869,#4068,.T.);
#7455=EDGE_CURVE('',#5872,#5870,#4069,.T.);
#7456=EDGE_CURVE('',#5872,#5873,#4070,.T.);
#7457=EDGE_CURVE('',#5873,#5871,#4071,.T.);
#7458=EDGE_CURVE('',#5874,#5872,#4072,.T.);
#7459=EDGE_CURVE('',#5874,#5875,#4073,.T.);
#7460=EDGE_CURVE('',#5875,#5873,#4074,.T.);
#7461=EDGE_CURVE('',#5865,#5874,#4075,.T.);
#7462=EDGE_CURVE('',#5867,#5875,#4076,.T.);
#7463=EDGE_CURVE('',#5876,#5876,#306,.T.);
#7464=EDGE_CURVE('',#5876,#5877,#4077,.T.);
#7465=EDGE_CURVE('',#5877,#5877,#307,.T.);
#9727=ORIENTED_EDGE('',*,*,#7286,.F.);
#9728=ORIENTED_EDGE('',*,*,#7287,.T.);
#9729=ORIENTED_EDGE('',*,*,#7288,.T.);
#9730=ORIENTED_EDGE('',*,*,#7289,.T.);
#9731=ORIENTED_EDGE('',*,*,#7290,.F.);
#9732=ORIENTED_EDGE('',*,*,#7291,.T.);
#9733=ORIENTED_EDGE('',*,*,#7286,.T.);
#9734=ORIENTED_EDGE('',*,*,#7292,.T.);
#9735=ORIENTED_EDGE('',*,*,#7293,.F.);
#9736=ORIENTED_EDGE('',*,*,#7294,.T.);
#9737=ORIENTED_EDGE('',*,*,#7290,.T.);
#9738=ORIENTED_EDGE('',*,*,#7295,.T.);
#9739=ORIENTED_EDGE('',*,*,#7296,.F.);
#9740=ORIENTED_EDGE('',*,*,#7297,.T.);
#9741=ORIENTED_EDGE('',*,*,#7293,.T.);
#9742=ORIENTED_EDGE('',*,*,#7298,.T.);
#9743=ORIENTED_EDGE('',*,*,#7299,.F.);
#9744=ORIENTED_EDGE('',*,*,#7300,.T.);
#9745=ORIENTED_EDGE('',*,*,#7296,.T.);
#9746=ORIENTED_EDGE('',*,*,#7301,.T.);
#9747=ORIENTED_EDGE('',*,*,#7302,.F.);
#9748=ORIENTED_EDGE('',*,*,#7303,.T.);
#9749=ORIENTED_EDGE('',*,*,#7299,.T.);
#9750=ORIENTED_EDGE('',*,*,#7304,.T.);
#9751=ORIENTED_EDGE('',*,*,#7305,.F.);
#9752=ORIENTED_EDGE('',*,*,#7306,.T.);
#9753=ORIENTED_EDGE('',*,*,#7302,.T.);
#9754=ORIENTED_EDGE('',*,*,#7307,.T.);
#9755=ORIENTED_EDGE('',*,*,#7308,.F.);
#9756=ORIENTED_EDGE('',*,*,#7309,.T.);
#9757=ORIENTED_EDGE('',*,*,#7305,.T.);
#9758=ORIENTED_EDGE('',*,*,#7310,.T.);
#9759=ORIENTED_EDGE('',*,*,#7311,.F.);
#9760=ORIENTED_EDGE('',*,*,#7312,.T.);
#9761=ORIENTED_EDGE('',*,*,#7308,.T.);
#9762=ORIENTED_EDGE('',*,*,#7313,.T.);
#9763=ORIENTED_EDGE('',*,*,#7314,.F.);
#9764=ORIENTED_EDGE('',*,*,#7315,.T.);
#9765=ORIENTED_EDGE('',*,*,#7311,.T.);
#9766=ORIENTED_EDGE('',*,*,#7316,.T.);
#9767=ORIENTED_EDGE('',*,*,#7317,.F.);
#9768=ORIENTED_EDGE('',*,*,#7318,.T.);
#9769=ORIENTED_EDGE('',*,*,#7314,.T.);
#9770=ORIENTED_EDGE('',*,*,#7319,.T.);
#9771=ORIENTED_EDGE('',*,*,#7320,.F.);
#9772=ORIENTED_EDGE('',*,*,#7321,.T.);
#9773=ORIENTED_EDGE('',*,*,#7317,.T.);
#9774=ORIENTED_EDGE('',*,*,#7322,.T.);
#9775=ORIENTED_EDGE('',*,*,#7323,.F.);
#9776=ORIENTED_EDGE('',*,*,#7324,.T.);
#9777=ORIENTED_EDGE('',*,*,#7320,.T.);
#9778=ORIENTED_EDGE('',*,*,#7325,.T.);
#9779=ORIENTED_EDGE('',*,*,#7326,.F.);
#9780=ORIENTED_EDGE('',*,*,#7327,.T.);
#9781=ORIENTED_EDGE('',*,*,#7323,.T.);
#9782=ORIENTED_EDGE('',*,*,#7328,.T.);
#9783=ORIENTED_EDGE('',*,*,#7329,.F.);
#9784=ORIENTED_EDGE('',*,*,#7330,.T.);
#9785=ORIENTED_EDGE('',*,*,#7326,.T.);
#9786=ORIENTED_EDGE('',*,*,#7331,.T.);
#9787=ORIENTED_EDGE('',*,*,#7332,.F.);
#9788=ORIENTED_EDGE('',*,*,#7333,.T.);
#9789=ORIENTED_EDGE('',*,*,#7329,.T.);
#9790=ORIENTED_EDGE('',*,*,#7334,.T.);
#9791=ORIENTED_EDGE('',*,*,#7335,.F.);
#9792=ORIENTED_EDGE('',*,*,#7336,.T.);
#9793=ORIENTED_EDGE('',*,*,#7332,.T.);
#9794=ORIENTED_EDGE('',*,*,#7337,.T.);
#9795=ORIENTED_EDGE('',*,*,#7338,.F.);
#9796=ORIENTED_EDGE('',*,*,#7339,.T.);
#9797=ORIENTED_EDGE('',*,*,#7335,.T.);
#9798=ORIENTED_EDGE('',*,*,#7340,.T.);
#9799=ORIENTED_EDGE('',*,*,#7341,.F.);
#9800=ORIENTED_EDGE('',*,*,#7342,.T.);
#9801=ORIENTED_EDGE('',*,*,#7338,.T.);
#9802=ORIENTED_EDGE('',*,*,#7343,.T.);
#9803=ORIENTED_EDGE('',*,*,#7344,.F.);
#9804=ORIENTED_EDGE('',*,*,#7345,.T.);
#9805=ORIENTED_EDGE('',*,*,#7341,.T.);
#9806=ORIENTED_EDGE('',*,*,#7346,.T.);
#9807=ORIENTED_EDGE('',*,*,#7347,.F.);
#9808=ORIENTED_EDGE('',*,*,#7348,.T.);
#9809=ORIENTED_EDGE('',*,*,#7344,.T.);
#9810=ORIENTED_EDGE('',*,*,#7349,.T.);
#9811=ORIENTED_EDGE('',*,*,#7350,.F.);
#9812=ORIENTED_EDGE('',*,*,#7351,.T.);
#9813=ORIENTED_EDGE('',*,*,#7347,.T.);
#9814=ORIENTED_EDGE('',*,*,#7352,.T.);
#9815=ORIENTED_EDGE('',*,*,#7353,.F.);
#9816=ORIENTED_EDGE('',*,*,#7354,.T.);
#9817=ORIENTED_EDGE('',*,*,#7350,.T.);
#9818=ORIENTED_EDGE('',*,*,#7355,.T.);
#9819=ORIENTED_EDGE('',*,*,#7356,.F.);
#9820=ORIENTED_EDGE('',*,*,#7357,.T.);
#9821=ORIENTED_EDGE('',*,*,#7353,.T.);
#9822=ORIENTED_EDGE('',*,*,#7358,.T.);
#9823=ORIENTED_EDGE('',*,*,#7359,.F.);
#9824=ORIENTED_EDGE('',*,*,#7360,.T.);
#9825=ORIENTED_EDGE('',*,*,#7361,.T.);
#9826=ORIENTED_EDGE('',*,*,#7362,.F.);
#9827=ORIENTED_EDGE('',*,*,#7363,.F.);
#9828=ORIENTED_EDGE('',*,*,#7364,.T.);
#9829=ORIENTED_EDGE('',*,*,#7359,.T.);
#9830=ORIENTED_EDGE('',*,*,#7365,.F.);
#9831=ORIENTED_EDGE('',*,*,#7366,.F.);
#9832=ORIENTED_EDGE('',*,*,#7367,.T.);
#9833=ORIENTED_EDGE('',*,*,#7363,.T.);
#9834=ORIENTED_EDGE('',*,*,#7368,.F.);
#9835=ORIENTED_EDGE('',*,*,#7369,.F.);
#9836=ORIENTED_EDGE('',*,*,#7370,.T.);
#9837=ORIENTED_EDGE('',*,*,#7366,.T.);
#9838=ORIENTED_EDGE('',*,*,#7371,.F.);
#9839=ORIENTED_EDGE('',*,*,#7372,.F.);
#9840=ORIENTED_EDGE('',*,*,#7373,.T.);
#9841=ORIENTED_EDGE('',*,*,#7369,.T.);
#9842=ORIENTED_EDGE('',*,*,#7374,.F.);
#9843=ORIENTED_EDGE('',*,*,#7375,.F.);
#9844=ORIENTED_EDGE('',*,*,#7376,.T.);
#9845=ORIENTED_EDGE('',*,*,#7372,.T.);
#9846=ORIENTED_EDGE('',*,*,#7377,.F.);
#9847=ORIENTED_EDGE('',*,*,#7378,.F.);
#9848=ORIENTED_EDGE('',*,*,#7379,.T.);
#9849=ORIENTED_EDGE('',*,*,#7375,.T.);
#9850=ORIENTED_EDGE('',*,*,#7380,.F.);
#9851=ORIENTED_EDGE('',*,*,#7381,.F.);
#9852=ORIENTED_EDGE('',*,*,#7382,.T.);
#9853=ORIENTED_EDGE('',*,*,#7378,.T.);
#9854=ORIENTED_EDGE('',*,*,#7383,.F.);
#9855=ORIENTED_EDGE('',*,*,#7384,.F.);
#9856=ORIENTED_EDGE('',*,*,#7385,.T.);
#9857=ORIENTED_EDGE('',*,*,#7381,.T.);
#9858=ORIENTED_EDGE('',*,*,#7386,.F.);
#9859=ORIENTED_EDGE('',*,*,#7387,.F.);
#9860=ORIENTED_EDGE('',*,*,#7388,.T.);
#9861=ORIENTED_EDGE('',*,*,#7384,.T.);
#9862=ORIENTED_EDGE('',*,*,#7389,.F.);
#9863=ORIENTED_EDGE('',*,*,#7390,.F.);
#9864=ORIENTED_EDGE('',*,*,#7391,.T.);
#9865=ORIENTED_EDGE('',*,*,#7387,.T.);
#9866=ORIENTED_EDGE('',*,*,#7392,.F.);
#9867=ORIENTED_EDGE('',*,*,#7393,.F.);
#9868=ORIENTED_EDGE('',*,*,#7394,.T.);
#9869=ORIENTED_EDGE('',*,*,#7390,.T.);
#9870=ORIENTED_EDGE('',*,*,#7395,.F.);
#9871=ORIENTED_EDGE('',*,*,#7396,.F.);
#9872=ORIENTED_EDGE('',*,*,#7397,.T.);
#9873=ORIENTED_EDGE('',*,*,#7393,.T.);
#9874=ORIENTED_EDGE('',*,*,#7398,.F.);
#9875=ORIENTED_EDGE('',*,*,#7399,.F.);
#9876=ORIENTED_EDGE('',*,*,#7400,.T.);
#9877=ORIENTED_EDGE('',*,*,#7396,.T.);
#9878=ORIENTED_EDGE('',*,*,#7401,.F.);
#9879=ORIENTED_EDGE('',*,*,#7402,.F.);
#9880=ORIENTED_EDGE('',*,*,#7403,.T.);
#9881=ORIENTED_EDGE('',*,*,#7399,.T.);
#9882=ORIENTED_EDGE('',*,*,#7404,.F.);
#9883=ORIENTED_EDGE('',*,*,#7405,.F.);
#9884=ORIENTED_EDGE('',*,*,#7406,.T.);
#9885=ORIENTED_EDGE('',*,*,#7402,.T.);
#9886=ORIENTED_EDGE('',*,*,#7407,.F.);
#9887=ORIENTED_EDGE('',*,*,#7408,.F.);
#9888=ORIENTED_EDGE('',*,*,#7409,.T.);
#9889=ORIENTED_EDGE('',*,*,#7405,.T.);
#9890=ORIENTED_EDGE('',*,*,#7410,.F.);
#9891=ORIENTED_EDGE('',*,*,#7411,.F.);
#9892=ORIENTED_EDGE('',*,*,#7412,.T.);
#9893=ORIENTED_EDGE('',*,*,#7408,.T.);
#9894=ORIENTED_EDGE('',*,*,#7413,.F.);
#9895=ORIENTED_EDGE('',*,*,#7414,.F.);
#9896=ORIENTED_EDGE('',*,*,#7415,.T.);
#9897=ORIENTED_EDGE('',*,*,#7411,.T.);
#9898=ORIENTED_EDGE('',*,*,#7416,.F.);
#9899=ORIENTED_EDGE('',*,*,#7417,.F.);
#9900=ORIENTED_EDGE('',*,*,#7418,.T.);
#9901=ORIENTED_EDGE('',*,*,#7414,.T.);
#9902=ORIENTED_EDGE('',*,*,#7419,.F.);
#9903=ORIENTED_EDGE('',*,*,#7420,.F.);
#9904=ORIENTED_EDGE('',*,*,#7421,.T.);
#9905=ORIENTED_EDGE('',*,*,#7417,.T.);
#9906=ORIENTED_EDGE('',*,*,#7422,.F.);
#9907=ORIENTED_EDGE('',*,*,#7423,.F.);
#9908=ORIENTED_EDGE('',*,*,#7424,.T.);
#9909=ORIENTED_EDGE('',*,*,#7420,.T.);
#9910=ORIENTED_EDGE('',*,*,#7425,.F.);
#9911=ORIENTED_EDGE('',*,*,#7426,.F.);
#9912=ORIENTED_EDGE('',*,*,#7427,.T.);
#9913=ORIENTED_EDGE('',*,*,#7423,.T.);
#9914=ORIENTED_EDGE('',*,*,#7428,.F.);
#9915=ORIENTED_EDGE('',*,*,#7429,.F.);
#9916=ORIENTED_EDGE('',*,*,#7430,.T.);
#9917=ORIENTED_EDGE('',*,*,#7426,.T.);
#9918=ORIENTED_EDGE('',*,*,#7431,.F.);
#9919=ORIENTED_EDGE('',*,*,#7432,.F.);
#9920=ORIENTED_EDGE('',*,*,#7361,.F.);
#9921=ORIENTED_EDGE('',*,*,#7433,.F.);
#9922=ORIENTED_EDGE('',*,*,#7434,.F.);
#9923=ORIENTED_EDGE('',*,*,#7435,.F.);
#9924=ORIENTED_EDGE('',*,*,#7436,.T.);
#9925=ORIENTED_EDGE('',*,*,#7437,.F.);
#9926=ORIENTED_EDGE('',*,*,#7436,.F.);
#9927=ORIENTED_EDGE('',*,*,#7433,.T.);
#9928=ORIENTED_EDGE('',*,*,#7360,.F.);
#9929=ORIENTED_EDGE('',*,*,#7364,.F.);
#9930=ORIENTED_EDGE('',*,*,#7367,.F.);
#9931=ORIENTED_EDGE('',*,*,#7370,.F.);
#9932=ORIENTED_EDGE('',*,*,#7373,.F.);
#9933=ORIENTED_EDGE('',*,*,#7376,.F.);
#9934=ORIENTED_EDGE('',*,*,#7379,.F.);
#9935=ORIENTED_EDGE('',*,*,#7382,.F.);
#9936=ORIENTED_EDGE('',*,*,#7385,.F.);
#9937=ORIENTED_EDGE('',*,*,#7388,.F.);
#9938=ORIENTED_EDGE('',*,*,#7391,.F.);
#9939=ORIENTED_EDGE('',*,*,#7394,.F.);
#9940=ORIENTED_EDGE('',*,*,#7397,.F.);
#9941=ORIENTED_EDGE('',*,*,#7400,.F.);
#9942=ORIENTED_EDGE('',*,*,#7403,.F.);
#9943=ORIENTED_EDGE('',*,*,#7406,.F.);
#9944=ORIENTED_EDGE('',*,*,#7409,.F.);
#9945=ORIENTED_EDGE('',*,*,#7412,.F.);
#9946=ORIENTED_EDGE('',*,*,#7415,.F.);
#9947=ORIENTED_EDGE('',*,*,#7418,.F.);
#9948=ORIENTED_EDGE('',*,*,#7421,.F.);
#9949=ORIENTED_EDGE('',*,*,#7424,.F.);
#9950=ORIENTED_EDGE('',*,*,#7427,.F.);
#9951=ORIENTED_EDGE('',*,*,#7430,.F.);
#9952=ORIENTED_EDGE('',*,*,#7438,.F.);
#9953=ORIENTED_EDGE('',*,*,#7439,.F.);
#9954=ORIENTED_EDGE('',*,*,#7287,.F.);
#9955=ORIENTED_EDGE('',*,*,#7291,.F.);
#9956=ORIENTED_EDGE('',*,*,#7294,.F.);
#9957=ORIENTED_EDGE('',*,*,#7297,.F.);
#9958=ORIENTED_EDGE('',*,*,#7300,.F.);
#9959=ORIENTED_EDGE('',*,*,#7303,.F.);
#9960=ORIENTED_EDGE('',*,*,#7306,.F.);
#9961=ORIENTED_EDGE('',*,*,#7309,.F.);
#9962=ORIENTED_EDGE('',*,*,#7312,.F.);
#9963=ORIENTED_EDGE('',*,*,#7315,.F.);
#9964=ORIENTED_EDGE('',*,*,#7318,.F.);
#9965=ORIENTED_EDGE('',*,*,#7321,.F.);
#9966=ORIENTED_EDGE('',*,*,#7324,.F.);
#9967=ORIENTED_EDGE('',*,*,#7327,.F.);
#9968=ORIENTED_EDGE('',*,*,#7330,.F.);
#9969=ORIENTED_EDGE('',*,*,#7333,.F.);
#9970=ORIENTED_EDGE('',*,*,#7336,.F.);
#9971=ORIENTED_EDGE('',*,*,#7339,.F.);
#9972=ORIENTED_EDGE('',*,*,#7342,.F.);
#9973=ORIENTED_EDGE('',*,*,#7345,.F.);
#9974=ORIENTED_EDGE('',*,*,#7348,.F.);
#9975=ORIENTED_EDGE('',*,*,#7351,.F.);
#9976=ORIENTED_EDGE('',*,*,#7354,.F.);
#9977=ORIENTED_EDGE('',*,*,#7357,.F.);
#9978=ORIENTED_EDGE('',*,*,#7440,.F.);
#9979=ORIENTED_EDGE('',*,*,#7429,.T.);
#9980=ORIENTED_EDGE('',*,*,#7441,.F.);
#9981=ORIENTED_EDGE('',*,*,#7442,.F.);
#9982=ORIENTED_EDGE('',*,*,#7438,.T.);
#9983=ORIENTED_EDGE('',*,*,#7432,.T.);
#9984=ORIENTED_EDGE('',*,*,#7435,.T.);
#9985=ORIENTED_EDGE('',*,*,#7443,.F.);
#9986=ORIENTED_EDGE('',*,*,#7358,.F.);
#9987=ORIENTED_EDGE('',*,*,#7355,.F.);
#9988=ORIENTED_EDGE('',*,*,#7352,.F.);
#9989=ORIENTED_EDGE('',*,*,#7349,.F.);
#9990=ORIENTED_EDGE('',*,*,#7346,.F.);
#9991=ORIENTED_EDGE('',*,*,#7343,.F.);
#9992=ORIENTED_EDGE('',*,*,#7340,.F.);
#9993=ORIENTED_EDGE('',*,*,#7337,.F.);
#9994=ORIENTED_EDGE('',*,*,#7334,.F.);
#9995=ORIENTED_EDGE('',*,*,#7331,.F.);
#9996=ORIENTED_EDGE('',*,*,#7328,.F.);
#9997=ORIENTED_EDGE('',*,*,#7325,.F.);
#9998=ORIENTED_EDGE('',*,*,#7322,.F.);
#9999=ORIENTED_EDGE('',*,*,#7319,.F.);
#10000=ORIENTED_EDGE('',*,*,#7316,.F.);
#10001=ORIENTED_EDGE('',*,*,#7313,.F.);
#10002=ORIENTED_EDGE('',*,*,#7310,.F.);
#10003=ORIENTED_EDGE('',*,*,#7307,.F.);
#10004=ORIENTED_EDGE('',*,*,#7304,.F.);
#10005=ORIENTED_EDGE('',*,*,#7301,.F.);
#10006=ORIENTED_EDGE('',*,*,#7298,.F.);
#10007=ORIENTED_EDGE('',*,*,#7295,.F.);
#10008=ORIENTED_EDGE('',*,*,#7292,.F.);
#10009=ORIENTED_EDGE('',*,*,#7289,.F.);
#10010=ORIENTED_EDGE('',*,*,#7444,.F.);
#10011=ORIENTED_EDGE('',*,*,#7441,.T.);
#10012=ORIENTED_EDGE('',*,*,#7431,.T.);
#10013=ORIENTED_EDGE('',*,*,#7428,.T.);
#10014=ORIENTED_EDGE('',*,*,#7425,.T.);
#10015=ORIENTED_EDGE('',*,*,#7422,.T.);
#10016=ORIENTED_EDGE('',*,*,#7419,.T.);
#10017=ORIENTED_EDGE('',*,*,#7416,.T.);
#10018=ORIENTED_EDGE('',*,*,#7413,.T.);
#10019=ORIENTED_EDGE('',*,*,#7410,.T.);
#10020=ORIENTED_EDGE('',*,*,#7407,.T.);
#10021=ORIENTED_EDGE('',*,*,#7404,.T.);
#10022=ORIENTED_EDGE('',*,*,#7401,.T.);
#10023=ORIENTED_EDGE('',*,*,#7398,.T.);
#10024=ORIENTED_EDGE('',*,*,#7395,.T.);
#10025=ORIENTED_EDGE('',*,*,#7392,.T.);
#10026=ORIENTED_EDGE('',*,*,#7389,.T.);
#10027=ORIENTED_EDGE('',*,*,#7386,.T.);
#10028=ORIENTED_EDGE('',*,*,#7383,.T.);
#10029=ORIENTED_EDGE('',*,*,#7380,.T.);
#10030=ORIENTED_EDGE('',*,*,#7377,.T.);
#10031=ORIENTED_EDGE('',*,*,#7374,.T.);
#10032=ORIENTED_EDGE('',*,*,#7371,.T.);
#10033=ORIENTED_EDGE('',*,*,#7368,.T.);
#10034=ORIENTED_EDGE('',*,*,#7365,.T.);
#10035=ORIENTED_EDGE('',*,*,#7362,.T.);
#10036=ORIENTED_EDGE('',*,*,#7356,.T.);
#10037=ORIENTED_EDGE('',*,*,#7443,.T.);
#10038=ORIENTED_EDGE('',*,*,#7434,.T.);
#10039=ORIENTED_EDGE('',*,*,#7440,.T.);
#10040=ORIENTED_EDGE('',*,*,#7445,.F.);
#10041=ORIENTED_EDGE('',*,*,#7446,.T.);
#10042=ORIENTED_EDGE('',*,*,#7447,.T.);
#10043=ORIENTED_EDGE('',*,*,#7448,.F.);
#10044=ORIENTED_EDGE('',*,*,#7449,.F.);
#10045=ORIENTED_EDGE('',*,*,#7450,.T.);
#10046=ORIENTED_EDGE('',*,*,#7451,.T.);
#10047=ORIENTED_EDGE('',*,*,#7446,.F.);
#10048=ORIENTED_EDGE('',*,*,#7452,.F.);
#10049=ORIENTED_EDGE('',*,*,#7453,.T.);
#10050=ORIENTED_EDGE('',*,*,#7454,.T.);
#10051=ORIENTED_EDGE('',*,*,#7450,.F.);
#10052=ORIENTED_EDGE('',*,*,#7455,.F.);
#10053=ORIENTED_EDGE('',*,*,#7456,.T.);
#10054=ORIENTED_EDGE('',*,*,#7457,.T.);
#10055=ORIENTED_EDGE('',*,*,#7453,.F.);
#10056=ORIENTED_EDGE('',*,*,#7458,.F.);
#10057=ORIENTED_EDGE('',*,*,#7459,.T.);
#10058=ORIENTED_EDGE('',*,*,#7460,.T.);
#10059=ORIENTED_EDGE('',*,*,#7456,.F.);
#10060=ORIENTED_EDGE('',*,*,#7461,.F.);
#10061=ORIENTED_EDGE('',*,*,#7448,.T.);
#10062=ORIENTED_EDGE('',*,*,#7462,.T.);
#10063=ORIENTED_EDGE('',*,*,#7459,.F.);
#10064=ORIENTED_EDGE('',*,*,#7462,.F.);
#10065=ORIENTED_EDGE('',*,*,#7447,.F.);
#10066=ORIENTED_EDGE('',*,*,#7451,.F.);
#10067=ORIENTED_EDGE('',*,*,#7454,.F.);
#10068=ORIENTED_EDGE('',*,*,#7457,.F.);
#10069=ORIENTED_EDGE('',*,*,#7460,.F.);
#10070=ORIENTED_EDGE('',*,*,#7463,.T.);
#10071=ORIENTED_EDGE('',*,*,#7439,.T.);
#10072=ORIENTED_EDGE('',*,*,#7442,.T.);
#10073=ORIENTED_EDGE('',*,*,#7444,.T.);
#10074=ORIENTED_EDGE('',*,*,#7288,.F.);
#10075=ORIENTED_EDGE('',*,*,#7463,.F.);
#10076=ORIENTED_EDGE('',*,*,#7464,.T.);
#10077=ORIENTED_EDGE('',*,*,#7465,.T.);
#10078=ORIENTED_EDGE('',*,*,#7464,.F.);
#10079=ORIENTED_EDGE('',*,*,#7465,.F.);
#10080=ORIENTED_EDGE('',*,*,#7445,.T.);
#10081=ORIENTED_EDGE('',*,*,#7461,.T.);
#10082=ORIENTED_EDGE('',*,*,#7458,.T.);
#10083=ORIENTED_EDGE('',*,*,#7455,.T.);
#10084=ORIENTED_EDGE('',*,*,#7452,.T.);
#10085=ORIENTED_EDGE('',*,*,#7449,.T.);
#10086=ORIENTED_EDGE('',*,*,#7437,.T.);
#13435=PLANE('',#14678);
#13436=PLANE('',#14679);
#13437=PLANE('',#14680);
#13438=PLANE('',#14681);
#13439=PLANE('',#14682);
#13440=PLANE('',#14683);
#13441=PLANE('',#14684);
#13442=PLANE('',#14685);
#13443=PLANE('',#14689);
#13444=PLANE('',#14690);
#13655=ADVANCED_FACE('',(#2409),#1662,.T.);
#13656=ADVANCED_FACE('',(#2410),#1663,.T.);
#13657=ADVANCED_FACE('',(#2411),#1664,.T.);
#13658=ADVANCED_FACE('',(#2412),#1665,.T.);
#13659=ADVANCED_FACE('',(#2413),#1666,.T.);
#13660=ADVANCED_FACE('',(#2414),#1667,.T.);
#13661=ADVANCED_FACE('',(#2415),#1668,.T.);
#13662=ADVANCED_FACE('',(#2416),#1669,.T.);
#13663=ADVANCED_FACE('',(#2417),#1670,.T.);
#13664=ADVANCED_FACE('',(#2418),#1671,.T.);
#13665=ADVANCED_FACE('',(#2419),#1672,.T.);
#13666=ADVANCED_FACE('',(#2420),#1673,.T.);
#13667=ADVANCED_FACE('',(#2421),#1674,.T.);
#13668=ADVANCED_FACE('',(#2422),#1675,.T.);
#13669=ADVANCED_FACE('',(#2423),#1676,.T.);
#13670=ADVANCED_FACE('',(#2424),#1677,.T.);
#13671=ADVANCED_FACE('',(#2425),#1678,.T.);
#13672=ADVANCED_FACE('',(#2426),#1679,.T.);
#13673=ADVANCED_FACE('',(#2427),#1680,.T.);
#13674=ADVANCED_FACE('',(#2428),#1681,.T.);
#13675=ADVANCED_FACE('',(#2429),#1682,.T.);
#13676=ADVANCED_FACE('',(#2430),#1683,.T.);
#13677=ADVANCED_FACE('',(#2431),#1684,.T.);
#13678=ADVANCED_FACE('',(#2432),#1685,.T.);
#13679=ADVANCED_FACE('',(#2433),#1686,.T.);
#13680=ADVANCED_FACE('',(#2434),#1687,.T.);
#13681=ADVANCED_FACE('',(#2435),#1688,.T.);
#13682=ADVANCED_FACE('',(#2436),#1689,.T.);
#13683=ADVANCED_FACE('',(#2437),#1690,.T.);
#13684=ADVANCED_FACE('',(#2438),#1691,.T.);
#13685=ADVANCED_FACE('',(#2439),#1692,.T.);
#13686=ADVANCED_FACE('',(#2440),#1693,.T.);
#13687=ADVANCED_FACE('',(#2441),#1694,.T.);
#13688=ADVANCED_FACE('',(#2442),#1695,.T.);
#13689=ADVANCED_FACE('',(#2443),#1696,.T.);
#13690=ADVANCED_FACE('',(#2444),#1697,.T.);
#13691=ADVANCED_FACE('',(#2445),#1698,.T.);
#13692=ADVANCED_FACE('',(#2446),#1699,.T.);
#13693=ADVANCED_FACE('',(#2447),#1700,.T.);
#13694=ADVANCED_FACE('',(#2448),#1701,.T.);
#13695=ADVANCED_FACE('',(#2449),#1702,.T.);
#13696=ADVANCED_FACE('',(#2450),#1703,.T.);
#13697=ADVANCED_FACE('',(#2451),#1704,.T.);
#13698=ADVANCED_FACE('',(#2452),#1705,.T.);
#13699=ADVANCED_FACE('',(#2453),#1706,.T.);
#13700=ADVANCED_FACE('',(#2454),#1707,.T.);
#13701=ADVANCED_FACE('',(#2455),#1708,.T.);
#13702=ADVANCED_FACE('',(#2456),#1709,.T.);
#13703=ADVANCED_FACE('',(#2457),#254,.T.);
#13704=ADVANCED_FACE('',(#2458),#265,.F.);
#13705=ADVANCED_FACE('',(#2459),#1710,.T.);
#13706=ADVANCED_FACE('',(#2460),#266,.F.);
#13707=ADVANCED_FACE('',(#2461),#1711,.T.);
#13708=ADVANCED_FACE('',(#2462),#13435,.F.);
#13709=ADVANCED_FACE('',(#2463),#13436,.F.);
#13710=ADVANCED_FACE('',(#2464),#13437,.F.);
#13711=ADVANCED_FACE('',(#2465),#13438,.F.);
#13712=ADVANCED_FACE('',(#2466),#13439,.F.);
#13713=ADVANCED_FACE('',(#2467),#13440,.F.);
#13714=ADVANCED_FACE('',(#2468),#13441,.F.);
#13715=ADVANCED_FACE('',(#2469,#2252),#13442,.T.);
#13716=ADVANCED_FACE('',(#2470),#1712,.T.);
#13717=ADVANCED_FACE('',(#2471,#2253),#13443,.F.);
#13718=ADVANCED_FACE('',(#2472),#13444,.T.);
#14312=CLOSED_SHELL('',(#13655,#13656,#13657,#13658,#13659,#13660,#13661,
#13662,#13663,#13664,#13665,#13666,#13667,#13668,#13669,#13670,#13671,#13672,
#13673,#13674,#13675,#13676,#13677,#13678,#13679,#13680,#13681,#13682,#13683,
#13684,#13685,#13686,#13687,#13688,#13689,#13690,#13691,#13692,#13693,#13694,
#13695,#13696,#13697,#13698,#13699,#13700,#13701,#13702,#13703,#13704,#13705,
#13706,#13707,#13708,#13709,#13710,#13711,#13712,#13713,#13714,#13715,#13716,
#13717,#13718));
#14621=AXIS2_PLACEMENT_3D('',#24316,#15877,#15878);
#14622=AXIS2_PLACEMENT_3D('',#24317,#15879,#15880);
#14623=AXIS2_PLACEMENT_3D('',#24333,#15882,#15883);
#14624=AXIS2_PLACEMENT_3D('',#24341,#15884,#15885);
#14625=AXIS2_PLACEMENT_3D('',#24389,#15887,#15888);
#14626=AXIS2_PLACEMENT_3D('',#24437,#15890,#15891);
#14627=AXIS2_PLACEMENT_3D('',#24485,#15893,#15894);
#14628=AXIS2_PLACEMENT_3D('',#24539,#15896,#15897);
#14629=AXIS2_PLACEMENT_3D('',#24587,#15899,#15900);
#14630=AXIS2_PLACEMENT_3D('',#24635,#15902,#15903);
#14631=AXIS2_PLACEMENT_3D('',#24689,#15905,#15906);
#14632=AXIS2_PLACEMENT_3D('',#24737,#15908,#15909);
#14633=AXIS2_PLACEMENT_3D('',#24785,#15911,#15912);
#14634=AXIS2_PLACEMENT_3D('',#24839,#15914,#15915);
#14635=AXIS2_PLACEMENT_3D('',#24887,#15917,#15918);
#14636=AXIS2_PLACEMENT_3D('',#24935,#15920,#15921);
#14637=AXIS2_PLACEMENT_3D('',#24983,#15923,#15924);
#14638=AXIS2_PLACEMENT_3D('',#25037,#15926,#15927);
#14639=AXIS2_PLACEMENT_3D('',#25085,#15929,#15930);
#14640=AXIS2_PLACEMENT_3D('',#25133,#15932,#15933);
#14641=AXIS2_PLACEMENT_3D('',#25187,#15935,#15936);
#14642=AXIS2_PLACEMENT_3D('',#25235,#15938,#15939);
#14643=AXIS2_PLACEMENT_3D('',#25283,#15941,#15942);
#14644=AXIS2_PLACEMENT_3D('',#25331,#15944,#15945);
#14645=AXIS2_PLACEMENT_3D('',#25385,#15947,#15948);
#14646=AXIS2_PLACEMENT_3D('',#25433,#15950,#15951);
#14647=AXIS2_PLACEMENT_3D('',#25481,#15953,#15954);
#14648=AXIS2_PLACEMENT_3D('',#25497,#15956,#15957);
#14649=AXIS2_PLACEMENT_3D('',#25506,#15958,#15959);
#14650=AXIS2_PLACEMENT_3D('',#25531,#15961,#15962);
#14651=AXIS2_PLACEMENT_3D('',#25555,#15964,#15965);
#14652=AXIS2_PLACEMENT_3D('',#25580,#15967,#15968);
#14653=AXIS2_PLACEMENT_3D('',#25605,#15970,#15971);
#14654=AXIS2_PLACEMENT_3D('',#25629,#15973,#15974);
#14655=AXIS2_PLACEMENT_3D('',#25653,#15976,#15977);
#14656=AXIS2_PLACEMENT_3D('',#25678,#15979,#15980);
#14657=AXIS2_PLACEMENT_3D('',#25703,#15982,#15983);
#14658=AXIS2_PLACEMENT_3D('',#25727,#15985,#15986);
#14659=AXIS2_PLACEMENT_3D('',#25752,#15988,#15989);
#14660=AXIS2_PLACEMENT_3D('',#25777,#15991,#15992);
#14661=AXIS2_PLACEMENT_3D('',#25801,#15994,#15995);
#14662=AXIS2_PLACEMENT_3D('',#25825,#15997,#15998);
#14663=AXIS2_PLACEMENT_3D('',#25850,#16000,#16001);
#14664=AXIS2_PLACEMENT_3D('',#25875,#16003,#16004);
#14665=AXIS2_PLACEMENT_3D('',#25899,#16006,#16007);
#14666=AXIS2_PLACEMENT_3D('',#25924,#16009,#16010);
#14667=AXIS2_PLACEMENT_3D('',#25949,#16012,#16013);
#14668=AXIS2_PLACEMENT_3D('',#25973,#16015,#16016);
#14669=AXIS2_PLACEMENT_3D('',#25998,#16018,#16019);
#14670=AXIS2_PLACEMENT_3D('',#26023,#16021,#16022);
#14671=AXIS2_PLACEMENT_3D('',#26047,#16024,#16025);
#14672=AXIS2_PLACEMENT_3D('',#26071,#16027,#16028);
#14673=AXIS2_PLACEMENT_3D('',#26374,#16029,#16030);
#14674=AXIS2_PLACEMENT_3D('',#26408,#16032,#16033);
#14675=AXIS2_PLACEMENT_3D('',#27166,#16034,#16035);
#14676=AXIS2_PLACEMENT_3D('',#27177,#16036,#16037);
#14677=AXIS2_PLACEMENT_3D('',#27937,#16038,#16039);
#14678=AXIS2_PLACEMENT_3D('',#27938,#16040,#16041);
#14679=AXIS2_PLACEMENT_3D('',#27947,#16046,#16047);
#14680=AXIS2_PLACEMENT_3D('',#27953,#16051,#16052);
#14681=AXIS2_PLACEMENT_3D('',#27959,#16056,#16057);
#14682=AXIS2_PLACEMENT_3D('',#27965,#16061,#16062);
#14683=AXIS2_PLACEMENT_3D('',#27971,#16066,#16067);
#14684=AXIS2_PLACEMENT_3D('',#27974,#16070,#16071);
#14685=AXIS2_PLACEMENT_3D('',#27975,#16072,#16073);
#14686=AXIS2_PLACEMENT_3D('',#27977,#16074,#16075);
#14687=AXIS2_PLACEMENT_3D('',#27978,#16076,#16077);
#14688=AXIS2_PLACEMENT_3D('',#27981,#16079,#16080);
#14689=AXIS2_PLACEMENT_3D('',#27982,#16081,#16082);
#14690=AXIS2_PLACEMENT_3D('',#27983,#16083,#16084);
#15877=DIRECTION('axis',(0.,0.,1.));
#15878=DIRECTION('refdir',(1.,0.,0.));
#15879=DIRECTION('center_axis',(0.,0.,1.));
#15880=DIRECTION('ref_axis',(1.,0.,0.));
#15881=DIRECTION('',(0.,0.,-1.));
#15882=DIRECTION('center_axis',(0.,0.,-1.));
#15883=DIRECTION('ref_axis',(1.,0.,0.));
#15884=DIRECTION('center_axis',(0.,0.,1.));
#15885=DIRECTION('ref_axis',(1.,0.,0.));
#15886=DIRECTION('',(0.,0.,-1.));
#15887=DIRECTION('center_axis',(0.,0.,1.));
#15888=DIRECTION('ref_axis',(1.,0.,0.));
#15889=DIRECTION('',(0.,0.,-1.));
#15890=DIRECTION('center_axis',(0.,0.,1.));
#15891=DIRECTION('ref_axis',(1.,0.,0.));
#15892=DIRECTION('',(0.,0.,-1.));
#15893=DIRECTION('center_axis',(0.,0.,1.));
#15894=DIRECTION('ref_axis',(1.,0.,0.));
#15895=DIRECTION('',(0.,0.,-1.));
#15896=DIRECTION('center_axis',(0.,0.,1.));
#15897=DIRECTION('ref_axis',(1.,0.,0.));
#15898=DIRECTION('',(0.,0.,-1.));
#15899=DIRECTION('center_axis',(0.,0.,1.));
#15900=DIRECTION('ref_axis',(1.,0.,0.));
#15901=DIRECTION('',(0.,0.,-1.));
#15902=DIRECTION('center_axis',(0.,0.,1.));
#15903=DIRECTION('ref_axis',(1.,0.,0.));
#15904=DIRECTION('',(0.,0.,-1.));
#15905=DIRECTION('center_axis',(0.,0.,1.));
#15906=DIRECTION('ref_axis',(1.,0.,0.));
#15907=DIRECTION('',(0.,0.,-1.));
#15908=DIRECTION('center_axis',(0.,0.,1.));
#15909=DIRECTION('ref_axis',(1.,0.,0.));
#15910=DIRECTION('',(0.,0.,-1.));
#15911=DIRECTION('center_axis',(0.,0.,1.));
#15912=DIRECTION('ref_axis',(1.,0.,0.));
#15913=DIRECTION('',(0.,0.,-1.));
#15914=DIRECTION('center_axis',(0.,0.,1.));
#15915=DIRECTION('ref_axis',(1.,0.,0.));
#15916=DIRECTION('',(0.,0.,-1.));
#15917=DIRECTION('center_axis',(0.,0.,1.));
#15918=DIRECTION('ref_axis',(1.,0.,0.));
#15919=DIRECTION('',(0.,0.,-1.));
#15920=DIRECTION('center_axis',(0.,0.,1.));
#15921=DIRECTION('ref_axis',(1.,0.,0.));
#15922=DIRECTION('',(0.,0.,-1.));
#15923=DIRECTION('center_axis',(0.,0.,1.));
#15924=DIRECTION('ref_axis',(1.,0.,0.));
#15925=DIRECTION('',(0.,0.,-1.));
#15926=DIRECTION('center_axis',(0.,0.,1.));
#15927=DIRECTION('ref_axis',(1.,0.,0.));
#15928=DIRECTION('',(0.,0.,-1.));
#15929=DIRECTION('center_axis',(0.,0.,1.));
#15930=DIRECTION('ref_axis',(1.,0.,0.));
#15931=DIRECTION('',(0.,0.,-1.));
#15932=DIRECTION('center_axis',(0.,0.,1.));
#15933=DIRECTION('ref_axis',(1.,0.,0.));
#15934=DIRECTION('',(0.,0.,-1.));
#15935=DIRECTION('center_axis',(0.,0.,1.));
#15936=DIRECTION('ref_axis',(1.,0.,0.));
#15937=DIRECTION('',(0.,0.,-1.));
#15938=DIRECTION('center_axis',(0.,0.,1.));
#15939=DIRECTION('ref_axis',(1.,0.,0.));
#15940=DIRECTION('',(0.,0.,-1.));
#15941=DIRECTION('center_axis',(0.,0.,1.));
#15942=DIRECTION('ref_axis',(1.,0.,0.));
#15943=DIRECTION('',(0.,0.,-1.));
#15944=DIRECTION('center_axis',(0.,0.,1.));
#15945=DIRECTION('ref_axis',(1.,0.,0.));
#15946=DIRECTION('',(0.,0.,-1.));
#15947=DIRECTION('center_axis',(0.,0.,1.));
#15948=DIRECTION('ref_axis',(1.,0.,0.));
#15949=DIRECTION('',(0.,0.,-1.));
#15950=DIRECTION('center_axis',(0.,0.,1.));
#15951=DIRECTION('ref_axis',(1.,0.,0.));
#15952=DIRECTION('',(0.,0.,-1.));
#15953=DIRECTION('center_axis',(0.,0.,1.));
#15954=DIRECTION('ref_axis',(0.997333825498281,-0.0729742455731076,0.));
#15955=DIRECTION('',(0.,0.,1.));
#15956=DIRECTION('center_axis',(0.,0.,-1.));
#15957=DIRECTION('ref_axis',(1.,-6.20171864138877E-14,0.));
#15958=DIRECTION('center_axis',(0.,0.,1.));
#15959=DIRECTION('ref_axis',(1.,-6.20171864138877E-14,0.));
#15960=DIRECTION('',(0.,0.,1.));
#15961=DIRECTION('center_axis',(0.,0.,1.));
#15962=DIRECTION('ref_axis',(1.,-6.20171864138877E-14,0.));
#15963=DIRECTION('',(0.,0.,1.));
#15964=DIRECTION('center_axis',(0.,0.,1.));
#15965=DIRECTION('ref_axis',(1.,-6.20171864138877E-14,0.));
#15966=DIRECTION('',(0.,0.,1.));
#15967=DIRECTION('center_axis',(0.,0.,1.));
#15968=DIRECTION('ref_axis',(1.,-6.20171864138877E-14,0.));
#15969=DIRECTION('',(0.,0.,1.));
#15970=DIRECTION('center_axis',(0.,0.,1.));
#15971=DIRECTION('ref_axis',(1.,-6.20171864138877E-14,0.));
#15972=DIRECTION('',(0.,0.,1.));
#15973=DIRECTION('center_axis',(0.,0.,1.));
#15974=DIRECTION('ref_axis',(1.,-6.20171864138877E-14,0.));
#15975=DIRECTION('',(0.,0.,1.));
#15976=DIRECTION('center_axis',(0.,0.,1.));
#15977=DIRECTION('ref_axis',(1.,-6.20171864138877E-14,0.));
#15978=DIRECTION('',(0.,0.,1.));
#15979=DIRECTION('center_axis',(0.,0.,1.));
#15980=DIRECTION('ref_axis',(1.,-6.20171864138877E-14,0.));
#15981=DIRECTION('',(0.,0.,1.));
#15982=DIRECTION('center_axis',(0.,0.,1.));
#15983=DIRECTION('ref_axis',(1.,-6.20171864138877E-14,0.));
#15984=DIRECTION('',(0.,0.,1.));
#15985=DIRECTION('center_axis',(0.,0.,1.));
#15986=DIRECTION('ref_axis',(1.,-6.20171864138877E-14,0.));
#15987=DIRECTION('',(0.,0.,1.));
#15988=DIRECTION('center_axis',(0.,0.,1.));
#15989=DIRECTION('ref_axis',(1.,-6.20171864138877E-14,0.));
#15990=DIRECTION('',(0.,0.,1.));
#15991=DIRECTION('center_axis',(0.,0.,1.));
#15992=DIRECTION('ref_axis',(1.,-6.20171864138877E-14,0.));
#15993=DIRECTION('',(0.,0.,1.));
#15994=DIRECTION('center_axis',(0.,0.,1.));
#15995=DIRECTION('ref_axis',(1.,-6.20171864138877E-14,0.));
#15996=DIRECTION('',(0.,0.,1.));
#15997=DIRECTION('center_axis',(0.,0.,1.));
#15998=DIRECTION('ref_axis',(1.,-6.20171864138877E-14,0.));
#15999=DIRECTION('',(0.,0.,1.));
#16000=DIRECTION('center_axis',(0.,0.,1.));
#16001=DIRECTION('ref_axis',(1.,-6.20171864138877E-14,0.));
#16002=DIRECTION('',(0.,0.,1.));
#16003=DIRECTION('center_axis',(0.,0.,1.));
#16004=DIRECTION('ref_axis',(1.,-6.20171864138877E-14,0.));
#16005=DIRECTION('',(0.,0.,1.));
#16006=DIRECTION('center_axis',(0.,0.,1.));
#16007=DIRECTION('ref_axis',(1.,-6.20171864138877E-14,0.));
#16008=DIRECTION('',(0.,0.,1.));
#16009=DIRECTION('center_axis',(0.,0.,1.));
#16010=DIRECTION('ref_axis',(1.,-6.20171864138877E-14,0.));
#16011=DIRECTION('',(0.,0.,1.));
#16012=DIRECTION('center_axis',(0.,0.,1.));
#16013=DIRECTION('ref_axis',(1.,-6.20171864138877E-14,0.));
#16014=DIRECTION('',(0.,0.,1.));
#16015=DIRECTION('center_axis',(0.,0.,1.));
#16016=DIRECTION('ref_axis',(1.,-6.20171864138877E-14,0.));
#16017=DIRECTION('',(0.,0.,1.));
#16018=DIRECTION('center_axis',(0.,0.,1.));
#16019=DIRECTION('ref_axis',(1.,-6.20171864138877E-14,0.));
#16020=DIRECTION('',(0.,0.,1.));
#16021=DIRECTION('center_axis',(0.,0.,1.));
#16022=DIRECTION('ref_axis',(1.,-6.20171864138877E-14,0.));
#16023=DIRECTION('',(0.,0.,1.));
#16024=DIRECTION('center_axis',(0.,0.,1.));
#16025=DIRECTION('ref_axis',(1.,-6.20171864138877E-14,0.));
#16026=DIRECTION('',(0.,0.,1.));
#16027=DIRECTION('center_axis',(0.,0.,-1.));
#16028=DIRECTION('ref_axis',(1.,0.,0.));
#16029=DIRECTION('center_axis',(0.,0.,-1.));
#16030=DIRECTION('ref_axis',(1.,0.,0.));
#16031=DIRECTION('',(0.707106781186547,8.65956056235493E-17,0.707106781186548));
#16032=DIRECTION('center_axis',(0.,0.,1.));
#16033=DIRECTION('ref_axis',(1.,0.,0.));
#16034=DIRECTION('center_axis',(0.,0.,1.));
#16035=DIRECTION('ref_axis',(1.,-6.20171864138877E-14,0.));
#16036=DIRECTION('center_axis',(0.,0.,-1.));
#16037=DIRECTION('ref_axis',(1.,-6.20171864138877E-14,0.));
#16038=DIRECTION('center_axis',(0.,0.,1.));
#16039=DIRECTION('ref_axis',(1.,0.,0.));
#16040=DIRECTION('center_axis',(-1.60246890531964E-16,-1.,0.));
#16041=DIRECTION('ref_axis',(1.,-1.60246890531964E-16,0.));
#16042=DIRECTION('',(1.,-1.60246890531964E-16,0.));
#16043=DIRECTION('',(0.,0.,1.));
#16044=DIRECTION('',(1.,-1.60246890531964E-16,0.));
#16045=DIRECTION('',(0.,0.,1.));
#16046=DIRECTION('center_axis',(-0.866025403784439,-0.5,0.));
#16047=DIRECTION('ref_axis',(0.5,-0.866025403784439,0.));
#16048=DIRECTION('',(0.5,-0.866025403784439,0.));
#16049=DIRECTION('',(0.,0.,1.));
#16050=DIRECTION('',(0.5,-0.866025403784439,0.));
#16051=DIRECTION('center_axis',(-0.866025403784439,0.5,0.));
#16052=DIRECTION('ref_axis',(-0.5,-0.866025403784439,0.));
#16053=DIRECTION('',(-0.5,-0.866025403784439,0.));
#16054=DIRECTION('',(0.,0.,1.));
#16055=DIRECTION('',(-0.5,-0.866025403784439,0.));
#16056=DIRECTION('center_axis',(1.60246890531964E-16,1.,0.));
#16057=DIRECTION('ref_axis',(-1.,1.60246890531964E-16,0.));
#16058=DIRECTION('',(-1.,1.60246890531964E-16,0.));
#16059=DIRECTION('',(0.,0.,1.));
#16060=DIRECTION('',(-1.,1.60246890531964E-16,0.));
#16061=DIRECTION('center_axis',(0.866025403784439,0.5,0.));
#16062=DIRECTION('ref_axis',(-0.5,0.866025403784439,0.));
#16063=DIRECTION('',(-0.5,0.866025403784439,0.));
#16064=DIRECTION('',(0.,0.,1.));
#16065=DIRECTION('',(-0.5,0.866025403784439,0.));
#16066=DIRECTION('center_axis',(0.866025403784439,-0.5,0.));
#16067=DIRECTION('ref_axis',(0.5,0.866025403784439,0.));
#16068=DIRECTION('',(0.5,0.866025403784439,0.));
#16069=DIRECTION('',(0.5,0.866025403784439,0.));
#16070=DIRECTION('center_axis',(0.,0.,1.));
#16071=DIRECTION('ref_axis',(1.,0.,0.));
#16072=DIRECTION('center_axis',(0.,0.,1.));
#16073=DIRECTION('ref_axis',(1.,0.,0.));
#16074=DIRECTION('center_axis',(0.,0.,1.));
#16075=DIRECTION('ref_axis',(1.,0.,0.));
#16076=DIRECTION('center_axis',(0.,0.,1.));
#16077=DIRECTION('ref_axis',(1.,0.,0.));
#16078=DIRECTION('',(0.,0.,-1.));
#16079=DIRECTION('center_axis',(0.,0.,1.));
#16080=DIRECTION('ref_axis',(1.,0.,0.));
#16081=DIRECTION('center_axis',(0.,0.,1.));
#16082=DIRECTION('ref_axis',(1.,0.,0.));
#16083=DIRECTION('center_axis',(0.,0.,1.));
#16084=DIRECTION('ref_axis',(1.,0.,0.));
#24316=CARTESIAN_POINT('',(0.,0.,0.));
#24317=CARTESIAN_POINT('Origin',(0.,0.,0.));
#24318=CARTESIAN_POINT('',(-3.94684541635378,0.00250618816942501,0.322176117089595));
#24319=CARTESIAN_POINT('',(-3.94571229786942,0.00420644411048898,0.1778238829104));
#24320=CARTESIAN_POINT('',(-3.942,-4.82755768223887E-16,0.));
#24321=CARTESIAN_POINT('',(1.7270326134187,3.54354657824448,0.));
#24322=CARTESIAN_POINT('Ctrl Pts',(-3.94684541635378,0.00250618816942501,
0.322176117089595));
#24323=CARTESIAN_POINT('Ctrl Pts',(-3.94773112778461,0.132835587750837,
0.316895328369763));
#24324=CARTESIAN_POINT('Ctrl Pts',(-3.94183789351545,0.26307859818693,0.311614539649932));
#24325=CARTESIAN_POINT('Ctrl Pts',(-3.92890301514817,0.39261184999977,0.3063337509301));
#24326=CARTESIAN_POINT('Ctrl Pts',(-3.79917189807037,1.69177315474756,0.253369772435476));
#24327=CARTESIAN_POINT('Ctrl Pts',(-2.96110743411295,2.91953839146377,0.200405793940852));
#24328=CARTESIAN_POINT('Ctrl Pts',(-1.79852789548214,3.51470668248002,0.147441815446229));
#24329=CARTESIAN_POINT('Ctrl Pts',(-0.719726524887938,4.06698577113378,
0.098294543630819));
#24330=CARTESIAN_POINT('Ctrl Pts',(0.638504507243322,4.07455564834572,0.0491472718154096));
#24331=CARTESIAN_POINT('Ctrl Pts',(1.73118107496479,3.54876586530513,-4.77048955893622E-17));
#24332=CARTESIAN_POINT('',(-1.72703261341866,3.5435465782445,0.));
#24333=CARTESIAN_POINT('Origin',(0.,0.,0.));
#24334=CARTESIAN_POINT('Ctrl Pts',(-1.72703261341866,3.5435465782445,-1.38777878078145E-15));
#24335=CARTESIAN_POINT('Ctrl Pts',(-2.90680413394004,2.96855656546122,0.0529882887282479));
#24336=CARTESIAN_POINT('Ctrl Pts',(-3.76655616656995,1.76297958901422,0.105976577456497));
#24337=CARTESIAN_POINT('Ctrl Pts',(-3.92036033233788,0.467860933696955,
0.158964866184747));
#24338=CARTESIAN_POINT('Ctrl Pts',(-3.93860710223307,0.314212741058287,
0.165251205093298));
#24339=CARTESIAN_POINT('Ctrl Pts',(-3.94691794439651,0.159304285881835,
0.171537544001849));
#24340=CARTESIAN_POINT('Ctrl Pts',(-3.94571229786942,0.00420644411048898,
0.1778238829104));
#24341=CARTESIAN_POINT('Origin',(0.,0.,0.));
#24342=CARTESIAN_POINT('',(-3.93670753965503,0.00216852164164449,1.32217611708959));
#24343=CARTESIAN_POINT('',(-3.93636006504333,0.00190811380198534,1.1778238829104));
#24344=CARTESIAN_POINT('',(-3.942,-4.82755768223887E-16,0.));
#24345=CARTESIAN_POINT('Ctrl Pts',(-3.93670753965503,0.00216852164164449,
1.32217611708959));
#24346=CARTESIAN_POINT('Ctrl Pts',(-3.93928378279248,0.519701728735777,
1.30134586600417));
#24347=CARTESIAN_POINT('Ctrl Pts',(-3.8445230015698,1.03632804611489,1.28051561491875));
#24348=CARTESIAN_POINT('Ctrl Pts',(-3.6480161981814,1.51081450660005,1.25968536383333));
#24349=CARTESIAN_POINT('Ctrl Pts',(-3.14836873517057,2.71726615166507,1.2067213853387));
#24350=CARTESIAN_POINT('Ctrl Pts',(-1.9909276922364,3.6512813246822,1.15375740684408));
#24351=CARTESIAN_POINT('Ctrl Pts',(-0.706151782787128,3.88482400643261,
1.10079342834945));
#24352=CARTESIAN_POINT('Ctrl Pts',(0.57862412666215,4.11836668818302,1.04782944985483));
#24353=CARTESIAN_POINT('Ctrl Pts',(1.99073490262654,3.65143687866671,0.994865471360208));
#24354=CARTESIAN_POINT('Ctrl Pts',(2.88298828242626,2.69797395029701,0.941901492865584));
#24355=CARTESIAN_POINT('Ctrl Pts',(3.77524166222597,1.74451102192732,0.88893751437096));
#24356=CARTESIAN_POINT('Ctrl Pts',(4.14763764586101,0.304514974704242,0.835973535876336));
#24357=CARTESIAN_POINT('Ctrl Pts',(3.82952478082154,-0.96194142997557,0.783009557381713));
#24358=CARTESIAN_POINT('Ctrl Pts',(3.51141191578207,-2.22839783465538,0.730045578887089));
#24359=CARTESIAN_POINT('Ctrl Pts',(2.50279020206811,-3.32131459679193,0.677081600392466));
#24360=CARTESIAN_POINT('Ctrl Pts',(1.26587965171505,-3.74001178475658,0.624117621897842));
#24361=CARTESIAN_POINT('Ctrl Pts',(0.0289691013620001,-4.15870897272123,
0.571153643403219));
#24362=CARTESIAN_POINT('Ctrl Pts',(-1.43623028563014,-3.90318658651399,
0.518189664908595));
#24363=CARTESIAN_POINT('Ctrl Pts',(-2.45813109402713,-3.09014670702069,
0.465225686413971));
#24364=CARTESIAN_POINT('Ctrl Pts',(-3.37814298820071,-2.35817120272038,
0.417542496639179));
#24365=CARTESIAN_POINT('Ctrl Pts',(-3.9388478333255,-1.17431072748125,0.369859306864387));
#24366=CARTESIAN_POINT('Ctrl Pts',(-3.94684541635378,0.00250618816942501,
0.322176117089595));
#24367=CARTESIAN_POINT('Ctrl Pts',(-3.94571229786942,0.00420644411048898,
0.1778238829104));
#24368=CARTESIAN_POINT('Ctrl Pts',(-3.93675540826681,-1.14803363217555,
0.224525832730098));
#24369=CARTESIAN_POINT('Ctrl Pts',(-3.40256651647006,-2.31072629277711,
0.271227782549796));
#24370=CARTESIAN_POINT('Ctrl Pts',(-2.51512664140724,-3.04478428612434,
0.317929732369494));
#24371=CARTESIAN_POINT('Ctrl Pts',(-1.50823248580272,-3.87765051644084,
0.370918021097743));
#24372=CARTESIAN_POINT('Ctrl Pts',(-0.0465878756876988,-4.1587226428863,
0.423906309825993));
#24373=CARTESIAN_POINT('Ctrl Pts',(1.1983574972874,-3.76190237425103,0.476894598554242));
#24374=CARTESIAN_POINT('Ctrl Pts',(2.44330287026249,-3.36508210561577,0.529882887282491));
#24375=CARTESIAN_POINT('Ctrl Pts',(3.47154900609766,-2.29036944189979,0.58287117601074));
#24376=CARTESIAN_POINT('Ctrl Pts',(3.81196419489399,-1.02929753659268,0.635859464738989));
#24377=CARTESIAN_POINT('Ctrl Pts',(4.15237938369031,0.231774368714438,0.688847753467239));
#24378=CARTESIAN_POINT('Ctrl Pts',(3.80496362544778,1.67920551561269,0.741836042195488));
#24379=CARTESIAN_POINT('Ctrl Pts',(2.92880392464218,2.64832610367255,0.794824330923737));
#24380=CARTESIAN_POINT('Ctrl Pts',(2.05264422383658,3.61744669173242,0.847812619651987));
#24381=CARTESIAN_POINT('Ctrl Pts',(0.647740580467906,4.1082567209539,0.900800908380236));
#24382=CARTESIAN_POINT('Ctrl Pts',(-0.641345987445116,3.89601342814375,
0.953789197108486));
#24383=CARTESIAN_POINT('Ctrl Pts',(-1.93043255535814,3.68377013533359,1.00677748583673));
#24384=CARTESIAN_POINT('Ctrl Pts',(-3.10370204781551,2.7684735204918,1.05976577456498));
#24385=CARTESIAN_POINT('Ctrl Pts',(-3.6230578333699,1.56976054866973,1.11275406329323));
#24386=CARTESIAN_POINT('Ctrl Pts',(-3.83564812513838,1.0790858560709,1.13444400316562));
#24387=CARTESIAN_POINT('Ctrl Pts',(-3.9386720278785,0.540923388712033,1.15613394303801));
#24388=CARTESIAN_POINT('Ctrl Pts',(-3.93636006504333,0.00190811380198534,
1.1778238829104));
#24389=CARTESIAN_POINT('Origin',(0.,0.,0.));
#24390=CARTESIAN_POINT('',(-3.93898402517327,-0.0032694952000395,2.32217611708959));
#24391=CARTESIAN_POINT('',(-3.93943713807335,-0.00339197931643889,2.1778238829104));
#24392=CARTESIAN_POINT('',(-3.942,-4.82755768223887E-16,0.));
#24393=CARTESIAN_POINT('Ctrl Pts',(-3.93898402517327,-0.0032694952000395,
2.32217611708959));
#24394=CARTESIAN_POINT('Ctrl Pts',(-3.93192709039827,0.89928000152811,2.28579640363858));
#24395=CARTESIAN_POINT('Ctrl Pts',(-3.6239186993101,1.80618191912708,2.24941669018756));
#24396=CARTESIAN_POINT('Ctrl Pts',(-3.05593295732034,2.50036976841156,2.21303697673655));
#24397=CARTESIAN_POINT('Ctrl Pts',(-2.22902197396405,3.51101407626844,2.16007299824193));
#24398=CARTESIAN_POINT('Ctrl Pts',(-0.851077281590667,4.07080133208995,
2.1071090197473));
#24399=CARTESIAN_POINT('Ctrl Pts',(0.446378324979883,3.92317725380663,2.05414504125268));
#24400=CARTESIAN_POINT('Ctrl Pts',(1.74383393155043,3.77555317552331,2.00118106275806));
#24401=CARTESIAN_POINT('Ctrl Pts',(2.96080045231815,2.92051776313515,1.94821708426343));
#24402=CARTESIAN_POINT('Ctrl Pts',(3.53953231896037,1.74993928366879,1.89525310576881));
#24403=CARTESIAN_POINT('Ctrl Pts',(4.11826418560259,0.57936080420243,1.84228912727419));
#24404=CARTESIAN_POINT('Ctrl Pts',(4.05876139811932,-0.906760742342139,
1.78932514877956));
#24405=CARTESIAN_POINT('Ctrl Pts',(3.38829497669137,-2.0273218478537,1.73636117028494));
#24406=CARTESIAN_POINT('Ctrl Pts',(2.71782855526341,-3.14788295336526,1.68339719179031));
#24407=CARTESIAN_POINT('Ctrl Pts',(1.43639849989078,-3.90288361784382,1.63043321329569));
#24408=CARTESIAN_POINT('Ctrl Pts',(0.131293493556904,-3.9463054651445,1.57746923480107));
#24409=CARTESIAN_POINT('Ctrl Pts',(-1.17381151277698,-3.98972731244518,
1.52450525630644));
#24410=CARTESIAN_POINT('Ctrl Pts',(-2.50259147007212,-3.32157034256797,
1.47154127781182));
#24411=CARTESIAN_POINT('Ctrl Pts',(-3.24605450717593,-2.24804779907291,
1.4185772993172));
#24412=CARTESIAN_POINT('Ctrl Pts',(-3.69712029286904,-1.59673190927805,
1.386443571908));
#24413=CARTESIAN_POINT('Ctrl Pts',(-3.93273330552895,-0.796202603784206,
1.3543098444988));
#24414=CARTESIAN_POINT('Ctrl Pts',(-3.93670753965503,0.00216852164164449,
1.32217611708959));
#24415=CARTESIAN_POINT('Ctrl Pts',(-3.93636006504333,0.00190811380198534,
1.1778238829104));
#24416=CARTESIAN_POINT('Ctrl Pts',(-3.93302392765509,-0.775885103331329,
1.20912223176626));
#24417=CARTESIAN_POINT('Ctrl Pts',(-3.71035557449182,-1.55545405153981,
1.24042058062212));
#24418=CARTESIAN_POINT('Ctrl Pts',(-3.28106611164764,-2.19667847798475,
1.27171892947798));
#24419=CARTESIAN_POINT('Ctrl Pts',(-2.5542765257196,-3.28227520401484,1.32470721820623));
#24420=CARTESIAN_POINT('Ctrl Pts',(-1.23525527521213,-3.97133932727269,
1.37769550693448));
#24421=CARTESIAN_POINT('Ctrl Pts',(0.0709513775297463,-3.94785759961686,
1.43068379566273));
#24422=CARTESIAN_POINT('Ctrl Pts',(1.37715803027162,-3.92437587196102,1.48367208439098));
#24423=CARTESIAN_POINT('Ctrl Pts',(2.67055008524789,-3.1883482933915,1.53666037311923));
#24424=CARTESIAN_POINT('Ctrl Pts',(3.3578681272901,-2.07735647460328,1.58964866184748));
#24425=CARTESIAN_POINT('Ctrl Pts',(4.0451861693323,-0.966364655815065,1.64263695057573));
#24426=CARTESIAN_POINT('Ctrl Pts',(4.12643019844044,0.519591403191845,1.69562523930397));
#24427=CARTESIAN_POINT('Ctrl Pts',(3.56432857554823,1.69889860460012,1.74861352803222));
#24428=CARTESIAN_POINT('Ctrl Pts',(3.00222695265603,2.87820580600839,1.80160181676047));
#24429=CARTESIAN_POINT('Ctrl Pts',(1.7967796777635,3.75086414981802,1.85459010548872));
#24430=CARTESIAN_POINT('Ctrl Pts',(0.500920035194316,3.91659925522552,1.90757839421697));
#24431=CARTESIAN_POINT('Ctrl Pts',(-0.794939607374858,4.08233436063301,
1.96056668294522));
#24432=CARTESIAN_POINT('Ctrl Pts',(-2.18121161762068,3.54114622763838,2.01355497167347));
#24433=CARTESIAN_POINT('Ctrl Pts',(-3.02202408579975,2.54126994215436,2.06654326040172));
#24434=CARTESIAN_POINT('Ctrl Pts',(-3.61062040344951,1.84132373296486,2.10363680123794));
#24435=CARTESIAN_POINT('Ctrl Pts',(-3.93191648715648,0.916599256990189,
2.14073034207417));
#24436=CARTESIAN_POINT('Ctrl Pts',(-3.93943713807335,-0.00339197931643889,
2.1778238829104));
#24437=CARTESIAN_POINT('Origin',(0.,0.,0.));
#24438=CARTESIAN_POINT('',(-3.94841909008794,-0.000476659622032916,3.3221761170896));
#24439=CARTESIAN_POINT('',(-3.94848727448062,-0.000227313299713517,3.1778238829104));
#24440=CARTESIAN_POINT('',(-3.942,-4.82755768223887E-16,0.));
#24441=CARTESIAN_POINT('Ctrl Pts',(-3.94841909008794,-0.000476659622032916,
3.3221761170896));
#24442=CARTESIAN_POINT('Ctrl Pts',(-3.94623626626659,1.27989932784314,3.27024694127299));
#24443=CARTESIAN_POINT('Ctrl Pts',(-3.2656648832367,2.56226681984272,3.21831776545638));
#24444=CARTESIAN_POINT('Ctrl Pts',(-2.20319423243154,3.27666141545475,3.16638858963978));
#24445=CARTESIAN_POINT('Ctrl Pts',(-1.11955152454134,4.00529188962783,3.11342461114515));
#24446=CARTESIAN_POINT('Ctrl Pts',(0.361362461026873,4.14308771897741,3.06046063265053));
#24447=CARTESIAN_POINT('Ctrl Pts',(1.56083317716561,3.62689600200629,3.00749665415591));
#24448=CARTESIAN_POINT('Ctrl Pts',(2.76030389330435,3.11070428503517,2.95453267566128));
#24449=CARTESIAN_POINT('Ctrl Pts',(3.67833134001362,1.94052502174336,2.90156869716666));
#24450=CARTESIAN_POINT('Ctrl Pts',(3.89417629964206,0.652660565018754,2.84860471867204));
#24451=CARTESIAN_POINT('Ctrl Pts',(4.11002125927051,-0.635203891705856,
2.79564074017741));
#24452=CARTESIAN_POINT('Ctrl Pts',(3.62368373181814,-2.04075354186327,2.74267676168279));
#24453=CARTESIAN_POINT('Ctrl Pts',(2.65805604729365,-2.91981385750971,2.68971278318817));
#24454=CARTESIAN_POINT('Ctrl Pts',(1.69242836276915,-3.79887417315615,2.63674880469354));
#24455=CARTESIAN_POINT('Ctrl Pts',(0.247510521172539,-4.15144515429161,
2.58378482619892));
#24456=CARTESIAN_POINT('Ctrl Pts',(-1.01448026111426,-3.8159408321598,2.53082084770429));
#24457=CARTESIAN_POINT('Ctrl Pts',(-2.27647104340105,-3.48043651002799,
2.47785686920967));
#24458=CARTESIAN_POINT('Ctrl Pts',(-3.35553476637803,-2.45685688462891,
2.42489289071505));
#24459=CARTESIAN_POINT('Ctrl Pts',(-3.75712799069693,-1.21431639198325,
2.37192891222042));
#24460=CARTESIAN_POINT('Ctrl Pts',(-3.88287625699264,-0.825247793982355,
2.35534464717681));
#24461=CARTESIAN_POINT('Ctrl Pts',(-3.94220103997636,-0.414710890659917,
2.3387603821332));
#24462=CARTESIAN_POINT('Ctrl Pts',(-3.93898402517327,-0.0032694952000395,
2.32217611708959));
#24463=CARTESIAN_POINT('Ctrl Pts',(-3.93943713807335,-0.00339197931643889,
2.1778238829104));
#24464=CARTESIAN_POINT('Ctrl Pts',(-3.9426597705752,-0.397612332356497,
2.19371863080242));
#24465=CARTESIAN_POINT('Ctrl Pts',(-3.8882681890457,-0.790963586497156,
2.20961337869445));
#24466=CARTESIAN_POINT('Ctrl Pts',(-3.77260571048107,-1.16538770550329,
2.22550812658647));
#24467=CARTESIAN_POINT('Ctrl Pts',(-3.387021940871,-2.41360462970351,2.27849641531472));
#24468=CARTESIAN_POINT('Ctrl Pts',(-2.32050147553854,-3.45147404013054,
2.33148470404296));
#24469=CARTESIAN_POINT('Ctrl Pts',(-1.06225033291184,-3.80293352608456,
2.38447299277121));
#24470=CARTESIAN_POINT('Ctrl Pts',(0.19600080971487,-4.15439301203859,2.43746128149946));
#24471=CARTESIAN_POINT('Ctrl Pts',(1.64598262963581,-3.81944257351961,2.49044957022771));
#24472=CARTESIAN_POINT('Ctrl Pts',(2.62259865984893,-2.95172107137353,2.54343785895596));
#24473=CARTESIAN_POINT('Ctrl Pts',(3.59921469006204,-2.08399956922746,2.59642614768421));
#24474=CARTESIAN_POINT('Ctrl Pts',(4.10246493056733,-0.683507003454308,
2.64941443641246));
#24475=CARTESIAN_POINT('Ctrl Pts',(3.90151184350976,0.607360005829592,2.70240272514071));
#24476=CARTESIAN_POINT('Ctrl Pts',(3.70055875645219,1.89822701511349,2.75539101386896));
#24477=CARTESIAN_POINT('Ctrl Pts',(2.79540234183177,3.07946846790813,2.80837930259721));
#24478=CARTESIAN_POINT('Ctrl Pts',(1.60123168012205,3.60925720078016,2.86136759132546));
#24479=CARTESIAN_POINT('Ctrl Pts',(0.407061018412325,4.1390459336522,2.91435588005371));
#24480=CARTESIAN_POINT('Ctrl Pts',(-1.0761238903867,4.01738194660163,2.96734416878196));
#24481=CARTESIAN_POINT('Ctrl Pts',(-2.16799636339283,3.30007158724765,3.0203324575102));
#24482=CARTESIAN_POINT('Ctrl Pts',(-3.24974830176843,2.58940995703755,3.07282959931027));
#24483=CARTESIAN_POINT('Ctrl Pts',(-3.94740831268547,1.29409283853931,3.12532674111033));
#24484=CARTESIAN_POINT('Ctrl Pts',(-3.94848727448062,-0.000227313299713517,
3.1778238829104));
#24485=CARTESIAN_POINT('Origin',(0.,0.,0.));
#24486=CARTESIAN_POINT('',(-3.94039517343639,0.00354505425716481,4.32217611708959));
#24487=CARTESIAN_POINT('',(-3.94011414712863,0.00351656949004968,4.1778238829104));
#24488=CARTESIAN_POINT('',(-3.942,-4.82755768223887E-16,0.));
#24489=CARTESIAN_POINT('Ctrl Pts',(-3.94039517343639,0.00354505425716481,
4.32217611708959));
#24490=CARTESIAN_POINT('Ctrl Pts',(-3.94353004938676,0.363314892612021,
4.30766145740202));
#24491=CARTESIAN_POINT('Ctrl Pts',(-3.89832073254977,0.722311104007169,
4.29314679771445));
#24492=CARTESIAN_POINT('Ctrl Pts',(-3.80162926767229,1.06685976451013,4.27863213802688));
#24493=CARTESIAN_POINT('Ctrl Pts',(-3.44880221029601,2.32411747761066,4.22566815953225));
#24494=CARTESIAN_POINT('Ctrl Pts',(-2.41048038450093,3.38900325344725,4.17270418103763));
#24495=CARTESIAN_POINT('Ctrl Pts',(-1.16253486527102,3.7734715492884,4.119740202543));
#24496=CARTESIAN_POINT('Ctrl Pts',(0.0854106539588831,4.15793984512954,
4.06677622404838));
#24497=CARTESIAN_POINT('Ctrl Pts',(1.54297986662362,3.86199066097525,4.01381224555376));
#24498=CARTESIAN_POINT('Ctrl Pts',(2.54215731665373,3.02125984033277,3.96084826705914));
#24499=CARTESIAN_POINT('Ctrl Pts',(3.54133476668386,2.18052901969028,3.90788428856451));
#24500=CARTESIAN_POINT('Ctrl Pts',(4.08212045407936,0.795016562559593,3.85492031006988));
#24501=CARTESIAN_POINT('Ctrl Pts',(3.91666803670668,-0.500286254334146,
3.80195633157526));
#24502=CARTESIAN_POINT('Ctrl Pts',(3.75121561933401,-1.79558907122787,3.74899235308063));
#24503=CARTESIAN_POINT('Ctrl Pts',(2.87952509719318,-3.00068224788464,3.69602837458601));
#24504=CARTESIAN_POINT('Ctrl Pts',(1.70109910586756,-3.56326208407903,3.64306439609139));
#24505=CARTESIAN_POINT('Ctrl Pts',(0.522673114541947,-4.12584192027342,
3.59010041759677));
#24506=CARTESIAN_POINT('Ctrl Pts',(-0.962488345968457,-4.04590841600543,
3.53713643910214));
#24507=CARTESIAN_POINT('Ctrl Pts',(-2.07372407526821,-3.36009572803379,
3.48417246060752));
#24508=CARTESIAN_POINT('Ctrl Pts',(-3.18495980456796,-2.67428304006214,
3.4312084821129));
#24509=CARTESIAN_POINT('Ctrl Pts',(-3.92226980265706,-1.38259116838684,
3.37824450361827));
#24510=CARTESIAN_POINT('Ctrl Pts',(-3.94773908659551,-0.0770126730508915,
3.32528052512365));
#24511=CARTESIAN_POINT('Ctrl Pts',(-3.94823670184224,-0.0515044661197667,
3.32424572244563));
#24512=CARTESIAN_POINT('Ctrl Pts',(-3.94846258763822,-0.025990958277152,
3.32321091976761));
#24513=CARTESIAN_POINT('Ctrl Pts',(-3.94841909008794,-0.000476659622032916,
3.3221761170896));
#24514=CARTESIAN_POINT('Ctrl Pts',(-3.94848727448062,-0.000227313299713517,
3.1778238829104));
#24515=CARTESIAN_POINT('Ctrl Pts',(-3.94849736891154,-0.0123365700109349,
3.17831502983858));
#24516=CARTESIAN_POINT('Ctrl Pts',(-3.94844649235883,-0.0244457394587464,
3.17880617676677));
#24517=CARTESIAN_POINT('Ctrl Pts',(-3.94833438892723,-0.0365543420562738,
3.17929732369495));
#24518=CARTESIAN_POINT('Ctrl Pts',(-3.9362399042423,-1.34291318034886,3.2322856124232));
#24519=CARTESIAN_POINT('Ctrl Pts',(-3.21149089765924,-2.64267412527665,
3.28527390115145));
#24520=CARTESIAN_POINT('Ctrl Pts',(-2.1065247612934,-3.33964579658387,3.3382621898797));
#24521=CARTESIAN_POINT('Ctrl Pts',(-1.00155862492758,-4.03661746789108,
3.39125047860795));
#24522=CARTESIAN_POINT('Ctrl Pts',(0.483624641221001,-4.13079986557773,
3.4442387673362));
#24523=CARTESIAN_POINT('Ctrl Pts',(1.66778169459976,-3.57899215935798,3.49722705606445));
#24524=CARTESIAN_POINT('Ctrl Pts',(2.85193874797851,-3.02718445313824,3.5502153447927));
#24525=CARTESIAN_POINT('Ctrl Pts',(3.73506958858744,-1.82938664301209,3.60320363352094));
#24526=CARTESIAN_POINT('Ctrl Pts',(3.91208817286041,-0.535020350876169,
3.65619192224919));
#24527=CARTESIAN_POINT('Ctrl Pts',(4.08910675713339,0.759345941259773,3.70918021097745));
#24528=CARTESIAN_POINT('Ctrl Pts',(3.56001308507038,2.1502807154055,3.7621684997057));
#24529=CARTESIAN_POINT('Ctrl Pts',(2.56749878545275,2.99977176280624,3.81515678843395));
#24530=CARTESIAN_POINT('Ctrl Pts',(1.57498448583515,3.84926281020697,3.86814507716219));
#24531=CARTESIAN_POINT('Ctrl Pts',(0.11904955866294,4.15731013086274,3.92113336589044));
#24532=CARTESIAN_POINT('Ctrl Pts',(-1.13247866152849,3.78261453618225,3.97412165461869));
#24533=CARTESIAN_POINT('Ctrl Pts',(-2.38400688171994,3.40791894150175,4.02710994334694));
#24534=CARTESIAN_POINT('Ctrl Pts',(-3.43112839493061,2.35048043148498,4.08009823207519));
#24535=CARTESIAN_POINT('Ctrl Pts',(-3.79353576624568,1.09533877709901,4.13308652080344));
#24536=CARTESIAN_POINT('Ctrl Pts',(-3.89552779876129,0.742105210239426,
4.14799897483909));
#24537=CARTESIAN_POINT('Ctrl Pts',(-3.94328881467064,0.373213076031263,
4.16291142887475));
#24538=CARTESIAN_POINT('Ctrl Pts',(-3.94011414712863,0.00351656949004968,
4.1778238829104));
#24539=CARTESIAN_POINT('Origin',(0.,0.,0.));
#24540=CARTESIAN_POINT('',(-3.93600110646763,-0.0014281919745418,5.32217611708959));
#24541=CARTESIAN_POINT('',(-3.93605515638862,-0.00152114337219748,5.1778238829104));
#24542=CARTESIAN_POINT('',(-3.942,-4.82755768223887E-16,0.));
#24543=CARTESIAN_POINT('Ctrl Pts',(-3.93600110646763,-0.0014281919745418,
5.32217611708959));
#24544=CARTESIAN_POINT('Ctrl Pts',(-3.93357236454694,0.74585693902175,5.29211199503643));
#24545=CARTESIAN_POINT('Ctrl Pts',(-3.72918845072319,1.49437332783476,5.26204787298327));
#24546=CARTESIAN_POINT('Ctrl Pts',(-3.33126090733014,2.11973479786067,5.2319837509301));
#24547=CARTESIAN_POINT('Ctrl Pts',(-2.63023175991589,3.22143440482896,5.17901977243548));
#24548=CARTESIAN_POINT('Ctrl Pts',(-1.32852280829314,3.94091180862283,5.12605579394085));
#24549=CARTESIAN_POINT('Ctrl Pts',(-0.0227175227337642,3.94842484544612,
5.07309181544622));
#24550=CARTESIAN_POINT('Ctrl Pts',(1.28308776282561,3.95593788226941,5.0201278369516));
#24551=CARTESIAN_POINT('Ctrl Pts',(2.59298938232161,3.25148655212212,4.96716385845699));
#24552=CARTESIAN_POINT('Ctrl Pts',(3.30664910123763,2.15792645084216,4.91419987996236));
#24553=CARTESIAN_POINT('Ctrl Pts',(4.02030882015365,1.06436634956219,4.86123590146774));
#24554=CARTESIAN_POINT('Ctrl Pts',(4.13772663848969,-0.418302522850447,
4.80827192297311));
#24555=CARTESIAN_POINT('Ctrl Pts',(3.60508904482309,-1.61056133843436,4.75530794447848));
#24556=CARTESIAN_POINT('Ctrl Pts',(3.07245145115649,-2.80282015401828,4.70234396598386));
#24557=CARTESIAN_POINT('Ctrl Pts',(1.88975844548724,-3.70466891277347,4.64937998748924));
#24558=CARTESIAN_POINT('Ctrl Pts',(0.599047552189011,-3.90278322178284,
4.59641600899462));
#24559=CARTESIAN_POINT('Ctrl Pts',(-0.691663341109217,-4.10089753079221,
4.54345203049999));
#24560=CARTESIAN_POINT('Ctrl Pts',(-2.09039212203642,-3.59527739005576,
4.49048805200536));
#24561=CARTESIAN_POINT('Ctrl Pts',(-2.95609036802126,-2.61765249450529,
4.43752407351074));
#24562=CARTESIAN_POINT('Ctrl Pts',(-3.58454594852404,-1.90794351207784,
4.39907475470369));
#24563=CARTESIAN_POINT('Ctrl Pts',(-3.93209089021995,-0.949484883048943,
4.36062543589664));
#24564=CARTESIAN_POINT('Ctrl Pts',(-3.94039517343639,0.00354505425716481,
4.32217611708959));
#24565=CARTESIAN_POINT('Ctrl Pts',(-3.94011414712863,0.00351656949004968,
4.1778238829104));
#24566=CARTESIAN_POINT('Ctrl Pts',(-3.93200829706235,-0.94042619377602,
4.215899717603));
#24567=CARTESIAN_POINT('Ctrl Pts',(-3.59183770381144,-1.88961289751958,
4.25397555229559));
#24568=CARTESIAN_POINT('Ctrl Pts',(-2.97445535308007,-2.59678570511794,
4.29205138698818));
#24569=CARTESIAN_POINT('Ctrl Pts',(-2.1152743391799,-3.5809237341938,4.34503967571643));
#24570=CARTESIAN_POINT('Ctrl Pts',(-0.719219081960083,-4.09635499359035,
4.39802796444469));
#24571=CARTESIAN_POINT('Ctrl Pts',(0.573349476162703,-3.90665471020838,
4.45101625317294));
#24572=CARTESIAN_POINT('Ctrl Pts',(1.86591803428548,-3.7169544268264,4.50400454190118));
#24573=CARTESIAN_POINT('Ctrl Pts',(3.05499989331122,-2.82212260066591,4.55699283062943));
#24574=CARTESIAN_POINT('Ctrl Pts',(3.59517138458731,-1.63261243464328,4.60998111935768));
#24575=CARTESIAN_POINT('Ctrl Pts',(4.13534287586339,-0.443102268620652,
4.66296940808593));
#24576=CARTESIAN_POINT('Ctrl Pts',(4.02660399938981,1.04108623726411,4.71595769681418));
#24577=CARTESIAN_POINT('Ctrl Pts',(3.31883252977577,2.13916602570979,4.76894598554243));
#24578=CARTESIAN_POINT('Ctrl Pts',(2.61106106016173,3.23724581415546,4.82193427427068));
#24579=CARTESIAN_POINT('Ctrl Pts',(1.3042569974072,3.94921688516205,4.87492256299893));
#24580=CARTESIAN_POINT('Ctrl Pts',(-0.00215762490102876,3.94850300633285,
4.92791085172718));
#24581=CARTESIAN_POINT('Ctrl Pts',(-1.30857224720925,3.94778912750366,4.98089914045543));
#24582=CARTESIAN_POINT('Ctrl Pts',(-2.61459742907118,3.23439029883869,5.03388742918367));
#24583=CARTESIAN_POINT('Ctrl Pts',(-3.32116840418697,2.13553765533301,5.08687571791192));
#24584=CARTESIAN_POINT('Ctrl Pts',(-3.72541706095167,1.50685388432656,5.11719177291141));
#24585=CARTESIAN_POINT('Ctrl Pts',(-3.93344647436031,0.751999581783958,
5.14750782791091));
#24586=CARTESIAN_POINT('Ctrl Pts',(-3.93605515638862,-0.00152114337219748,
5.1778238829104));
#24587=CARTESIAN_POINT('Origin',(0.,0.,0.));
#24588=CARTESIAN_POINT('',(-3.94563673384516,-0.00288256983268176,6.3221761170896));
#24589=CARTESIAN_POINT('',(-3.94570073178844,-0.00286656758253237,6.1778238829104));
#24590=CARTESIAN_POINT('',(-3.942,-4.82755768223887E-16,0.));
#24591=CARTESIAN_POINT('Ctrl Pts',(-3.94563673384516,-0.00288256983268176,
6.3221761170896));
#24592=CARTESIAN_POINT('Ctrl Pts',(-3.93638288024859,1.12386902299333,6.27656253267084));
#24593=CARTESIAN_POINT('Ctrl Pts',(-3.42887602753453,2.25790074792199,6.23094894825208));
#24594=CARTESIAN_POINT('Ctrl Pts',(-2.57675389815072,2.99180784716095,6.18533536383333));
#24595=CARTESIAN_POINT('Ctrl Pts',(-1.58731667872186,3.84398029351578,6.1323713853387));
#24596=CARTESIAN_POINT('Ctrl Pts',(-0.133249377743896,4.15668177021255,
6.07940740684408));
#24597=CARTESIAN_POINT('Ctrl Pts',(1.1190375023862,3.78659872632712,6.02644342834946));
#24598=CARTESIAN_POINT('Ctrl Pts',(2.37132438251632,3.41651568244167,5.97347944985483));
#24599=CARTESIAN_POINT('Ctrl Pts',(3.42183084179856,2.363648117974,5.92051547136021));
#24600=CARTESIAN_POINT('Ctrl Pts',(3.78910149173018,1.11053353453949,5.86755149286558));
#24601=CARTESIAN_POINT('Ctrl Pts',(4.15637214166179,-0.142581048895014,
5.81458751437096));
#24602=CARTESIAN_POINT('Ctrl Pts',(3.84040698224279,-1.59594265129635,5.76162353587634));
#24603=CARTESIAN_POINT('Ctrl Pts',(2.98601533590735,-2.58346419748652,5.70865955738171));
#24604=CARTESIAN_POINT('Ctrl Pts',(2.1316236895719,-3.57098574367668,5.65569557888709));
#24605=CARTESIAN_POINT('Ctrl Pts',(0.738805556320001,-4.09266723365567,
5.60273160039247));
#24606=CARTESIAN_POINT('Ctrl Pts',(-0.554099537676607,-3.9094179296049,
5.54976762189784));
#24607=CARTESIAN_POINT('Ctrl Pts',(-1.84700463167322,-3.72616862555414,
5.49680364340322));
#24608=CARTESIAN_POINT('Ctrl Pts',(-3.03999668641454,-2.83798852747363,
5.44383966490859));
#24609=CARTESIAN_POINT('Ctrl Pts',(-3.58631804218233,-1.65193757336201,
5.39087568641397));
#24610=CARTESIAN_POINT('Ctrl Pts',(-3.8225291610139,-1.1391287294386,5.36797582997251));
#24611=CARTESIAN_POINT('Ctrl Pts',(-3.93785108037402,-0.570635640986049,
5.34507597353105));
#24612=CARTESIAN_POINT('Ctrl Pts',(-3.93600110646763,-0.0014281919745418,
5.32217611708959));
#24613=CARTESIAN_POINT('Ctrl Pts',(-3.93605515638862,-0.00152114337219748,
5.1778238829104));
#24614=CARTESIAN_POINT('Ctrl Pts',(-3.93800609125369,-0.565050863861574,
5.20049611663916));
#24615=CARTESIAN_POINT('Ctrl Pts',(-3.82506562686086,-1.12783471721807,
5.22316835036792));
#24616=CARTESIAN_POINT('Ctrl Pts',(-3.59338498454405,-1.63654055836231,
5.24584058409668));
#24617=CARTESIAN_POINT('Ctrl Pts',(-3.05191382141567,-2.82545967020557,
5.29882887282492));
#24618=CARTESIAN_POINT('Ctrl Pts',(-1.86185472678928,-3.71899143554569,
5.35181716155317));
#24619=CARTESIAN_POINT('Ctrl Pts',(-0.569079620514193,-3.90727898054932,
5.40480545028142));
#24620=CARTESIAN_POINT('Ctrl Pts',(0.723695485760891,-4.09556652555295,
5.45779373900967));
#24621=CARTESIAN_POINT('Ctrl Pts',(2.11918660368467,-3.57860985022007,5.51078202773792));
#24622=CARTESIAN_POINT('Ctrl Pts',(2.97729155756073,-2.59353342519368,5.56377031646617));
#24623=CARTESIAN_POINT('Ctrl Pts',(3.83539651143679,-1.60845700016728,5.61675860519442));
#24624=CARTESIAN_POINT('Ctrl Pts',(4.15611530126515,-0.155260825447382,
5.66974689392266));
#24625=CARTESIAN_POINT('Ctrl Pts',(3.79233642449449,1.09948401069401,5.72273518265091));
#24626=CARTESIAN_POINT('Ctrl Pts',(3.42855754772383,2.35422884683541,5.77572347137916));
#24627=CARTESIAN_POINT('Ctrl Pts',(2.38028100435414,3.41052234439828,5.82871176010741));
#24628=CARTESIAN_POINT('Ctrl Pts',(1.12834403334923,3.78384994268096,5.88170004883566));
#24629=CARTESIAN_POINT('Ctrl Pts',(-0.12359293765566,4.15717754096363,5.93468833756392));
#24630=CARTESIAN_POINT('Ctrl Pts',(-1.57919033629578,3.8475392399661,5.98767662629216));
#24631=CARTESIAN_POINT('Ctrl Pts',(-2.57077564940419,2.99696399824068,6.04066491502041));
#24632=CARTESIAN_POINT('Ctrl Pts',(-3.4263409160258,2.26306584157345,6.08638457098374));
#24633=CARTESIAN_POINT('Ctrl Pts',(-3.93646396625886,1.126457364296,6.13210422694707));
#24634=CARTESIAN_POINT('Ctrl Pts',(-3.94570073178844,-0.00286656758253237,
6.1778238829104));
#24635=CARTESIAN_POINT('Origin',(0.,0.,0.));
#24636=CARTESIAN_POINT('',(-3.94505905468816,0.00309284708018512,7.32217611708959));
#24637=CARTESIAN_POINT('',(-3.94511280640764,0.00308469250234145,7.1778238829104));
#24638=CARTESIAN_POINT('',(-3.942,-4.82755768223887E-16,0.));
#24639=CARTESIAN_POINT('Ctrl Pts',(-3.94505905468816,0.00309284708018512,
7.32217611708959));
#24640=CARTESIAN_POINT('Ctrl Pts',(-3.9468047458557,0.205704294057958,7.31397704879987));
#24641=CARTESIAN_POINT('Ctrl Pts',(-3.93254600075262,0.408069386251045,
7.30577798051015));
#24642=CARTESIAN_POINT('Ctrl Pts',(-3.90142848745745,0.607808031556218,
7.29757891222042));
#24643=CARTESIAN_POINT('Ctrl Pts',(-3.7004169521544,1.89807089322147,7.2446149337258));
#24644=CARTESIAN_POINT('Ctrl Pts',(-2.79591524746178,3.0787362122301,7.19165095523118));
#24645=CARTESIAN_POINT('Ctrl Pts',(-1.60246363230549,3.60869576898733,7.13868697673655));
#24646=CARTESIAN_POINT('Ctrl Pts',(-0.409012017149199,4.13865532574456,
7.08572299824193));
#24647=CARTESIAN_POINT('Ctrl Pts',(1.07338950847076,4.01790912025038,7.03275901974731));
#24648=CARTESIAN_POINT('Ctrl Pts',(2.16534464372431,3.30179608998848,6.97979504125268));
#24649=CARTESIAN_POINT('Ctrl Pts',(3.25729977897786,2.58568305972658,6.92683106275806));
#24650=CARTESIAN_POINT('Ctrl Pts',(3.95880852386501,1.27420320469696,6.87386708426343));
#24651=CARTESIAN_POINT('Ctrl Pts',(3.94836389256626,-0.0315819228008631,
6.82090310576881));
#24652=CARTESIAN_POINT('Ctrl Pts',(3.93791926126751,-1.33736705029871,6.76793912727419));
#24653=CARTESIAN_POINT('Ctrl Pts',(3.21552125378285,-2.63745745026476,6.71497514877956));
#24654=CARTESIAN_POINT('Ctrl Pts',(2.11225056959203,-3.33601144740646,6.66201117028494));
#24655=CARTESIAN_POINT('Ctrl Pts',(1.00897988540122,-4.03456544454814,6.60904719179032));
#24656=CARTESIAN_POINT('Ctrl Pts',(-0.475163475495736,-4.1315830388655,
6.55608321329569));
#24657=CARTESIAN_POINT('Ctrl Pts',(-1.65998491543528,-3.58260030236365,
6.50311923480107));
#24658=CARTESIAN_POINT('Ctrl Pts',(-2.84480635537483,-3.0336175658618,6.45015525630644));
#24659=CARTESIAN_POINT('Ctrl Pts',(-3.73030587435696,-1.83863449854073,
6.39719127781182));
#24660=CARTESIAN_POINT('Ctrl Pts',(-3.91065206490815,-0.545321256873756,
6.3442272993172));
#24661=CARTESIAN_POINT('Ctrl Pts',(-3.93568069017971,-0.365833947574368,
6.33687690524133));
#24662=CARTESIAN_POINT('Ctrl Pts',(-3.94712794466584,-0.1844527827072,6.32952651116546));
#24663=CARTESIAN_POINT('Ctrl Pts',(-3.94563673384516,-0.00288256983268176,
6.3221761170896));
#24664=CARTESIAN_POINT('Ctrl Pts',(-3.94570073178844,-0.00286656758253237,
6.1778238829104));
#24665=CARTESIAN_POINT('Ctrl Pts',(-3.94716921739174,-0.182409496340425,
6.18509251567532));
#24666=CARTESIAN_POINT('Ctrl Pts',(-3.93597755777244,-0.361768304659314,
6.19236114844024));
#24667=CARTESIAN_POINT('Ctrl Pts',(-3.91150112201508,-0.539295483751872,
6.19962978120516));
#24668=CARTESIAN_POINT('Ctrl Pts',(-3.73306805394085,-1.83346754156567,
6.25261806993341));
#24669=CARTESIAN_POINT('Ctrl Pts',(-2.84862869021566,-3.03029947473994,
6.30560635866166));
#24670=CARTESIAN_POINT('Ctrl Pts',(-1.66386928259682,-3.58081270897423,
6.35859464738991));
#24671=CARTESIAN_POINT('Ctrl Pts',(-0.479109874977974,-4.13132594320853,
6.41158293611816));
#24672=CARTESIAN_POINT('Ctrl Pts',(1.00596957653452,-4.03552047850286,6.4645712248464));
#24673=CARTESIAN_POINT('Ctrl Pts',(2.11017334393921,-3.33734162243677,6.51755951357465));
#24674=CARTESIAN_POINT('Ctrl Pts',(3.21437711134392,-2.63916276637067,6.5705478023029));
#24675=CARTESIAN_POINT('Ctrl Pts',(3.9377051946408,-1.33861051894414,6.62353609103116));
#24676=CARTESIAN_POINT('Ctrl Pts',(3.94837197806129,-0.0322392490748367,
6.6765243797594));
#24677=CARTESIAN_POINT('Ctrl Pts',(3.95903876148178,1.27413202079445,6.72951266848765));
#24678=CARTESIAN_POINT('Ctrl Pts',(3.25704424502592,2.58632231310649,6.7825009572159));
#24679=CARTESIAN_POINT('Ctrl Pts',(2.16438848411372,3.30243896781703,6.83548924594415));
#24680=CARTESIAN_POINT('Ctrl Pts',(1.07173272320153,4.01855562252758,6.8884775346724));
#24681=CARTESIAN_POINT('Ctrl Pts',(-0.411584282167038,4.13859863963661,
6.94146582340065));
#24682=CARTESIAN_POINT('Ctrl Pts',(-1.60517522591216,3.60750511301625,6.9944541121289));
#24683=CARTESIAN_POINT('Ctrl Pts',(-2.7987661696573,3.07641158639588,7.04744240085715));
#24684=CARTESIAN_POINT('Ctrl Pts',(-3.70263105177901,1.89418151604613,7.1004306895854));
#24685=CARTESIAN_POINT('Ctrl Pts',(-3.9021732688668,0.603095702241273,7.15341897831364));
#24686=CARTESIAN_POINT('Ctrl Pts',(-3.9328077662116,0.404883186052253,7.16155394651256));
#24687=CARTESIAN_POINT('Ctrl Pts',(-3.94684167082104,0.204104985193814,
7.16968891471148));
#24688=CARTESIAN_POINT('Ctrl Pts',(-3.94511280640764,0.00308469250234145,
7.1778238829104));
#24689=CARTESIAN_POINT('Origin',(0.,0.,0.));
#24690=CARTESIAN_POINT('',(-3.93579878224384,0.00110209819909501,8.3221761170896));
#24691=CARTESIAN_POINT('',(-3.93583379497513,0.00119086740244391,8.17782388291041));
#24692=CARTESIAN_POINT('',(-3.942,-4.82755768223887E-16,0.));
#24693=CARTESIAN_POINT('Ctrl Pts',(-3.93579878224384,0.00110209819909501,
8.3221761170896));
#24694=CARTESIAN_POINT('Ctrl Pts',(-3.93727495532409,0.591480280077664,
8.29842758643428));
#24695=CARTESIAN_POINT('Ctrl Pts',(-3.81287497830763,1.18126751761344,8.27467905577897));
#24696=CARTESIAN_POINT('Ctrl Pts',(-3.55943403140727,1.70909456204991,8.25093052512365));
#24697=CARTESIAN_POINT('Ctrl Pts',(-2.9942099737124,2.88625455717395,8.19796654662903));
#24698=CARTESIAN_POINT('Ctrl Pts',(-1.78716283564177,3.75523737390689,8.1450025681344));
#24699=CARTESIAN_POINT('Ctrl Pts',(-0.491491832360601,3.91778133957111,
8.09203858963978));
#24700=CARTESIAN_POINT('Ctrl Pts',(0.804179170920576,4.08032530523533,8.03907461114515));
#24701=CARTESIAN_POINT('Ctrl Pts',(2.18847403941229,3.53643041983081,7.98611063265053));
#24702=CARTESIAN_POINT('Ctrl Pts',(3.02695952634759,2.53536799534552,7.93314665415591));
#24703=CARTESIAN_POINT('Ctrl Pts',(3.86544501328289,1.53430557086022,7.88018267566129));
#24704=CARTESIAN_POINT('Ctrl Pts',(4.15812111866178,0.0760756072941503,
7.82721869716666));
#24705=CARTESIAN_POINT('Ctrl Pts',(3.77085207703933,-1.17100361188895,7.77425471867203));
#24706=CARTESIAN_POINT('Ctrl Pts',(3.38358303541687,-2.41808283107204,7.72129074017741));
#24707=CARTESIAN_POINT('Ctrl Pts',(2.31636884679309,-3.45401130587216,7.66832676168279));
#24708=CARTESIAN_POINT('Ctrl Pts',(1.05832218368842,-3.8040148529523,7.61536278318817));
#24709=CARTESIAN_POINT('Ctrl Pts',(-0.199724479416271,-4.15401840003245,
7.56239880469355));
#24710=CARTESIAN_POINT('Ctrl Pts',(-1.64860361700185,-3.81809701939261,
7.50943482619892));
#24711=CARTESIAN_POINT('Ctrl Pts',(-2.62428250283791,-2.95020612691174,
7.45647084770429));
#24712=CARTESIAN_POINT('Ctrl Pts',(-3.44892179457277,-2.21666874973946,
7.41170593749939));
#24713=CARTESIAN_POINT('Ctrl Pts',(-3.93552800730583,-1.10311616471836,
7.36694102729449));
#24714=CARTESIAN_POINT('Ctrl Pts',(-3.94505905468816,0.00309284708018512,
7.32217611708959));
#24715=CARTESIAN_POINT('Ctrl Pts',(-3.94511280640764,0.00308469250234145,
7.1778238829104));
#24716=CARTESIAN_POINT('Ctrl Pts',(-3.93558046309789,-1.10526968584544,
7.22267720343973));
#24717=CARTESIAN_POINT('Ctrl Pts',(-3.44685564182305,-2.22098372195378,
7.26753052396906));
#24718=CARTESIAN_POINT('Ctrl Pts',(-2.61937124393104,-2.95458540793588,
7.31238384449839));
#24719=CARTESIAN_POINT('Ctrl Pts',(-1.64180744985364,-3.82123914704826,
7.36537213322664));
#24720=CARTESIAN_POINT('Ctrl Pts',(-0.191460309644946,-4.15460506801304,
7.41836042195489));
#24721=CARTESIAN_POINT('Ctrl Pts',(1.06640592095225,-3.80177051623037,7.47134871068314));
#24722=CARTESIAN_POINT('Ctrl Pts',(2.32427215154943,-3.44893596444769,7.52433699941139));
#24723=CARTESIAN_POINT('Ctrl Pts',(3.38965747253514,-2.40990093991759,7.57732528813964));
#24724=CARTESIAN_POINT('Ctrl Pts',(3.77387696635039,-1.16126366048821,7.63031357686789));
#24725=CARTESIAN_POINT('Ctrl Pts',(4.15809646016565,0.0873736189411645,
7.68330186559614));
#24726=CARTESIAN_POINT('Ctrl Pts',(3.86115012681045,1.5456131532698,7.73629015432439));
#24727=CARTESIAN_POINT('Ctrl Pts',(3.01924520659187,2.54457049986684,7.78927844305264));
#24728=CARTESIAN_POINT('Ctrl Pts',(2.17734028637328,3.54352784646387,7.84226673178089));
#24729=CARTESIAN_POINT('Ctrl Pts',(0.79047677929132,4.08320300532929,7.89525502050913));
#24730=CARTESIAN_POINT('Ctrl Pts',(-0.505200564699283,3.91605069371529,
7.94824330923738));
#24731=CARTESIAN_POINT('Ctrl Pts',(-1.80087790868988,3.74889838210129,8.00123159796563));
#24732=CARTESIAN_POINT('Ctrl Pts',(-3.00536908958914,2.87491860000785,8.05421988669388));
#24733=CARTESIAN_POINT('Ctrl Pts',(-3.56618228885602,1.69499986105314,8.10720817542213));
#24734=CARTESIAN_POINT('Ctrl Pts',(-3.81530790878367,1.17085387502675,8.13074674458489));
#24735=CARTESIAN_POINT('Ctrl Pts',(-3.93741444221381,0.586335951582262,
8.15428531374765));
#24736=CARTESIAN_POINT('Ctrl Pts',(-3.93583379497513,0.00119086740244391,
8.17782388291041));
#24737=CARTESIAN_POINT('Origin',(0.,0.,0.));
#24738=CARTESIAN_POINT('',(-3.94101045068862,-0.00360005201630542,9.3221761170896));
#24739=CARTESIAN_POINT('',(-3.94073510056759,-0.00358878591061127,9.1778238829104));
#24740=CARTESIAN_POINT('',(-3.942,-4.82755768223887E-16,0.));
#24741=CARTESIAN_POINT('Ctrl Pts',(-3.94101045068862,-0.00360005201630542,
9.3221761170896));
#24742=CARTESIAN_POINT('Ctrl Pts',(-3.93228175108165,0.970079126201241,
9.28287812406869));
#24743=CARTESIAN_POINT('Ctrl Pts',(-3.56768740150403,1.94959821666609,9.24358013104778));
#24744=CARTESIAN_POINT('Ctrl Pts',(-2.91383898553304,2.66460451331084,9.20428213802687));
#24745=CARTESIAN_POINT('Ctrl Pts',(-2.03261297931419,3.6282562219074,9.15131815953225));
#24746=CARTESIAN_POINT('Ctrl Pts',(-0.625975040492547,4.11143697314778,
9.09835418103763));
#24747=CARTESIAN_POINT('Ctrl Pts',(0.661401578964616,3.89270122117173,9.04539020254301));
#24748=CARTESIAN_POINT('Ctrl Pts',(1.9487781984218,3.67396546919568,8.99242622404838));
#24749=CARTESIAN_POINT('Ctrl Pts',(3.11689349851449,2.75331321400316,8.93946224555376));
#24750=CARTESIAN_POINT('Ctrl Pts',(3.63039103221387,1.55268663908397,8.88649826705913));
#24751=CARTESIAN_POINT('Ctrl Pts',(4.14388856591324,0.352060064164805,8.83353428856451));
#24752=CARTESIAN_POINT('Ctrl Pts',(4.00276833321932,-1.12854083048104,8.78057031006989));
#24753=CARTESIAN_POINT('Ctrl Pts',(3.2717068488331,-2.21054498738825,8.72760633157527));
#24754=CARTESIAN_POINT('Ctrl Pts',(2.54064536444688,-3.29254914429547,8.67464235308064));
#24755=CARTESIAN_POINT('Ctrl Pts',(1.21964262836836,-3.97595656346406,8.62167837458601));
#24756=CARTESIAN_POINT('Ctrl Pts',(-0.0858753956759256,-3.94755623929365,
8.56871439609139));
#24757=CARTESIAN_POINT('Ctrl Pts',(-1.39139341972021,-3.91915591512325,
8.51575041759677));
#24758=CARTESIAN_POINT('Ctrl Pts',(-2.68142673173026,-3.17894784761384,
8.46278643910214));
#24759=CARTESIAN_POINT('Ctrl Pts',(-3.36474289907574,-2.06617522710156,
8.40982246060752));
#24760=CARTESIAN_POINT('Ctrl Pts',(-3.74166677096472,-1.45235898112435,
8.38060701276821));
#24761=CARTESIAN_POINT('Ctrl Pts',(-3.93398279378317,-0.725181276064265,
8.35139156492891));
#24762=CARTESIAN_POINT('Ctrl Pts',(-3.93579878224384,0.00110209819909501,
8.3221761170896));
#24763=CARTESIAN_POINT('Ctrl Pts',(-3.93583379497513,0.00119086740244391,
8.17782388291041));
#24764=CARTESIAN_POINT('Ctrl Pts',(-3.93385620587065,-0.730899452746949,
8.2072736024759));
#24765=CARTESIAN_POINT('Ctrl Pts',(-3.73826901230947,-1.46397147804348,
8.23672332204139));
#24766=CARTESIAN_POINT('Ctrl Pts',(-3.35559744737338,-2.0810205230852,8.26617304160688));
#24767=CARTESIAN_POINT('Ctrl Pts',(-2.66706418898931,-3.19126447245286,
8.31916133033513));
#24768=CARTESIAN_POINT('Ctrl Pts',(-1.37286245458661,-3.92589467537216,
8.37214961906338));
#24769=CARTESIAN_POINT('Ctrl Pts',(-0.0666336764464662,-3.94794131155515,
8.42513790779163));
#24770=CARTESIAN_POINT('Ctrl Pts',(1.23959510169366,-3.96998794773813,8.47812619651988));
#24771=CARTESIAN_POINT('Ctrl Pts',(2.55785092357125,-3.27945101718484,8.53111448524812));
#24772=CARTESIAN_POINT('Ctrl Pts',(3.28345891245731,-2.19307505948273,8.58410277397638));
#24773=CARTESIAN_POINT('Ctrl Pts',(4.00906690134337,-1.10669910178063,8.63709106270462));
#24774=CARTESIAN_POINT('Ctrl Pts',(4.14202705723791,0.375515883070263,8.69007935143287));
#24775=CARTESIAN_POINT('Ctrl Pts',(3.62135147131388,1.57368807822049,8.74306764016112));
#24776=CARTESIAN_POINT('Ctrl Pts',(3.10067588538986,2.77186027337072,8.79605592888937));
#24777=CARTESIAN_POINT('Ctrl Pts',(1.92636455764724,3.68598967882027,8.84904421761762));
#24778=CARTESIAN_POINT('Ctrl Pts',(0.637066015602396,3.89677142492153,8.90203250634587));
#24779=CARTESIAN_POINT('Ctrl Pts',(-0.652232526442438,4.1075531710228,8.95502079507412));
#24780=CARTESIAN_POINT('Ctrl Pts',(-2.05651828278951,3.61498725777581,9.00800908380237));
#24781=CARTESIAN_POINT('Ctrl Pts',(-2.93165503760022,2.64501028104501,9.06099737253062));
#24782=CARTESIAN_POINT('Ctrl Pts',(-3.57481082178969,1.93215449058061,9.09993954265721));
#24783=CARTESIAN_POINT('Ctrl Pts',(-3.93216906200874,0.9614452240408,9.13888171278381));
#24784=CARTESIAN_POINT('Ctrl Pts',(-3.94073510056759,-0.00358878591061127,
9.1778238829104));
#24785=CARTESIAN_POINT('Origin',(0.,0.,0.));
#24786=CARTESIAN_POINT('',(-3.94826120782986,0.000860587304522282,10.3221761170896));
#24787=CARTESIAN_POINT('',(-3.94838239458768,0.000624922565347272,10.1778238829104));
#24788=CARTESIAN_POINT('',(-3.942,-4.82755768223887E-16,0.));
#24789=CARTESIAN_POINT('Ctrl Pts',(-3.94826120782986,0.000860587304522282,
10.3221761170896));
#24790=CARTESIAN_POINT('Ctrl Pts',(-3.94839882197096,0.0473049479418113,
10.3202926401977));
#24791=CARTESIAN_POINT('Ctrl Pts',(-3.94765033544244,0.0937447675908473,
10.3184091633059));
#24792=CARTESIAN_POINT('Ctrl Pts',(-3.94600203836796,0.140152628104641,
10.316525686414));
#24793=CARTESIAN_POINT('Ctrl Pts',(-3.89965139229318,1.4451566538172,10.2635617079194));
#24794=CARTESIAN_POINT('Ctrl Pts',(-3.14177325024928,2.72488891140618,10.2105977294247));
#24795=CARTESIAN_POINT('Ctrl Pts',(-2.0197091369755,3.39283802265691,10.1576337509301));
#24796=CARTESIAN_POINT('Ctrl Pts',(-0.897645023701731,4.06078713390763,
10.1046697724355));
#24797=CARTESIAN_POINT('Ctrl Pts',(0.588605060801912,4.11695309882012,10.0517057939409));
#24798=CARTESIAN_POINT('Ctrl Pts',(1.75788099084149,3.53559461307527,9.99874181544624));
#24799=CARTESIAN_POINT('Ctrl Pts',(2.92715692088108,2.95423612733042,9.94577783695161));
#24800=CARTESIAN_POINT('Ctrl Pts',(3.7794586964566,1.73535319092823,9.89281385845698));
#24801=CARTESIAN_POINT('Ctrl Pts',(3.92416969750304,0.437569458677891,9.83984987996236));
#24802=CARTESIAN_POINT('Ctrl Pts',(4.06888069854947,-0.860214273572448,
9.78688590146773));
#24803=CARTESIAN_POINT('Ctrl Pts',(3.50600092506682,-2.23689880167093,9.73392192297312));
#24804=CARTESIAN_POINT('Ctrl Pts',(2.49350261285418,-3.06153875782394,9.68095794447849));
#24805=CARTESIAN_POINT('Ctrl Pts',(1.48100430064151,-3.88617871397697,9.62799396598387));
#24806=CARTESIAN_POINT('Ctrl Pts',(0.0188874496988303,-4.15877409818449,
9.57502998748924));
#24807=CARTESIAN_POINT('Ctrl Pts',(-1.22274826539589,-3.75439229775474,
9.52206600899461));
#24808=CARTESIAN_POINT('Ctrl Pts',(-2.46438398049055,-3.350010497325,9.46910203049999));
#24809=CARTESIAN_POINT('Ctrl Pts',(-3.48553855973727,-2.26865151225807,
9.41613805200537));
#24810=CARTESIAN_POINT('Ctrl Pts',(-3.81820881255261,-1.00591068674825,
9.36317407351075));
#24811=CARTESIAN_POINT('Ctrl Pts',(-3.90404577140141,-0.680093059958056,
9.34950808803704));
#24812=CARTESIAN_POINT('Ctrl Pts',(-3.94404588005443,-0.342199672065631,
9.33584210256332));
#24813=CARTESIAN_POINT('Ctrl Pts',(-3.94101045068862,-0.00360005201630542,
9.3221761170896));
#24814=CARTESIAN_POINT('Ctrl Pts',(-3.94073510056759,-0.00358878591061127,
9.1778238829104));
#24815=CARTESIAN_POINT('Ctrl Pts',(-3.94382479981015,-0.351668569711599,
9.19187000151206));
#24816=CARTESIAN_POINT('Ctrl Pts',(-3.90153714912137,-0.6990100110183,9.20591612011371));
#24817=CARTESIAN_POINT('Ctrl Pts',(-3.81091609517323,-1.03324690266663,
9.21996223871536));
#24818=CARTESIAN_POINT('Ctrl Pts',(-3.46905264466117,-2.29413906943288,
9.27295052744361));
#24819=CARTESIAN_POINT('Ctrl Pts',(-2.4393379903627,-3.36853536275074,9.32593881617186));
#24820=CARTESIAN_POINT('Ctrl Pts',(-1.194095160419,-3.76361759404226,9.37892710490011));
#24821=CARTESIAN_POINT('Ctrl Pts',(0.0511476695246889,-4.15869982533377,
9.43191539362836));
#24822=CARTESIAN_POINT('Ctrl Pts',(1.5119186751136,-3.87446799459896,9.48490368235661));
#24823=CARTESIAN_POINT('Ctrl Pts',(2.5181722452647,-3.04129728726066,9.53789197108486));
#24824=CARTESIAN_POINT('Ctrl Pts',(3.5244258154158,-2.20812657992236,9.59088025981311));
#24825=CARTESIAN_POINT('Ctrl Pts',(4.07616195012909,-0.826016995980571,
9.64386854854136));
#24826=CARTESIAN_POINT('Ctrl Pts',(3.92030308000722,0.471067306450377,9.69685683726961));
#24827=CARTESIAN_POINT('Ctrl Pts',(3.76444420988535,1.76815160888132,9.74984512599786));
#24828=CARTESIAN_POINT('Ctrl Pts',(2.90099033492832,2.98021062980143,9.8028334147261));
#24829=CARTESIAN_POINT('Ctrl Pts',(1.72600180756239,3.55128123451409,9.85582170345435));
#24830=CARTESIAN_POINT('Ctrl Pts',(0.551013280196442,4.12235183922675,9.90880999218261));
#24831=CARTESIAN_POINT('Ctrl Pts',(-0.935509899578419,4.05243402773195,
9.96179828091086));
#24832=CARTESIAN_POINT('Ctrl Pts',(-2.05170977553871,3.37359861917203,10.0147865696391));
#24833=CARTESIAN_POINT('Ctrl Pts',(-3.16790965149901,2.69476321061211,10.0677748583674));
#24834=CARTESIAN_POINT('Ctrl Pts',(-3.91378622364473,1.40701020498706,10.1207631470956));
#24835=CARTESIAN_POINT('Ctrl Pts',(-3.94721103949169,0.101023047050935,
10.1737514358238));
#24836=CARTESIAN_POINT('Ctrl Pts',(-3.94806733432703,0.0675655685271688,
10.175108918186));
#24837=CARTESIAN_POINT('Ctrl Pts',(-3.94845604040098,0.0340961227584357,
10.1764664005482));
#24838=CARTESIAN_POINT('Ctrl Pts',(-3.94838239458768,0.000624922565347272,
10.1778238829104));
#24839=CARTESIAN_POINT('Origin',(0.,0.,0.));
#24840=CARTESIAN_POINT('',(-3.93845364011251,0.00310220437029302,11.3221761170896));
#24841=CARTESIAN_POINT('',(-3.93886953396072,0.00324640498314072,11.1778238829104));
#24842=CARTESIAN_POINT('',(-3.942,-4.82755768223887E-16,0.));
#24843=CARTESIAN_POINT('Ctrl Pts',(-3.93845364011251,0.00310220437029302,
11.3221761170896));
#24844=CARTESIAN_POINT('Ctrl Pts',(-3.94163276156383,0.435745363096063,
11.3047431778321));
#24845=CARTESIAN_POINT('Ctrl Pts',(-3.87593103620607,0.867449899692147,
11.2873102385747));
#24846=CARTESIAN_POINT('Ctrl Pts',(-3.73722250128773,1.27426167714383,11.2698772993172));
#24847=CARTESIAN_POINT('Ctrl Pts',(-3.31580441728399,2.51021907446466,11.2169133208226));
#24848=CARTESIAN_POINT('Ctrl Pts',(-2.2205051385,3.51640664107286,11.163949342328));
#24849=CARTESIAN_POINT('Ctrl Pts',(-0.953308955593125,3.83168068622044,
11.1109853638333));
#24850=CARTESIAN_POINT('Ctrl Pts',(0.313887227313751,4.14695473136801,11.0580213853387));
#24851=CARTESIAN_POINT('Ctrl Pts',(1.75298031434354,3.77131525505496,11.0050574068441));
#24852=CARTESIAN_POINT('Ctrl Pts',(2.70442260335169,2.87692078939432,10.9520934283495));
#24853=CARTESIAN_POINT('Ctrl Pts',(3.65586489235987,1.98252632373365,10.8991294498548));
#24854=CARTESIAN_POINT('Ctrl Pts',(4.11965638334642,0.569376868725343,10.8461654713602));
#24855=CARTESIAN_POINT('Ctrl Pts',(3.88323778121684,-0.714870044482812,
10.7932014928656));
#24856=CARTESIAN_POINT('Ctrl Pts',(3.64681917908728,-1.99911695769091,10.740237514371));
#24857=CARTESIAN_POINT('Ctrl Pts',(2.71019048384171,-3.15446132909884,10.6872735358763));
#24858=CARTESIAN_POINT('Ctrl Pts',(1.5026160073439,-3.65139972893172,10.6343095573817));
#24859=CARTESIAN_POINT('Ctrl Pts',(0.295041530846062,-4.14833812876461,
10.5813455788871));
#24860=CARTESIAN_POINT('Ctrl Pts',(-1.18347872690403,-3.98687055702237,
10.5283816003925));
#24861=CARTESIAN_POINT('Ctrl Pts',(-2.25532728072623,-3.24099887423319,
10.4754176218978));
#24862=CARTESIAN_POINT('Ctrl Pts',(-3.28905932517556,-2.52165148434584,
10.4243371202951));
#24863=CARTESIAN_POINT('Ctrl Pts',(-3.94452906787893,-1.25872547303165,
10.3732566186924));
#24864=CARTESIAN_POINT('Ctrl Pts',(-3.94826120782986,0.000860587304522282,
10.3221761170896));
#24865=CARTESIAN_POINT('Ctrl Pts',(-3.94838239458768,0.000624922565347272,
10.1778238829104));
#24866=CARTESIAN_POINT('Ctrl Pts',(-3.94558133224467,-1.27242665007483,
10.2294546892765));
#24867=CARTESIAN_POINT('Ctrl Pts',(-3.27394054517676,-2.548016178621,10.2810854956425));
#24868=CARTESIAN_POINT('Ctrl Pts',(-2.22159520444575,-3.26422967848529,
10.3327163020086));
#24869=CARTESIAN_POINT('Ctrl Pts',(-1.14158149400459,-3.99927393583826,
10.3857045907369));
#24870=CARTESIAN_POINT('Ctrl Pts',(0.339418986425944,-4.14514114029698,
10.4386928794651));
#24871=CARTESIAN_POINT('Ctrl Pts',(1.54208150481898,-3.63492300865035,10.4916811681933));
#24872=CARTESIAN_POINT('Ctrl Pts',(2.744744023212,-3.12470487700374,10.5446694569216));
#24873=CARTESIAN_POINT('Ctrl Pts',(3.66906857956751,-1.95840140925179,10.5976577456498));
#24874=CARTESIAN_POINT('Ctrl Pts',(3.89107385865357,-0.670987982622134,
10.6506460343781));
#24875=CARTESIAN_POINT('Ctrl Pts',(4.11307913773965,0.616425444007545,10.7036343231063));
#24876=CARTESIAN_POINT('Ctrl Pts',(3.63276513955622,2.02494882951498,10.7566226118346));
#24877=CARTESIAN_POINT('Ctrl Pts',(2.67044859081355,2.90850218671784,10.8096109005628));
#24878=CARTESIAN_POINT('Ctrl Pts',(1.70813204207087,3.79205554392072,10.8625991892911));
#24879=CARTESIAN_POINT('Ctrl Pts',(0.263812942768934,4.15063887281905,10.9155874780193));
#24880=CARTESIAN_POINT('Ctrl Pts',(-1.00000947224434,3.81977246727369,10.9685757667476));
#24881=CARTESIAN_POINT('Ctrl Pts',(-2.2638318872576,3.48890606172833,11.0215640554758));
#24882=CARTESIAN_POINT('Ctrl Pts',(-3.34715761798219,2.46858992173929,11.0745523442041));
#24883=CARTESIAN_POINT('Ctrl Pts',(-3.75307260433058,1.22683604158983,11.1275406329323));
#24884=CARTESIAN_POINT('Ctrl Pts',(-3.88147031395203,0.834048488809281,
11.1443017162584));
#24885=CARTESIAN_POINT('Ctrl Pts',(-3.94208881978707,0.419104697969423,
11.1610627995844));
#24886=CARTESIAN_POINT('Ctrl Pts',(-3.93886953396072,0.00324640498314072,
11.1778238829104));
#24887=CARTESIAN_POINT('Origin',(0.,0.,0.));
#24888=CARTESIAN_POINT('',(-3.93708098219134,-0.00243404615490106,12.3221761170896));
#24889=CARTESIAN_POINT('',(-3.93670434321626,-0.00217448122624482,12.1778238829104));
#24890=CARTESIAN_POINT('',(-3.942,-4.82755768223887E-16,0.));
#24891=CARTESIAN_POINT('Ctrl Pts',(-3.93708098219134,-0.00243404615490106,
12.3221761170896));
#24892=CARTESIAN_POINT('Ctrl Pts',(-3.93246581499902,0.816826384091263,
12.2891937154665));
#24893=CARTESIAN_POINT('Ctrl Pts',(-3.68329161894405,1.63865836153011,12.2562113138435));
#24894=CARTESIAN_POINT('Ctrl Pts',(-3.20967797357049,2.29968305467193,12.2232289122204));
#24895=CARTESIAN_POINT('Ctrl Pts',(-2.4491371489512,3.36117330126154,12.1702649337258));
#24896=CARTESIAN_POINT('Ctrl Pts',(-1.10983987433617,4.00799378602558,12.1173009552312));
#24897=CARTESIAN_POINT('Ctrl Pts',(0.194403355371928,3.94370158371407,12.0643369767366));
#24898=CARTESIAN_POINT('Ctrl Pts',(1.49864658508003,3.87940938140256,12.0113729982419));
#24899=CARTESIAN_POINT('Ctrl Pts',(2.7678357698812,3.1040044920155,11.9584090197473));
#24900=CARTESIAN_POINT('Ctrl Pts',(3.42029150490108,1.97286108671397,11.9054450412527));
#24901=CARTESIAN_POINT('Ctrl Pts',(4.07274723992097,0.841717681412442,11.8524810627581));
#24902=CARTESIAN_POINT('Ctrl Pts',(4.10846952515958,-0.645164239803552,
11.7995170842634));
#24903=CARTESIAN_POINT('Ctrl Pts',(3.51108655579286,-1.8063349754958,11.7465531057688));
#24904=CARTESIAN_POINT('Ctrl Pts',(2.91370358642613,-2.96750571118807,11.6935891272742));
#24905=CARTESIAN_POINT('Ctrl Pts',(1.68321536245406,-3.80296526135658,11.6406251487796));
#24906=CARTESIAN_POINT('Ctrl Pts',(0.383564333431266,-3.92981593056064,
11.5876611702849));
#24907=CARTESIAN_POINT('Ctrl Pts',(-0.91608669559151,-4.0566665997647,11.5346971917903));
#24908=CARTESIAN_POINT('Ctrl Pts',(-2.28490052966501,-3.47490838800432,
11.4817332132957));
#24909=CARTESIAN_POINT('Ctrl Pts',(-3.09553900209,-2.4511656681074,11.4287692348011));
#24910=CARTESIAN_POINT('Ctrl Pts',(-3.6393581823996,-1.76438488268918,11.3932381955639));
#24911=CARTESIAN_POINT('Ctrl Pts',(-3.93197409656805,-0.878691784660489,
11.3577071563268));
#24912=CARTESIAN_POINT('Ctrl Pts',(-3.93845364011251,0.00310220437029302,
11.3221761170896));
#24913=CARTESIAN_POINT('Ctrl Pts',(-3.93886953396072,0.00324640498314072,
11.1778238829104));
#24914=CARTESIAN_POINT('Ctrl Pts',(-3.9319114080084,-0.895584744841287,
11.2140510883126));
#24915=CARTESIAN_POINT('Ctrl Pts',(-3.62672875965172,-1.79868808138705,
11.2502782937149));
#24916=CARTESIAN_POINT('Ctrl Pts',(-3.06311856673542,-2.49158288893653,
11.2865054991171));
#24917=CARTESIAN_POINT('Ctrl Pts',(-2.23874530081967,-3.50505631900356,
11.3394937878453));
#24918=CARTESIAN_POINT('Ctrl Pts',(-0.861494527015975,-4.06881155882777,
11.3924820765736));
#24919=CARTESIAN_POINT('Ctrl Pts',(0.436898299346125,-3.92425795818127,
11.4454703653018));
#24920=CARTESIAN_POINT('Ctrl Pts',(1.73529112570822,-3.77970435753476,11.4984586540301));
#24921=CARTESIAN_POINT('Ctrl Pts',(2.95482600462875,-2.92684191641753,11.5514469427583));
#24922=CARTESIAN_POINT('Ctrl Pts',(3.53611067677546,-1.75687276941591,11.6044352314866));
#24923=CARTESIAN_POINT('Ctrl Pts',(4.11739534892219,-0.586903622414244,
11.6574235202148));
#24924=CARTESIAN_POINT('Ctrl Pts',(4.06042981429509,0.900172230471804,11.7104118089431));
#24925=CARTESIAN_POINT('Ctrl Pts',(3.39134377174076,2.02224332566476,11.7634000976713));
#24926=CARTESIAN_POINT('Ctrl Pts',(2.72225772918646,3.14431442085768,11.8163883863996));
#24927=CARTESIAN_POINT('Ctrl Pts',(1.44105117870494,3.90138075835749,11.8693766751278));
#24928=CARTESIAN_POINT('Ctrl Pts',(0.135404751111381,3.94618121729058,11.9223649638561));
#24929=CARTESIAN_POINT('Ctrl Pts',(-1.17024167648218,3.99098167622367,11.9753532525843));
#24930=CARTESIAN_POINT('Ctrl Pts',(-2.50032798118779,3.32351625659005,12.0283415413126));
#24931=CARTESIAN_POINT('Ctrl Pts',(-3.24475272518949,2.24994675463574,12.0813298300408));
#24932=CARTESIAN_POINT('Ctrl Pts',(-3.69662968598688,1.59827399972424,12.1134945143307));
#24933=CARTESIAN_POINT('Ctrl Pts',(-3.93270958942814,0.796965223217272,
12.1456591986205));
#24934=CARTESIAN_POINT('Ctrl Pts',(-3.93670434321626,-0.00217448122624482,
12.1778238829104));
#24935=CARTESIAN_POINT('Origin',(0.,0.,0.));
#24936=CARTESIAN_POINT('',(-3.94733077553239,-0.00192598462593618,13.3221761170896));
#24937=CARTESIAN_POINT('',(-3.94682996399265,-0.00229165249276323,13.1778238829104));
#24938=CARTESIAN_POINT('',(-3.942,-4.82755768223887E-16,0.));
#24939=CARTESIAN_POINT('Ctrl Pts',(-3.94733077553239,-0.00192598462593618,
13.3221761170896));
#24940=CARTESIAN_POINT('Ctrl Pts',(-3.94013816129704,1.1955636687552,13.273644253101));
#24941=CARTESIAN_POINT('Ctrl Pts',(-3.356565432248,2.39912123530496,13.2251123891123));
#24942=CARTESIAN_POINT('Ctrl Pts',(-2.40836516771617,3.12895382914166,13.1765805251237));
#24943=CARTESIAN_POINT('Ctrl Pts',(-1.37357164668001,3.92543751280327,13.123616546629));
#24944=CARTESIAN_POINT('Ctrl Pts',(0.0954887653771007,4.15772060523228,
13.0706525681344));
#24945=CARTESIAN_POINT('Ctrl Pts',(1.32553410510171,3.71934593472844,13.0176885896398));
#24946=CARTESIAN_POINT('Ctrl Pts',(2.55557944482628,3.28097126422461,12.9647246111452));
#24947=CARTESIAN_POINT('Ctrl Pts',(3.54660971221836,2.17193883078797,12.9117606326505));
#24948=CARTESIAN_POINT('Ctrl Pts',(3.84442792620346,0.900526938073336,12.8587966541559));
#24949=CARTESIAN_POINT('Ctrl Pts',(4.14224614018855,-0.370884954641299,
12.8058326756613));
#24950=CARTESIAN_POINT('Ctrl Pts',(3.74685230076666,-1.80467630663392,12.7528686971667));
#24951=CARTESIAN_POINT('Ctrl Pts',(2.83945852033214,-2.74372924270635,12.699904718672));
#24952=CARTESIAN_POINT('Ctrl Pts',(1.93206473989763,-3.68278217877878,12.6469407401774));
#24953=CARTESIAN_POINT('Ctrl Pts',(0.512671018450501,-4.127096698931,12.5939767616828));
#24954=CARTESIAN_POINT('Ctrl Pts',(-0.768203316346435,-3.8730399572846,
12.5410127831882));
#24955=CARTESIAN_POINT('Ctrl Pts',(-2.04907765114337,-3.6189832156382,12.4880488046935));
#24956=CARTESIAN_POINT('Ctrl Pts',(-3.19143259929011,-2.66655521219318,
12.4350848261989));
#24957=CARTESIAN_POINT('Ctrl Pts',(-3.67171788605172,-1.45226120626306,
12.3821208477043));
#24958=CARTESIAN_POINT('Ctrl Pts',(-3.85291381676684,-0.994147791942479,
12.3621392708327));
#24959=CARTESIAN_POINT('Ctrl Pts',(-3.93987696773182,-0.498762829361246,
12.3421576939612));
#24960=CARTESIAN_POINT('Ctrl Pts',(-3.93708098219134,-0.00243404615490106,
12.3221761170896));
#24961=CARTESIAN_POINT('Ctrl Pts',(-3.93670434321626,-0.00217448122624482,
12.1778238829104));
#24962=CARTESIAN_POINT('Ctrl Pts',(-3.93929057014649,-0.519542192545187,
12.1986474873488));
#24963=CARTESIAN_POINT('Ctrl Pts',(-3.84460194542603,-1.03600077131728,
12.2194710917872));
#24964=CARTESIAN_POINT('Ctrl Pts',(-3.64821869509448,-1.51035790430073,
12.2402946962256));
#24965=CARTESIAN_POINT('Ctrl Pts',(-3.14849673769996,-2.71741947700787,
12.2932829849538));
#24966=CARTESIAN_POINT('Ctrl Pts',(-1.99028963961311,-3.65186903814713,
12.3462712736821));
#24967=CARTESIAN_POINT('Ctrl Pts',(-0.704859028994106,-3.8850810024459,
12.3992595624103));
#24968=CARTESIAN_POINT('Ctrl Pts',(0.580571581624919,-4.11829296674466,
12.4522478511386));
#24969=CARTESIAN_POINT('Ctrl Pts',(1.99322570477611,-3.6502673342029,12.5052361398668));
#24970=CARTESIAN_POINT('Ctrl Pts',(2.88512861233689,-2.6956842427472,12.5582244285951));
#24971=CARTESIAN_POINT('Ctrl Pts',(3.77703151989765,-1.74110115129151,12.6112127173233));
#24972=CARTESIAN_POINT('Ctrl Pts',(4.148183211868,-0.299960600921891,12.6642010060516));
#24973=CARTESIAN_POINT('Ctrl Pts',(3.82833896043004,0.966696152042594,12.7171892947798));
#24974=CARTESIAN_POINT('Ctrl Pts',(3.50849470899208,2.23335290500708,12.7701775835081));
#24975=CARTESIAN_POINT('Ctrl Pts',(2.4976545141458,3.32552586056643,12.8231658722363));
#24976=CARTESIAN_POINT('Ctrl Pts',(1.259483819326,3.74224279746471,12.8761541609646));
#24977=CARTESIAN_POINT('Ctrl Pts',(0.0213131245061955,4.158959734363,12.9291424496928));
#24978=CARTESIAN_POINT('Ctrl Pts',(-1.44418807028713,3.90022065260022,12.9821307384211));
#24979=CARTESIAN_POINT('Ctrl Pts',(-2.46480444872359,3.08470738901973,13.0351190271493));
#24980=CARTESIAN_POINT('Ctrl Pts',(-3.38102522484729,2.35261038265819,13.082687312403));
#24981=CARTESIAN_POINT('Ctrl Pts',(-3.93871824071251,1.17181521210322,13.1302555976567));
#24982=CARTESIAN_POINT('Ctrl Pts',(-3.94682996399265,-0.00229165249276323,
13.1778238829104));
#24983=CARTESIAN_POINT('Origin',(0.,0.,0.));
#24984=CARTESIAN_POINT('',(-3.9429197498326,0.0035503728418125,14.3221761170896));
#24985=CARTESIAN_POINT('',(-3.94377660893062,0.00343048778150908,14.1778238829104));
#24986=CARTESIAN_POINT('',(-3.942,-4.82755768223887E-16,0.));
#24987=CARTESIAN_POINT('Ctrl Pts',(-3.9429197498326,0.0035503728418125,
14.3221761170896));
#24988=CARTESIAN_POINT('Ctrl Pts',(-3.94546599449794,0.278662013094457,
14.31105876923));
#24989=CARTESIAN_POINT('Ctrl Pts',(-3.91912941936741,0.553289499978031,
14.2999414213704));
#24990=CARTESIAN_POINT('Ctrl Pts',(-3.86210967795079,0.821391308358944,
14.2888240735108));
#24991=CARTESIAN_POINT('Ctrl Pts',(-3.59046284308573,2.09865083039248,14.2358600950161));
#24992=CARTESIAN_POINT('Ctrl Pts',(-2.62241565120338,3.22780031721448,14.1828961165215));
#24993=CARTESIAN_POINT('Ctrl Pts',(-1.40163175876062,3.69134166107696,14.1299321380269));
#24994=CARTESIAN_POINT('Ctrl Pts',(-0.18084786631787,4.15488300493943,14.0769681595322));
#24995=CARTESIAN_POINT('Ctrl Pts',(1.29267272668526,3.95281620584241,14.0240041810376));
#24996=CARTESIAN_POINT('Ctrl Pts',(2.34360392082064,3.17775007014128,13.971040202543));
#24997=CARTESIAN_POINT('Ctrl Pts',(3.39453511495603,2.40268393444014,13.9180762240484));
#24998=CARTESIAN_POINT('Ctrl Pts',(4.02287691022366,1.05461846213484,13.8651122455537));
#24999=CARTESIAN_POINT('Ctrl Pts',(3.9406553103857,-0.24861731777516,13.8121482670591));
#25000=CARTESIAN_POINT('Ctrl Pts',(3.85843371054775,-1.55185309768514,13.7591842885645));
#25001=CARTESIAN_POINT('Ctrl Pts',(3.06564871560427,-2.81025918519985,13.7062203100699));
#25002=CARTESIAN_POINT('Ctrl Pts',(1.92563993605177,-3.44709815390442,13.6532563315753));
#25003=CARTESIAN_POINT('Ctrl Pts',(0.7856311564993,-4.08393712260898,13.6002923530807));
#25004=CARTESIAN_POINT('Ctrl Pts',(-0.701601407662154,-4.09920897250343,
13.547328374586));
#25005=CARTESIAN_POINT('Ctrl Pts',(-1.85444735256939,-3.48591449443573,
13.4943643960914));
#25006=CARTESIAN_POINT('Ctrl Pts',(-3.00729329747666,-2.87262001636802,
13.4414004175968));
#25007=CARTESIAN_POINT('Ctrl Pts',(-3.82575262312968,-1.63075921033812,
13.3884364391021));
#25008=CARTESIAN_POINT('Ctrl Pts',(-3.93471897094859,-0.329486669876098,
13.3354724606075));
#25009=CARTESIAN_POINT('Ctrl Pts',(-3.94383745759853,-0.22059400231727,
13.3310403461016));
#25010=CARTESIAN_POINT('Ctrl Pts',(-3.94798763243564,-0.111285296783124,
13.3266082315956));
#25011=CARTESIAN_POINT('Ctrl Pts',(-3.94733077553239,-0.00192598462593618,
13.3221761170896));
#25012=CARTESIAN_POINT('Ctrl Pts',(-3.94682996399265,-0.00229165249276323,
13.1778238829104));
#25013=CARTESIAN_POINT('Ctrl Pts',(-3.94775422620073,-0.13607119177326,
13.183243886385));
#25014=CARTESIAN_POINT('Ctrl Pts',(-3.94154345388817,-0.269763898960769,
13.1886638898595));
#25015=CARTESIAN_POINT('Ctrl Pts',(-3.92791502810543,-0.402696136440426,
13.1940838933341));
#25016=CARTESIAN_POINT('Ctrl Pts',(-3.79467766697122,-1.70229895292184,
13.2470721820623));
#25017=CARTESIAN_POINT('Ctrl Pts',(-2.95247138262324,-2.92921714048647,
13.3000604707906));
#25018=CARTESIAN_POINT('Ctrl Pts',(-1.78761040384536,-3.52067176691954,
13.3530487595188));
#25019=CARTESIAN_POINT('Ctrl Pts',(-0.622749425067479,-4.1121263933526,
13.4060370482471));
#25020=CARTESIAN_POINT('Ctrl Pts',(0.864766248140306,-4.0681174586541,13.4590253369753));
#25021=CARTESIAN_POINT('Ctrl Pts',(1.99262340964458,-3.4088315584166,13.5120136257036));
#25022=CARTESIAN_POINT('Ctrl Pts',(3.12048057114885,-2.7495456581791,13.5650019144318));
#25023=CARTESIAN_POINT('Ctrl Pts',(3.8886792209496,-1.4749827924026,13.6179902031601));
#25024=CARTESIAN_POINT('Ctrl Pts',(3.94485192310407,-0.169776179432411,
13.6709784918883));
#25025=CARTESIAN_POINT('Ctrl Pts',(4.00102462525853,1.13543043353777,13.7239667806165));
#25026=CARTESIAN_POINT('Ctrl Pts',(3.34517137976671,2.47128079370165,13.7769550693448));
#25027=CARTESIAN_POINT('Ctrl Pts',(2.27812755848019,3.2250295306576,13.829943358073));
#25028=CARTESIAN_POINT('Ctrl Pts',(1.21108373719365,3.97877826761357,13.8829316468013));
#25029=CARTESIAN_POINT('Ctrl Pts',(-0.267150659887593,4.15042538136161,
13.9359199355295));
#25030=CARTESIAN_POINT('Ctrl Pts',(-1.47851968414005,3.66123752164906,13.9889082242578));
#25031=CARTESIAN_POINT('Ctrl Pts',(-2.68988870839249,3.17204966193652,14.041896512986));
#25032=CARTESIAN_POINT('Ctrl Pts',(-3.63439235981614,2.02202682876341,14.0948848017143));
#25033=CARTESIAN_POINT('Ctrl Pts',(-3.87879331109071,0.738676584276535,
14.1478730904425));
#25034=CARTESIAN_POINT('Ctrl Pts',(-3.92484123568096,0.496878772227051,
14.1578566879318));
#25035=CARTESIAN_POINT('Ctrl Pts',(-3.9460363164428,0.250347989813759,14.1678402854211));
#25036=CARTESIAN_POINT('Ctrl Pts',(-3.94377660893062,0.00343048778150908,
14.1778238829104));
#25037=CARTESIAN_POINT('Origin',(0.,0.,0.));
#25038=CARTESIAN_POINT('',(-3.935515150562,-7.56757525427476E-5,15.3221761170896));
#25039=CARTESIAN_POINT('',(-3.93554762371472,0.000453016733568931,15.1778238829104));
#25040=CARTESIAN_POINT('',(-3.942,-4.82755768223887E-16,0.));
#25041=CARTESIAN_POINT('Ctrl Pts',(-3.935515150562,-7.56757525427476E-5,
15.3221761170896));
#25042=CARTESIAN_POINT('Ctrl Pts',(-3.93540179088204,0.662968867054025,
15.2955093068644));
#25043=CARTESIAN_POINT('Ctrl Pts',(-3.77682343808938,1.32606434282809,15.2688424966392));
#25044=CARTESIAN_POINT('Ctrl Pts',(-3.46008318945363,1.90220902322252,15.242175686414));
#25045=CARTESIAN_POINT('Ctrl Pts',(-2.83099318673311,3.04651215526165,15.1892117079193));
#25046=CARTESIAN_POINT('Ctrl Pts',(-1.57799465489921,3.84781647231203,15.1362477294247));
#25047=CARTESIAN_POINT('Ctrl Pts',(-0.275346694985541,3.93887789142153,
15.0832837509301));
#25048=CARTESIAN_POINT('Ctrl Pts',(1.02730126492813,4.02993931053103,15.0303197724355));
#25049=CARTESIAN_POINT('Ctrl Pts',(2.37959865292158,3.41075783169958,14.9773557939409));
#25050=CARTESIAN_POINT('Ctrl Pts',(3.16177691968707,2.36510920595707,14.9243918154462));
#25051=CARTESIAN_POINT('Ctrl Pts',(3.94395518645256,1.31946058021456,14.8714278369516));
#25052=CARTESIAN_POINT('Ctrl Pts',(4.15601433199016,-0.152655192438981,
14.818463858457));
#25053=CARTESIAN_POINT('Ctrl Pts',(3.70076597882895,-1.37655585281198,14.7654998799624));
#25054=CARTESIAN_POINT('Ctrl Pts',(3.24551762566774,-2.60045651318499,14.7125359014677));
#25055=CARTESIAN_POINT('Ctrl Pts',(2.1229617738077,-3.57614206127742,14.6595719229731));
#25056=CARTESIAN_POINT('Ctrl Pts',(0.847574616134508,-3.85644812178943,
14.6066079444785));
#25057=CARTESIAN_POINT('Ctrl Pts',(-0.427812541538684,-4.13675418230144,
14.5536439659839));
#25058=CARTESIAN_POINT('Ctrl Pts',(-1.85603100502504,-3.72168075523303,
14.5006799874892));
#25059=CARTESIAN_POINT('Ctrl Pts',(-2.78251699784433,-2.80145926307632,
14.4477160089946));
#25060=CARTESIAN_POINT('Ctrl Pts',(-3.5145299287451,-2.07439588945562,14.4058693783596));
#25061=CARTESIAN_POINT('Ctrl Pts',(-3.93333547115731,-1.0319929364451,14.3640227477246));
#25062=CARTESIAN_POINT('Ctrl Pts',(-3.9429197498326,0.0035503728418125,
14.3221761170896));
#25063=CARTESIAN_POINT('Ctrl Pts',(-3.94377660893062,0.00343048778150908,
14.1778238829104));
#25064=CARTESIAN_POINT('Ctrl Pts',(-3.93404284072175,-1.06017518620376,
14.2208285741494));
#25065=CARTESIAN_POINT('Ctrl Pts',(-3.48910890040614,-2.13095638625906,
14.2638332653883));
#25066=CARTESIAN_POINT('Ctrl Pts',(-2.72071532173612,-2.86153608825589,
14.3068379566273));
#25067=CARTESIAN_POINT('Ctrl Pts',(-1.77393812998146,-3.7617208605008,14.3598262453555));
#25068=CARTESIAN_POINT('Ctrl Pts',(-0.336085495346666,-4.14541274918995,
14.4128145340838));
#25069=CARTESIAN_POINT('Ctrl Pts',(0.933309470178012,-3.83661492453915,
14.465802822812));
#25070=CARTESIAN_POINT('Ctrl Pts',(2.20270443570267,-3.52781709988836,14.5187911115403));
#25071=CARTESIAN_POINT('Ctrl Pts',(3.30364173211722,-2.5265295618976,14.5717794002685));
#25072=CARTESIAN_POINT('Ctrl Pts',(3.73112899530853,-1.29203601601831,14.6247676889968));
#25073=CARTESIAN_POINT('Ctrl Pts',(4.15861625849985,-0.0575424701390118,
14.677755977725));
#25074=CARTESIAN_POINT('Ctrl Pts',(3.91265348846795,1.41015708362883,14.7307442664533));
#25075=CARTESIAN_POINT('Ctrl Pts',(3.10606211575817,2.43783895681654,14.7837325551815));
#25076=CARTESIAN_POINT('Ctrl Pts',(2.29947074304839,3.46552083000428,14.8367208439098));
#25077=CARTESIAN_POINT('Ctrl Pts',(0.932250767660721,4.05318502261185,14.889709132638));
#25078=CARTESIAN_POINT('Ctrl Pts',(-0.368463413303181,3.93127401224813,
14.9426974213663));
#25079=CARTESIAN_POINT('Ctrl Pts',(-1.66917759426705,3.80936300188441,14.9956857100945));
#25080=CARTESIAN_POINT('Ctrl Pts',(-2.90338598080718,2.9778767885494,15.0486739988228));
#25081=CARTESIAN_POINT('Ctrl Pts',(-3.50496567659063,1.81821237820066,15.101662287551));
#25082=CARTESIAN_POINT('Ctrl Pts',(-3.79318829122445,1.26260601250841,15.1270494860042));
#25083=CARTESIAN_POINT('Ctrl Pts',(-3.93619350756073,0.631667647738924,
15.1524366844573));
#25084=CARTESIAN_POINT('Ctrl Pts',(-3.93554762371472,0.000453016733568931,
15.1778238829104));
#25085=CARTESIAN_POINT('Origin',(0.,0.,0.));
#25086=CARTESIAN_POINT('',(-3.94319808732824,-0.00351593218956836,16.3221761170896));
#25087=CARTESIAN_POINT('',(-3.94210945089404,-0.00361990150021516,16.1778238829104));
#25088=CARTESIAN_POINT('',(-3.942,-4.82755768223887E-16,0.));
#25089=CARTESIAN_POINT('Ctrl Pts',(-3.94319808732824,-0.00351593218956836,
16.3221761170896));
#25090=CARTESIAN_POINT('Ctrl Pts',(-3.93355225073649,1.04098512265698,16.2799598444988));
#25091=CARTESIAN_POINT('Ctrl Pts',(-3.50650185007344,2.09245600266764,16.237743571908));
#25092=CARTESIAN_POINT('Ctrl Pts',(-2.76293020390983,2.82077853336478,16.1955272993172));
#25093=CARTESIAN_POINT('Ctrl Pts',(-1.83005502901329,3.73452236922869,16.1425633208226));
#25094=CARTESIAN_POINT('Ctrl Pts',(-0.398979196739877,4.13963456552086,
16.089599342328));
#25095=CARTESIAN_POINT('Ctrl Pts',(0.87442396179839,3.85044901031056,16.0366353638333));
#25096=CARTESIAN_POINT('Ctrl Pts',(2.14782712033666,3.56126345510026,15.9836713853387));
#25097=CARTESIAN_POINT('Ctrl Pts',(3.26355760513978,2.57778014838748,15.9307074068441));
#25098=CARTESIAN_POINT('Ctrl Pts',(3.7102673428296,1.35073723969577,15.8777434283495));
#25099=CARTESIAN_POINT('Ctrl Pts',(4.15697708051941,0.123694331004073,15.8247794498548));
#25100=CARTESIAN_POINT('Ctrl Pts',(3.93466607109594,-1.34690817966655,15.7718154713602));
#25101=CARTESIAN_POINT('Ctrl Pts',(3.14522120203587,-2.38708157301605,15.7188514928656));
#25102=CARTESIAN_POINT('Ctrl Pts',(2.3557763329758,-3.42725496636555,15.665887514371));
#25103=CARTESIAN_POINT('Ctrl Pts',(0.999197604279134,-4.03699924239392,
15.6129235358763));
#25104=CARTESIAN_POINT('Ctrl Pts',(-0.302784262564327,-3.93686379448313,
15.5599595573817));
#25105=CARTESIAN_POINT('Ctrl Pts',(-1.60476612940779,-3.83672834657235,
15.5069955788871));
#25106=CARTESIAN_POINT('Ctrl Pts',(-2.85215113439804,-3.02671317472241,
15.4540316003925));
#25107=CARTESIAN_POINT('Ctrl Pts',(-3.47325290008964,-1.8780546152835,15.4010676218978));
#25108=CARTESIAN_POINT('Ctrl Pts',(-3.78163641109193,-1.30773364846388,
15.3747704536284));
#25109=CARTESIAN_POINT('Ctrl Pts',(-3.9356269389069,-0.653929427477854,
15.348473285359));
#25110=CARTESIAN_POINT('Ctrl Pts',(-3.935515150562,-7.56757525427476E-5,
15.3221761170896));
#25111=CARTESIAN_POINT('Ctrl Pts',(-3.93554762371472,0.000453016733568931,
15.1778238829104));
#25112=CARTESIAN_POINT('Ctrl Pts',(-3.93484541553788,-0.685806715529583,
15.2054249731855));
#25113=CARTESIAN_POINT('Ctrl Pts',(-3.76434547901772,-1.37239299857592,
15.2330260634607));
#25114=CARTESIAN_POINT('Ctrl Pts',(-3.42606065206783,-1.96285227530577,
15.2606271537358));
#25115=CARTESIAN_POINT('Ctrl Pts',(-2.77662492673475,-3.09640991110095,
15.313615442464));
#25116=CARTESIAN_POINT('Ctrl Pts',(-1.5088024710418,-3.87568257532879,15.3666037311923));
#25117=CARTESIAN_POINT('Ctrl Pts',(-0.204134723598678,-3.94322325781103,
15.4195920199205));
#25118=CARTESIAN_POINT('Ctrl Pts',(1.10053302384446,-4.01076394029327,15.4725803086488));
#25119=CARTESIAN_POINT('Ctrl Pts',(2.44204606303776,-3.36657264102987,15.525568597377));
#25120=CARTESIAN_POINT('Ctrl Pts',(3.2050615916644,-2.30613547736428,15.5785568861053));
#25121=CARTESIAN_POINT('Ctrl Pts',(3.96807712029102,-1.24569831369873,15.6315451748335));
#25122=CARTESIAN_POINT('Ctrl Pts',(4.15259513835105,0.230984714368973,15.6845334635618));
#25123=CARTESIAN_POINT('Ctrl Pts',(3.67397850032763,1.44656926050946,15.73752175229));
#25124=CARTESIAN_POINT('Ctrl Pts',(3.1953618623042,2.66215380664994,15.7905100410183));
#25125=CARTESIAN_POINT('Ctrl Pts',(2.05361056819728,3.6166398708632,15.8434983297465));
#25126=CARTESIAN_POINT('Ctrl Pts',(0.772438082086977,3.87221126175501,15.8964866184748));
#25127=CARTESIAN_POINT('Ctrl Pts',(-0.508734404023323,4.12778265264681,
15.949474907203));
#25128=CARTESIAN_POINT('Ctrl Pts',(-1.92932808213704,3.68443937021718,16.0024631959313));
#25129=CARTESIAN_POINT('Ctrl Pts',(-2.83772640488938,2.74553992819521,16.0554514846595));
#25130=CARTESIAN_POINT('Ctrl Pts',(-3.53701854402849,2.02276778870165,16.0962422840765));
#25131=CARTESIAN_POINT('Ctrl Pts',(-3.93278162022236,1.00632704174549,16.1370330834934));
#25132=CARTESIAN_POINT('Ctrl Pts',(-3.94210945089404,-0.00361990150021516,
16.1778238829104));
#25133=CARTESIAN_POINT('Origin',(0.,0.,0.));
#25134=CARTESIAN_POINT('',(-3.94714763575412,0.00206509481356407,17.3221761170896));
#25135=CARTESIAN_POINT('',(-3.94786894067556,0.00143683566665543,17.1778238829104));
#25136=CARTESIAN_POINT('',(-3.942,-4.82755768223887E-16,0.));
#25137=CARTESIAN_POINT('Ctrl Pts',(-3.94714763575412,0.00206509481356407,
17.3221761170896));
#25138=CARTESIAN_POINT('Ctrl Pts',(-3.94790115726501,0.120559580499713,
17.3173743606278));
#25139=CARTESIAN_POINT('Ctrl Pts',(-3.94302847934562,0.238991236972465,
17.3125726041661));
#25140=CARTESIAN_POINT('Ctrl Pts',(-3.93232775304421,0.356893945881719,
17.3077708477043));
#25141=CARTESIAN_POINT('Ctrl Pts',(-3.81429739431669,1.6573756735258,17.2548068692097));
#25142=CARTESIAN_POINT('Ctrl Pts',(-2.98720523271932,2.89350369502107,17.201842890715));
#25143=CARTESIAN_POINT('Ctrl Pts',(-1.83011412357382,3.49875079716524,17.1488789122204));
#25144=CARTESIAN_POINT('Ctrl Pts',(-0.67302301442832,4.10399789930941,17.0959149337258));
#25145=CARTESIAN_POINT('Ctrl Pts',(0.814067042265299,4.07836408210249,17.0429509552312));
#25146=CARTESIAN_POINT('Ctrl Pts',(1.94961095493928,3.43359752597032,16.9899869767366));
#25147=CARTESIAN_POINT('Ctrl Pts',(3.08515486761327,2.78883096983815,16.9370229982419));
#25148=CARTESIAN_POINT('Ctrl Pts',(3.86915263626762,1.52493167478073,16.8840590197473));
#25149=CARTESIAN_POINT('Ctrl Pts',(3.94229190545934,0.221154647517415,16.8310950412527));
#25150=CARTESIAN_POINT('Ctrl Pts',(4.01543117465106,-1.08262237974594,16.7781310627581));
#25151=CARTESIAN_POINT('Ctrl Pts',(3.37771194438013,-2.42627713921516,16.7251670842634));
#25152=CARTESIAN_POINT('Ctrl Pts',(2.32140596324251,-3.19400206634104,16.6722031057688));
#25153=CARTESIAN_POINT('Ctrl Pts',(1.26509998210492,-3.96172699346691,16.6192391272742));
#25154=CARTESIAN_POINT('Ctrl Pts',(-0.209792749899407,-4.15352208824943,
16.5662751487796));
#25155=CARTESIAN_POINT('Ctrl Pts',(-1.42731727122521,-3.68148614736372,
16.5133111702849));
#25156=CARTESIAN_POINT('Ctrl Pts',(-2.64484179255099,-3.20945020647802,
16.4603471917903));
#25157=CARTESIAN_POINT('Ctrl Pts',(-3.60499810319833,-2.07358322992414,
16.4073832132957));
#25158=CARTESIAN_POINT('Ctrl Pts',(-3.86773899976216,-0.794462003929412,
16.3544192348011));
#25159=CARTESIAN_POINT('Ctrl Pts',(-3.92105564940663,-0.534896556939351,
16.3436715288973));
#25160=CARTESIAN_POINT('Ctrl Pts',(-3.94565379003534,-0.269432117224103,
16.3329238229934));
#25161=CARTESIAN_POINT('Ctrl Pts',(-3.94319808732824,-0.00351593218956836,
16.3221761170896));
#25162=CARTESIAN_POINT('Ctrl Pts',(-3.94210945089404,-0.00361990150021516,
16.1778238829104));
#25163=CARTESIAN_POINT('Ctrl Pts',(-3.94489871015204,-0.305619794154464,
16.1900213722217));
#25164=CARTESIAN_POINT('Ctrl Pts',(-3.91313437834161,-0.607039035223508,
16.202218861533));
#25165=CARTESIAN_POINT('Ctrl Pts',(-3.84459973154587,-0.899851960334574,
16.2144163508443));
#25166=CARTESIAN_POINT('Ctrl Pts',(-3.54687176805904,-2.17188880522799,
16.2674046395725));
#25167=CARTESIAN_POINT('Ctrl Pts',(-2.55521287369446,-3.2815068934005,16.3203929283008));
#25168=CARTESIAN_POINT('Ctrl Pts',(-1.32449016131116,-3.71973204127804,
16.373381217029));
#25169=CARTESIAN_POINT('Ctrl Pts',(-0.0937674489278181,-4.15795718915558,
16.4263695057573));
#25170=CARTESIAN_POINT('Ctrl Pts',(1.37601908147424,-3.9247893967381,16.4793577944855));
#25171=CARTESIAN_POINT('Ctrl Pts',(2.4106884596013,-3.12718112636055,16.5323460832138));
#25172=CARTESIAN_POINT('Ctrl Pts',(3.44535783772833,-2.32957285598302,16.585334371942));
#25173=CARTESIAN_POINT('Ctrl Pts',(4.04491006358037,-0.967524107645474,
16.6383226606703));
#25174=CARTESIAN_POINT('Ctrl Pts',(3.93433465569921,0.334202727823592,16.6913109493985));
#25175=CARTESIAN_POINT('Ctrl Pts',(3.82375924781804,1.63592956329268,16.7442992381268));
#25176=CARTESIAN_POINT('Ctrl Pts',(3.00305620620361,2.87733448589332,16.797287526855));
#25177=CARTESIAN_POINT('Ctrl Pts',(1.84867637012666,3.48899359770921,16.8502758155833));
#25178=CARTESIAN_POINT('Ctrl Pts',(0.694296534049695,4.10065270952511,16.9032641043115));
#25179=CARTESIAN_POINT('Ctrl Pts',(-0.793760096489806,4.08256601055629,
16.9562523930398));
#25180=CARTESIAN_POINT('Ctrl Pts',(-1.93293218195181,3.44302974519471,17.009240681768));
#25181=CARTESIAN_POINT('Ctrl Pts',(-3.0721042674138,2.80349347983313,17.0622289704962));
#25182=CARTESIAN_POINT('Ctrl Pts',(-3.86239180779829,1.54250764807881,17.1152172592245));
#25183=CARTESIAN_POINT('Ctrl Pts',(-3.94129534500935,0.238477776172487,
17.1682055479527));
#25184=CARTESIAN_POINT('Ctrl Pts',(-3.94606948578935,0.159576089253736,
17.1714116596053));
#25185=CARTESIAN_POINT('Ctrl Pts',(-3.9482392631182,0.0805168189138495,
17.1746177712579));
#25186=CARTESIAN_POINT('Ctrl Pts',(-3.94786894067556,0.00143683566665543,
17.1778238829104));
#25187=CARTESIAN_POINT('Origin',(0.,0.,0.));
#25188=CARTESIAN_POINT('',(-3.93691309430117,0.00231896033839218,18.3221761170896));
#25189=CARTESIAN_POINT('',(-3.93777174659584,0.00283174072808758,18.1778238829104));
#25190=CARTESIAN_POINT('',(-3.942,-4.82755768223887E-16,0.));
#25191=CARTESIAN_POINT('Ctrl Pts',(-3.93691309430117,0.00231896033839218,
18.3221761170896));
#25192=CARTESIAN_POINT('Ctrl Pts',(-3.93961914157867,0.507883428428715,
18.3018248982623));
#25193=CARTESIAN_POINT('Ctrl Pts',(-3.84930447301574,1.01251781158405,18.2814736794349));
#25194=CARTESIAN_POINT('Ctrl Pts',(-3.66151008646525,1.47780876052409,18.2611224606075));
#25195=CARTESIAN_POINT('Ctrl Pts',(-3.17277582759625,2.68872688893964,18.2081584821129));
#25196=CARTESIAN_POINT('Ctrl Pts',(-2.02381253743022,3.63317238083008,18.1551945036183));
#25197=CARTESIAN_POINT('Ctrl Pts',(-0.741199145924524,3.87829842483136,
18.1022305251237));
#25198=CARTESIAN_POINT('Ctrl Pts',(0.541414245581171,4.12342446883263,18.049266546629));
#25199=CARTESIAN_POINT('Ctrl Pts',(1.95767773842654,3.66923106494473,17.9963025681344));
#25200=CARTESIAN_POINT('Ctrl Pts',(2.8585066133837,2.72387862930978,17.9433385896398));
#25201=CARTESIAN_POINT('Ctrl Pts',(3.75933548834084,1.77852619367486,17.8903746111452));
#25202=CARTESIAN_POINT('Ctrl Pts',(4.14472974540982,0.342014726292911,17.8374106326505));
#25203=CARTESIAN_POINT('Ctrl Pts',(3.83806015958749,-0.927291247319836,
17.7844466541559));
#25204=CARTESIAN_POINT('Ctrl Pts',(3.53139057376515,-2.19659722093258,17.7314826756613));
#25205=CARTESIAN_POINT('Ctrl Pts',(2.53265714505146,-3.29869770077617,17.6785186971667));
#25206=CARTESIAN_POINT('Ctrl Pts',(1.29958727405717,-3.72849135215269,17.625554718672));
#25207=CARTESIAN_POINT('Ctrl Pts',(0.0665174030628353,-4.15828500352923,
17.5725907401774));
#25208=CARTESIAN_POINT('Ctrl Pts',(-1.40088891021208,-3.91577182643871,
17.5196267616828));
#25209=CARTESIAN_POINT('Ctrl Pts',(-2.43010778892075,-3.11209752099697,
17.4666627831882));
#25210=CARTESIAN_POINT('Ctrl Pts',(-3.36601686459191,-2.38128496799525,
17.4185005611553));
#25211=CARTESIAN_POINT('Ctrl Pts',(-3.93958972010326,-1.18644951952042,
17.3703383391225));
#25212=CARTESIAN_POINT('Ctrl Pts',(-3.94714763575412,0.00206509481356407,
17.3221761170896));
#25213=CARTESIAN_POINT('Ctrl Pts',(-3.94786894067556,0.00143683566665543,
17.1778238829104));
#25214=CARTESIAN_POINT('Ctrl Pts',(-3.94211884229706,-1.22645980543112,
17.2276060599861));
#25215=CARTESIAN_POINT('Ctrl Pts',(-3.32396017207549,-2.45935025115224,
17.2773882370618));
#25216=CARTESIAN_POINT('Ctrl Pts',(-2.33396838579359,-3.18485042355784,
17.3271704141375));
#25217=CARTESIAN_POINT('Ctrl Pts',(-1.28021835532917,-3.95707483932351,
17.3801587028657));
#25218=CARTESIAN_POINT('Ctrl Pts',(0.194801239637294,-4.15444975879655,
17.433146991594));
#25219=CARTESIAN_POINT('Ctrl Pts',(1.41450905809659,-3.68644066422928,17.4861352803222));
#25220=CARTESIAN_POINT('Ctrl Pts',(2.63421687655591,-3.21843156966201,17.5391235690505));
#25221=CARTESIAN_POINT('Ctrl Pts',(3.59861291850804,-2.08503846105438,17.5921118577787));
#25222=CARTESIAN_POINT('Ctrl Pts',(3.86533535394433,-0.806140960297021,
17.645100146507));
#25223=CARTESIAN_POINT('Ctrl Pts',(4.13205778938061,0.472756540460342,17.6980884352352));
#25224=CARTESIAN_POINT('Ctrl Pts',(3.70110661830104,1.89715843336744,17.7510767239635));
#25225=CARTESIAN_POINT('Ctrl Pts',(2.77015617820835,2.81370136913189,17.8040650126917));
#25226=CARTESIAN_POINT('Ctrl Pts',(1.83920573811566,3.73024430489631,17.85705330142));
#25227=CARTESIAN_POINT('Ctrl Pts',(0.408256029009864,4.13892828351809,17.9100415901482));
#25228=CARTESIAN_POINT('Ctrl Pts',(-0.866326161571161,3.85229277549071,
17.9630298788765));
#25229=CARTESIAN_POINT('Ctrl Pts',(-2.14090835215219,3.56565726746332,18.0160181676047));
#25230=CARTESIAN_POINT('Ctrl Pts',(-3.25912302420844,2.58370227278676,18.069006456333));
#25231=CARTESIAN_POINT('Ctrl Pts',(-3.70805280027739,1.35684379228987,18.1219947450612));
#25232=CARTESIAN_POINT('Ctrl Pts',(-3.86571884909867,0.925965870186712,
18.1406044576776));
#25233=CARTESIAN_POINT('Ctrl Pts',(-3.94083233343714,0.464880467044514,
18.159214170294));
#25234=CARTESIAN_POINT('Ctrl Pts',(-3.93777174659584,0.00283174072808758,
18.1778238829104));
#25235=CARTESIAN_POINT('Origin',(0.,0.,0.));
#25236=CARTESIAN_POINT('',(-3.93868067607543,-0.00317875339515938,19.3221761170896));
#25237=CARTESIAN_POINT('',(-3.93757571821786,-0.00273443803236162,19.1778238829104));
#25238=CARTESIAN_POINT('',(-3.942,-4.82755768223887E-16,0.));
#25239=CARTESIAN_POINT('Ctrl Pts',(-3.93868067607543,-0.00317875339515938,
19.3221761170896));
#25240=CARTESIAN_POINT('Ctrl Pts',(-3.93194593082782,0.887659399123926,
19.2862754358966));
#25241=CARTESIAN_POINT('Ctrl Pts',(-3.63268362464169,1.78259416274328,19.2503747547037));
#25242=CARTESIAN_POINT('Ctrl Pts',(-3.07838529125365,2.47267443157326,19.2144740735107));
#25243=CARTESIAN_POINT('Ctrl Pts',(-2.26063353742526,3.4907441534662,19.1615100950161));
#25244=CARTESIAN_POINT('Ctrl Pts',(-0.887799511314515,4.06295099197559,
19.1085461165215));
#25245=CARTESIAN_POINT('Ctrl Pts',(0.410936134697139,3.92704804390779,19.0555821380269));
#25246=CARTESIAN_POINT('Ctrl Pts',(1.70967178070872,3.79114509584001,19.0026181595322));
#25247=CARTESIAN_POINT('Ctrl Pts',(2.93430904662124,2.94713236119515,18.9496541810376));
#25248=CARTESIAN_POINT('Ctrl Pts',(3.52358702306116,1.78182752725689,18.896690202543));
#25249=CARTESIAN_POINT('Ctrl Pts',(4.11286499950109,0.616522693318613,18.8437262240484));
#25250=CARTESIAN_POINT('Ctrl Pts',(4.06678368646841,-0.870074239913033,
18.7907622455538));
#25251=CARTESIAN_POINT('Ctrl Pts',(3.40646251285886,-1.99664418323714,18.7377982670591));
#25252=CARTESIAN_POINT('Ctrl Pts',(2.74614133924929,-3.1232141265613,18.6848342885645));
#25253=CARTESIAN_POINT('Ctrl Pts',(1.47158030506274,-3.88975707997784,18.6318703100699));
#25254=CARTESIAN_POINT('Ctrl Pts',(0.166920776077049,-3.94496036741581,
18.5789063315753));
#25255=CARTESIAN_POINT('Ctrl Pts',(-1.1377387529086,-4.00016365485379,18.5259423530806));
#25256=CARTESIAN_POINT('Ctrl Pts',(-2.47249677669342,-3.34402727631325,
18.472978374586));
#25257=CARTESIAN_POINT('Ctrl Pts',(-3.22562317479983,-2.27726370457266,
18.4200143960914));
#25258=CARTESIAN_POINT('Ctrl Pts',(-3.689363454866,-1.62040021025458,18.3874016364241));
#25259=CARTESIAN_POINT('Ctrl Pts',(-3.93257666264772,-0.807846398012042,
18.3547888767569));
#25260=CARTESIAN_POINT('Ctrl Pts',(-3.93691309430117,0.00231896033839218,
18.3221761170896));
#25261=CARTESIAN_POINT('Ctrl Pts',(-3.93777174659584,0.00283174072808758,
18.1778238829104));
#25262=CARTESIAN_POINT('Ctrl Pts',(-3.93211778407426,-0.850732074710112,
18.2122024590223));
#25263=CARTESIAN_POINT('Ctrl Pts',(-3.65968019788323,-1.70758341046428,
18.2465810351341));
#25264=CARTESIAN_POINT('Ctrl Pts',(-3.14806281812505,-2.38335501750349,
18.280959611246));
#25265=CARTESIAN_POINT('Ctrl Pts',(-2.3594981798221,-3.42493338048278,18.3339478999742));
#25266=CARTESIAN_POINT('Ctrl Pts',(-1.00272402313454,-4.03632814012413,
18.3869361887025));
#25267=CARTESIAN_POINT('Ctrl Pts',(0.299916680013111,-3.93709672618929,
18.4399244774307));
#25268=CARTESIAN_POINT('Ctrl Pts',(1.60255738316074,-3.83786531225445,18.492912766159));
#25269=CARTESIAN_POINT('Ctrl Pts',(2.85106463276846,-3.02800772474346,18.5459010548872));
#25270=CARTESIAN_POINT('Ctrl Pts',(3.47275674238136,-1.8790000677396,18.5988893436155));
#25271=CARTESIAN_POINT('Ctrl Pts',(4.09444885199426,-0.729992410735758,
18.6518776323437));
#25272=CARTESIAN_POINT('Ctrl Pts',(4.08932582161236,0.758165315760947,18.704865921072));
#25273=CARTESIAN_POINT('Ctrl Pts',(3.45973755002874,1.90286540019034,18.7578542098002));
#25274=CARTESIAN_POINT('Ctrl Pts',(2.83014927844509,3.04756548461977,18.8108424985285));
#25275=CARTESIAN_POINT('Ctrl Pts',(1.57609576565968,3.84880792698187,18.8638307872567));
#25276=CARTESIAN_POINT('Ctrl Pts',(0.272802730892003,3.93906833100647,18.916819075985));
#25277=CARTESIAN_POINT('Ctrl Pts',(-1.03049030387567,4.02932873503108,18.9698073647132));
#25278=CARTESIAN_POINT('Ctrl Pts',(-2.3830228606256,3.4086071007182,19.0227956534415));
#25279=CARTESIAN_POINT('Ctrl Pts',(-3.16439756014476,2.36162417155469,19.0757839421697));
#25280=CARTESIAN_POINT('Ctrl Pts',(-3.66596391218726,1.68956324002662,19.10979725575));
#25281=CARTESIAN_POINT('Ctrl Pts',(-3.93219107470607,0.841866122485371,
19.1438105693302));
#25282=CARTESIAN_POINT('Ctrl Pts',(-3.93757571821786,-0.00273443803236162,
19.1778238829104));
#25283=CARTESIAN_POINT('Origin',(0.,0.,0.));
#25284=CARTESIAN_POINT('',(-3.94834041879863,-0.000694519400761262,20.3221761170896));
#25285=CARTESIAN_POINT('',(-3.94772619292891,-0.00158826883248112,20.1778238829104));
#25286=CARTESIAN_POINT('',(-3.942,-4.82755768223887E-16,0.));
#25287=CARTESIAN_POINT('Ctrl Pts',(-3.94834041879863,-0.000694519400761262,
20.3221761170896));
#25288=CARTESIAN_POINT('Ctrl Pts',(-3.94525718695861,1.26793825937276,20.270725973531));
#25289=CARTESIAN_POINT('Ctrl Pts',(-3.27892645249503,2.53935361509062,20.2192758299725));
#25290=CARTESIAN_POINT('Ctrl Pts',(-2.23269077785256,3.25663426508529,20.167825686414));
#25291=CARTESIAN_POINT('Ctrl Pts',(-1.15567135789659,3.9950197056954,20.1148617079193));
#25292=CARTESIAN_POINT('Ctrl Pts',(0.323938040913112,4.14618172311401,20.0618977294247));
#25293=CARTESIAN_POINT('Ctrl Pts',(1.52802077187684,3.64084157388599,20.0089337509301));
#25294=CARTESIAN_POINT('Ctrl Pts',(2.73210350284056,3.13550142465798,19.9559697724355));
#25295=CARTESIAN_POINT('Ctrl Pts',(3.66065956595831,1.97365910878334,19.9030057939409));
#25296=CARTESIAN_POINT('Ctrl Pts',(3.88812440006945,0.687796115025536,19.8500418154462));
#25297=CARTESIAN_POINT('Ctrl Pts',(4.11558923418059,-0.598066878732264,
19.7970778369516));
#25298=CARTESIAN_POINT('Ctrl Pts',(3.64196283928513,-2.00795055037323,19.744113858457));
#25299=CARTESIAN_POINT('Ctrl Pts',(2.68431192455269,-2.89569410291512,19.6911498799624));
#25300=CARTESIAN_POINT('Ctrl Pts',(1.72666100982023,-3.78343765545704,19.6381859014677));
#25301=CARTESIAN_POINT('Ctrl Pts',(0.284985575250775,-4.14904108889985,
19.5852219229731));
#25302=CARTESIAN_POINT('Ctrl Pts',(-0.979983166843207,-3.82494546870956,
19.5322579444785));
#25303=CARTESIAN_POINT('Ctrl Pts',(-2.24495190893719,-3.50084984851927,
19.4792939659839));
#25304=CARTESIAN_POINT('Ctrl Pts',(-3.3332139585557,-2.48705517469588,19.4263299874892));
#25305=CARTESIAN_POINT('Ctrl Pts',(-3.74601024259189,-1.24819153514592,
19.3733660089946));
#25306=CARTESIAN_POINT('Ctrl Pts',(-3.87899998240626,-0.849069354397836,
19.3563027116929));
#25307=CARTESIAN_POINT('Ctrl Pts',(-3.94188164487581,-0.426586770708422,
19.3392394143913));
#25308=CARTESIAN_POINT('Ctrl Pts',(-3.93868067607543,-0.00317875339515938,
19.3221761170896));
#25309=CARTESIAN_POINT('Ctrl Pts',(-3.93757571821786,-0.00273443803236162,
19.1778238829104));
#25310=CARTESIAN_POINT('Ctrl Pts',(-3.9405796442122,-0.473910955663478,
19.1967988580584));
#25311=CARTESIAN_POINT('Ctrl Pts',(-3.86240471339523,-0.944123769370189,
19.2157738332064));
#25312=CARTESIAN_POINT('Ctrl Pts',(-3.69862306761181,-1.38234150992047,
19.2347488083545));
#25313=CARTESIAN_POINT('Ctrl Pts',(-3.24125703327134,-2.60608003821792,
19.2877370970827));
#25314=CARTESIAN_POINT('Ctrl Pts',(-2.11630812230202,-3.58031287079873,
19.340725385811));
#25315=CARTESIAN_POINT('Ctrl Pts',(-0.839782661227222,-3.85816610946462,
19.3937136745392));
#25316=CARTESIAN_POINT('Ctrl Pts',(0.436742799847613,-4.13601934813052,
19.4467019632675));
#25317=CARTESIAN_POINT('Ctrl Pts',(1.86484481102796,-3.71749299288145,19.4996902519957));
#25318=CARTESIAN_POINT('Ctrl Pts',(2.78946280422149,-2.79456220367197,19.552678540724));
#25319=CARTESIAN_POINT('Ctrl Pts',(3.714080797415,-1.8716314144625,19.6056668294522));
#25320=CARTESIAN_POINT('Ctrl Pts',(4.13521477262173,-0.444296191292658,
19.6586551181805));
#25321=CARTESIAN_POINT('Ctrl Pts',(3.85969347255442,0.832734618130101,19.7116434069087));
#25322=CARTESIAN_POINT('Ctrl Pts',(3.5841721724871,2.10976542755288,19.764631695637));
#25323=CARTESIAN_POINT('Ctrl Pts',(2.6119955971457,3.23649182322855,19.8176199843652));
#25324=CARTESIAN_POINT('Ctrl Pts',(1.38909445367046,3.69609215863147,19.8706082730935));
#25325=CARTESIAN_POINT('Ctrl Pts',(0.166193310195227,4.1556924940344,19.9235965618217));
#25326=CARTESIAN_POINT('Ctrl Pts',(-1.30743240141386,3.94816676916459,19.97658485055));
#25327=CARTESIAN_POINT('Ctrl Pts',(-2.35584070483748,3.16870560636289,20.0295731392782));
#25328=CARTESIAN_POINT('Ctrl Pts',(-3.33358701031412,2.44177958936821,20.0789900538223));
#25329=CARTESIAN_POINT('Ctrl Pts',(-3.94150300763008,1.21741613169822,20.1284069683663));
#25330=CARTESIAN_POINT('Ctrl Pts',(-3.94772619292891,-0.00158826883248112,
20.1778238829104));
#25331=CARTESIAN_POINT('Origin',(0.,0.,0.));
#25332=CARTESIAN_POINT('',(-3.94074044801927,0.00358039056613663,21.3221761170896));
#25333=CARTESIAN_POINT('',(-3.94238528018782,0.00360576479228953,21.1778238829104));
#25334=CARTESIAN_POINT('',(-3.942,-4.82755768223887E-16,0.));
#25335=CARTESIAN_POINT('Ctrl Pts',(-3.94074044801927,0.00358039056613663,
21.3221761170896));
#25336=CARTESIAN_POINT('Ctrl Pts',(-3.94382356658785,0.35139917714199,21.3081404896601));
#25337=CARTESIAN_POINT('Ctrl Pts',(-3.90159553870986,0.69848167363253,21.2941048622306));
#25338=CARTESIAN_POINT('Ctrl Pts',(-3.81110742902655,1.03248974691214,21.2800692348011));
#25339=CARTESIAN_POINT('Ctrl Pts',(-3.46964707612424,2.29288202357064,21.2271052563065));
#25340=CARTESIAN_POINT('Ctrl Pts',(-2.44098286072968,3.36709985140295,21.1741412778118));
#25341=CARTESIAN_POINT('Ctrl Pts',(-1.19655973690358,3.76282070551412,21.1211772993172));
#25342=CARTESIAN_POINT('Ctrl Pts',(0.0478633869225303,4.15854155962529,
21.0682133208226));
#25343=CARTESIAN_POINT('Ctrl Pts',(1.50804541918014,3.87576544001532,21.0152493423279));
#25344=CARTESIAN_POINT('Ctrl Pts',(2.51477344786687,3.04409088599763,20.9622853638333));
#25345=CARTESIAN_POINT('Ctrl Pts',(3.52150147655357,2.21241633197998,20.9093213853387));
#25346=CARTESIAN_POINT('Ctrl Pts',(4.07477550166942,0.831843343554564,20.8563574068441));
#25347=CARTESIAN_POINT('Ctrl Pts',(3.92102566715379,-0.464900607518139,
20.8033934283495));
#25348=CARTESIAN_POINT('Ctrl Pts',(3.76727583263815,-1.76164455859092,20.7504294498548));
#25349=CARTESIAN_POINT('Ctrl Pts',(2.90650213849103,-2.97455947231102,20.6974654713602));
#25350=CARTESIAN_POINT('Ctrl Pts',(1.73320395728241,-3.54775688148229,20.6445014928656));
#25351=CARTESIAN_POINT('Ctrl Pts',(0.559905776073817,-4.12095429065355,
20.5915375143709));
#25352=CARTESIAN_POINT('Ctrl Pts',(-0.925916892196226,-4.05443419527599,
20.5385735358763));
#25353=CARTESIAN_POINT('Ctrl Pts',(-2.04329981292238,-3.37868328145881,
20.4856095573817));
#25354=CARTESIAN_POINT('Ctrl Pts',(-3.16068273364853,-2.70293236764162,
20.4326455788871));
#25355=CARTESIAN_POINT('Ctrl Pts',(-3.90962590683076,-1.41795063538484,
20.3796816003925));
#25356=CARTESIAN_POINT('Ctrl Pts',(-3.94688277287076,-0.11265533735563,
20.3267176218978));
#25357=CARTESIAN_POINT('Ctrl Pts',(-3.94794766163145,-0.0753469311478099,
20.3252037869617));
#25358=CARTESIAN_POINT('Ctrl Pts',(-3.94843113776951,-0.0380219297583325,
20.3236899520257));
#25359=CARTESIAN_POINT('Ctrl Pts',(-3.94834041879863,-0.000694519400761262,
20.3221761170896));
#25360=CARTESIAN_POINT('Ctrl Pts',(-3.94772619292891,-0.00158826883248112,
20.1778238829104));
#25361=CARTESIAN_POINT('Ctrl Pts',(-3.94817594426456,-0.0896860565358013,
20.1813952570946));
#25362=CARTESIAN_POINT('Ctrl Pts',(-3.9454830581488,-0.177755853920253,
20.1849666312788));
#25363=CARTESIAN_POINT('Ctrl Pts',(-3.93956001409796,-0.265607871813588,
20.188538005463));
#25364=CARTESIAN_POINT('Ctrl Pts',(-3.85168012469672,-1.56906358645505,
20.2415262941912));
#25365=CARTESIAN_POINT('Ctrl Pts',(-3.05272945065598,-2.82457841500438,
20.2945145829195));
#25366=CARTESIAN_POINT('Ctrl Pts',(-1.90918116982076,-3.45625634279478,
20.3475028716477));
#25367=CARTESIAN_POINT('Ctrl Pts',(-0.765632888985623,-4.08793427058512,
20.4004911603759));
#25368=CARTESIAN_POINT('Ctrl Pts',(0.722512998643886,-4.09577529761664,
20.4534794491042));
#25369=CARTESIAN_POINT('Ctrl Pts',(1.87265421179595,-3.47618279865318,20.5064677378324));
#25370=CARTESIAN_POINT('Ctrl Pts',(3.0227954249481,-2.85659029968967,20.5594560265607));
#25371=CARTESIAN_POINT('Ctrl Pts',(3.8349319636227,-1.60956427473106,20.6124443152889));
#25372=CARTESIAN_POINT('Ctrl Pts',(3.9365423847422,-0.307106982824769,20.6654326040172));
#25373=CARTESIAN_POINT('Ctrl Pts',(4.03815280586171,0.995350309081448,20.7184208927454));
#25374=CARTESIAN_POINT('Ctrl Pts',(3.4292371094262,2.35323886793535,20.7714091814737));
#25375=CARTESIAN_POINT('Ctrl Pts',(2.38910073600262,3.14370455348999,20.8243974702019));
#25376=CARTESIAN_POINT('Ctrl Pts',(1.348964362579,3.93417023904466,20.8773857589302));
#25377=CARTESIAN_POINT('Ctrl Pts',(-0.12239268783275,4.15721305130006,20.9303740476584));
#25378=CARTESIAN_POINT('Ctrl Pts',(-1.35006905738725,3.71052478612394,20.9833623363867));
#25379=CARTESIAN_POINT('Ctrl Pts',(-2.57774542694174,3.26383652094782,21.0363506251149));
#25380=CARTESIAN_POINT('Ctrl Pts',(-3.56174111563901,2.14741717834018,21.0893389138432));
#25381=CARTESIAN_POINT('Ctrl Pts',(-3.85070407192177,0.873360631535526,
21.1423272025715));
#25382=CARTESIAN_POINT('Ctrl Pts',(-3.91522918325707,0.588865201437585,
21.1541594293511));
#25383=CARTESIAN_POINT('Ctrl Pts',(-3.94509829421553,0.296509601950098,
21.1659916561308));
#25384=CARTESIAN_POINT('Ctrl Pts',(-3.94238528018782,0.00360576479228953,
21.1778238829104));
#25385=CARTESIAN_POINT('Origin',(0.,0.,0.));
#25386=CARTESIAN_POINT('',(-3.93587951376728,-0.00124481178566893,22.3221761170896));
#25387=CARTESIAN_POINT('',(-3.93552176014147,-0.00030393483444853,22.1778238829104));
#25388=CARTESIAN_POINT('',(-3.942,-4.82755768223887E-16,0.));
#25389=CARTESIAN_POINT('Ctrl Pts',(-3.93587951376728,-0.00124481178566893,
22.3221761170896));
#25390=CARTESIAN_POINT('Ctrl Pts',(-3.9337992464037,0.734189273701127,22.2925910272945));
#25391=CARTESIAN_POINT('Ctrl Pts',(-3.73627980596971,1.47066093628887,22.2630059374994));
#25392=CARTESIAN_POINT('Ctrl Pts',(-3.35026562609245,2.08956860583238,22.2334208477043));
#25393=CARTESIAN_POINT('Ctrl Pts',(-2.65921324588212,3.19755282108702,22.1804568692097));
#25394=CARTESIAN_POINT('Ctrl Pts',(-1.36405277538343,3.92875538432108,22.1274928907151));
#25395=CARTESIAN_POINT('Ctrl Pts',(-0.0583683106578484,3.94805897547177,
22.0745289122204));
#25396=CARTESIAN_POINT('Ctrl Pts',(1.2473161540677,3.96736256662245,22.0215649337258));
#25397=CARTESIAN_POINT('Ctrl Pts',(2.56352461302015,3.27476718568979,21.9686009552312));
#25398=CARTESIAN_POINT('Ctrl Pts',(3.28702932421304,2.18769549882087,21.9156369767366));
#25399=CARTESIAN_POINT('Ctrl Pts',(4.01053403540591,1.10062381195199,21.8626729982419));
#25400=CARTESIAN_POINT('Ctrl Pts',(4.14133499883926,-0.380924180853135,
21.8097090197473));
#25401=CARTESIAN_POINT('Ctrl Pts',(3.6194845960222,-1.57794374981529,21.7567450412527));
#25402=CARTESIAN_POINT('Ctrl Pts',(3.09763419320511,-2.77496331877751,21.7037810627581));
#25403=CARTESIAN_POINT('Ctrl Pts',(1.92313242413752,-3.68745446389673,21.6508170842634));
#25404=CARTESIAN_POINT('Ctrl Pts',(0.634262969967227,-3.89721509840628,
21.5978531057688));
#25405=CARTESIAN_POINT('Ctrl Pts',(-0.654606484203027,-4.10697573291583,
21.5448891272742));
#25406=CARTESIAN_POINT('Ctrl Pts',(-2.05784362347597,-3.61400585681575,
21.4919251487796));
#25407=CARTESIAN_POINT('Ctrl Pts',(-2.93233394790743,-2.64423755602338,
21.4389611702849));
#25408=CARTESIAN_POINT('Ctrl Pts',(-3.57508147783416,-1.93146102491564,
21.4000328192198));
#25409=CARTESIAN_POINT('Ctrl Pts',(-3.93218930040467,-0.961108355901809,
21.3611044681547));
#25410=CARTESIAN_POINT('Ctrl Pts',(-3.94074044801927,0.00358039056613663,
21.3221761170896));
#25411=CARTESIAN_POINT('Ctrl Pts',(-3.94238528018782,0.00360576479228953,
21.1778238829104));
#25412=CARTESIAN_POINT('Ctrl Pts',(-3.93294859718036,-1.0152023337623,21.218979944859));
#25413=CARTESIAN_POINT('Ctrl Pts',(-3.52931423770067,-2.04064333351309,
21.2601360068076));
#25414=CARTESIAN_POINT('Ctrl Pts',(-2.81875615331693,-2.76501254901743,
21.3012920687562));
#25415=CARTESIAN_POINT('Ctrl Pts',(-1.90391505456104,-3.69763543176414,
21.3542803574844));
#25416=CARTESIAN_POINT('Ctrl Pts',(-0.480302633180845,-4.13118744625593,
21.4072686462127));
#25417=CARTESIAN_POINT('Ctrl Pts',(0.799079880925017,-3.86680126221775,
21.4602569349409));
#25418=CARTESIAN_POINT('Ctrl Pts',(2.07846239503088,-3.60241507817958,21.5132452236692));
#25419=CARTESIAN_POINT('Ctrl Pts',(3.21361500186243,-2.64009069561159,21.5662335123974));
#25420=CARTESIAN_POINT('Ctrl Pts',(3.68385102080785,-1.42123969585553,21.6192218011257));
#25421=CARTESIAN_POINT('Ctrl Pts',(4.15408703975328,-0.202388696099407,
21.6722100898539));
#25422=CARTESIAN_POINT('Ctrl Pts',(3.95940647081237,1.27298892084472,21.7251983785822));
#25423=CARTESIAN_POINT('Ctrl Pts',(3.18910793065139,2.32814760557936,21.7781866673104));
#25424=CARTESIAN_POINT('Ctrl Pts',(2.41880939049046,3.38330629031394,21.8311749560387));
#25425=CARTESIAN_POINT('Ctrl Pts',(1.07289287910942,4.01824604283911,21.8841632447669));
#25426=CARTESIAN_POINT('Ctrl Pts',(-0.231278918613751,3.94172434024104,
21.9371515334952));
#25427=CARTESIAN_POINT('Ctrl Pts',(-1.53545071633696,3.86520263764296,21.9901398222234));
#25428=CARTESIAN_POINT('Ctrl Pts',(-2.79787780040235,3.07721947992169,22.0431281109517));
#25429=CARTESIAN_POINT('Ctrl Pts',(-3.43949362875525,1.93921737114795,22.0961163996799));
#25430=CARTESIAN_POINT('Ctrl Pts',(-3.76928231599023,1.35428756589898,22.1233522274234));
#25431=CARTESIAN_POINT('Ctrl Pts',(-3.93505699138564,0.676885190519015,
22.1505880551669));
#25432=CARTESIAN_POINT('Ctrl Pts',(-3.93552176014147,-0.00030393483444853,
22.1778238829104));
#25433=CARTESIAN_POINT('Origin',(0.,0.,0.));
#25434=CARTESIAN_POINT('',(-3.94525314071248,-0.00295827654940184,23.3221761170896));
#25435=CARTESIAN_POINT('',(-3.94350653563855,-0.00347714007584369,23.1778238829104));
#25436=CARTESIAN_POINT('',(-3.942,-4.82755768223887E-16,0.));
#25437=CARTESIAN_POINT('Ctrl Pts',(-3.94525314071248,-0.00295827654940184,
23.3221761170896));
#25438=CARTESIAN_POINT('Ctrl Pts',(-3.93582062597525,1.11220231279806,23.2770415649289));
#25439=CARTESIAN_POINT('Ctrl Pts',(-3.44025122786987,2.23463092251658,23.2319070127682));
#25440=CARTESIAN_POINT('Ctrl Pts',(-2.60368934111206,2.9683990932166,23.1867724606075));
#25441=CARTESIAN_POINT('Ctrl Pts',(-1.62201025804696,3.82945298103697,23.1338084821129));
#25442=CARTESIAN_POINT('Ctrl Pts',(-0.170774803008089,4.15531037113838,
23.0808445036183));
#25443=CARTESIAN_POINT('Ctrl Pts',(1.08481479710351,3.79655919604497,23.0278805251236));
#25444=CARTESIAN_POINT('Ctrl Pts',(2.34040439721512,3.43780802095157,22.974916546629));
#25445=CARTESIAN_POINT('Ctrl Pts',(3.40034814239945,2.39444828066336,22.9219525681344));
#25446=CARTESIAN_POINT('Ctrl Pts',(3.77891236751962,1.14469612557038,22.8689885896398));
#25447=CARTESIAN_POINT('Ctrl Pts',(4.15747659263979,-0.105056029522605,
22.8160246111452));
#25448=CARTESIAN_POINT('Ctrl Pts',(3.85466129769578,-1.56120059942036,22.7630606326505));
#25449=CARTESIAN_POINT('Ctrl Pts',(3.00922455792002,-2.55639398676302,22.7100966541559));
#25450=CARTESIAN_POINT('Ctrl Pts',(2.16378781814425,-3.55158737410568,22.6571326756613));
#25451=CARTESIAN_POINT('Ctrl Pts',(0.77572963353673,-4.08582957889326,22.6041686971666));
#25452=CARTESIAN_POINT('Ctrl Pts',(-0.518779131279689,-3.91426327466899,
22.551204718672));
#25453=CARTESIAN_POINT('Ctrl Pts',(-1.81328789609611,-3.74269697044473,
22.4982407401774));
#25454=CARTESIAN_POINT('Ctrl Pts',(-3.01424724112142,-2.86532215720863,
22.4452767616828));
#25455=CARTESIAN_POINT('Ctrl Pts',(-3.57125476867308,-1.684251816953,22.3923127831882));
#25456=CARTESIAN_POINT('Ctrl Pts',(-3.81712408139379,-1.16291424345579,
22.3689338944886));
#25457=CARTESIAN_POINT('Ctrl Pts',(-3.9375233938263,-0.582403488318747,
22.3455550057891));
#25458=CARTESIAN_POINT('Ctrl Pts',(-3.93587951376728,-0.00124481178566893,
22.3221761170896));
#25459=CARTESIAN_POINT('Ctrl Pts',(-3.93552176014147,-0.00030393483444853,
22.1778238829104));
#25460=CARTESIAN_POINT('Ctrl Pts',(-3.93596121582331,-0.640610765021898,
22.2035763438952));
#25461=CARTESIAN_POINT('Ctrl Pts',(-3.78860721752551,-1.28072694143294,
22.2293288048799));
#25462=CARTESIAN_POINT('Ctrl Pts',(-3.49236428582461,-1.84230088118771,
22.2550812658647));
#25463=CARTESIAN_POINT('Ctrl Pts',(-2.88281454190065,-2.99779596492355,
22.3080695545929));
#25464=CARTESIAN_POINT('Ctrl Pts',(-1.64291048141232,-3.82076507256913,
22.3610578433212));
#25465=CARTESIAN_POINT('Ctrl Pts',(-0.341387846963322,-3.93371775192091,
22.4140461320494));
#25466=CARTESIAN_POINT('Ctrl Pts',(0.96013478748571,-4.04667043127269,22.4670344207777));
#25467=CARTESIAN_POINT('Ctrl Pts',(2.3232759958954,-3.44960668233064,22.5200227095059));
#25468=CARTESIAN_POINT('Ctrl Pts',(3.12277281794346,-2.41639589080571,22.5730109982342));
#25469=CARTESIAN_POINT('Ctrl Pts',(3.92226963999152,-1.38318509928078,22.6259992869624));
#25470=CARTESIAN_POINT('Ctrl Pts',(4.15812207567794,0.0861727348270178,
22.6789875756907));
#25471=CARTESIAN_POINT('Ctrl Pts',(3.72214521454942,1.31769395259273,22.7319758644189));
#25472=CARTESIAN_POINT('Ctrl Pts',(3.28616835342092,2.5492151703584,22.7849641531472));
#25473=CARTESIAN_POINT('Ctrl Pts',(2.17836219547751,3.54289977178199,22.8379524418754));
#25474=CARTESIAN_POINT('Ctrl Pts',(0.906871753871591,3.84295018391872,22.8909407306037));
#25475=CARTESIAN_POINT('Ctrl Pts',(-0.364618687734369,4.14300059605545,
22.9439290193319));
#25476=CARTESIAN_POINT('Ctrl Pts',(-1.79979341300285,3.74941681890528,22.9969173080602));
#25477=CARTESIAN_POINT('Ctrl Pts',(-2.74035137198678,2.84273547234742,23.0499055967884));
#25478=CARTESIAN_POINT('Ctrl Pts',(-3.49721397313409,2.11313322315816,23.0925450254957));
#25479=CARTESIAN_POINT('Ctrl Pts',(-3.9337951138205,1.05128255440302,23.1351844542031));
#25480=CARTESIAN_POINT('Ctrl Pts',(-3.94350653563855,-0.00347714007584369,
23.1778238829104));
#25481=CARTESIAN_POINT('Origin',(0.,0.,-1.84858989190503));
#25482=CARTESIAN_POINT('',(-3.37453254114594,-0.00253033205341837,23.651410108095));
#25483=CARTESIAN_POINT('',(-3.37610896110192,0.00188753811008129,23.848589891905));
#25484=CARTESIAN_POINT('',(-3.37175,2.08693528006523E-13,-1.84858989190503));
#25485=CARTESIAN_POINT('',(-3.33611311329475,0.488924695431507,24.62825));
#25486=CARTESIAN_POINT('Ctrl Pts',(-3.37453254114594,-0.00253033205341877,
23.651410108095));
#25487=CARTESIAN_POINT('Ctrl Pts',(-3.37593208671392,-0.167991834513083,
23.6592395344289));
#25488=CARTESIAN_POINT('Ctrl Pts',(-3.28964411790747,-1.45130369571974,
23.7200329392575));
#25489=CARTESIAN_POINT('Ctrl Pts',(-1.64345961820725,-3.63211696072943,
23.8337903225806));
#25490=CARTESIAN_POINT('Ctrl Pts',(2.163389782855,-3.34808861530533,23.9926822580645));
#25491=CARTESIAN_POINT('Ctrl Pts',(3.98513370400483,0.0032270738820094,
24.1515741935484));
#25492=CARTESIAN_POINT('Ctrl Pts',(2.15811323746268,3.35470758430291,24.3104661290323));
#25493=CARTESIAN_POINT('Ctrl Pts',(-1.65524532662936,3.62504834974875,24.4693580645161));
#25494=CARTESIAN_POINT('Ctrl Pts',(-3.1734075349997,1.59912472915632,24.5752860215054));
#25495=CARTESIAN_POINT('Ctrl Pts',(-3.33611311329483,0.488924695430968,
24.62825));
#25496=CARTESIAN_POINT('',(-0.624728334461187,3.31336876465952,24.62825));
#25497=CARTESIAN_POINT('Origin',(0.,0.,24.62825));
#25498=CARTESIAN_POINT('Ctrl Pts',(-3.37610896110192,0.00188753811008135,
23.848589891905));
#25499=CARTESIAN_POINT('Ctrl Pts',(-3.36932955763165,-1.01002015324007,
23.8965234396903));
#25500=CARTESIAN_POINT('Ctrl Pts',(-2.34697770975975,-3.15243101165571,
23.997445276204));
#25501=CARTESIAN_POINT('Ctrl Pts',(1.29650641132588,-3.76899081084458,24.1513554014457));
#25502=CARTESIAN_POINT('Ctrl Pts',(3.87454091099827,-0.951014904317504,
24.3103202676305));
#25503=CARTESIAN_POINT('Ctrl Pts',(2.88961752940844,2.74513957150359,24.4692851338152));
#25504=CARTESIAN_POINT('Ctrl Pts',(0.478408881098333,3.52136284087264,24.5752617112718));
#25505=CARTESIAN_POINT('Ctrl Pts',(-0.624728334461281,3.3133687646595,24.62825));
#25506=CARTESIAN_POINT('Origin',(0.,0.,-1.84858989190503));
#25507=CARTESIAN_POINT('',(-3.36651490374044,-0.00106473722420811,22.651410108095));
#25508=CARTESIAN_POINT('',(-3.37303860008607,-0.00297413674536479,22.848589891905));
#25509=CARTESIAN_POINT('',(-3.37175,2.08693528006523E-13,-1.84858989190503));
#25510=CARTESIAN_POINT('Ctrl Pts',(-3.36651490374044,-0.00106473722420751,
22.651410108095));
#25511=CARTESIAN_POINT('Ctrl Pts',(-3.36792097999337,-0.498152958330381,
22.6747889967945));
#25512=CARTESIAN_POINT('Ctrl Pts',(-3.03163608822923,-2.11956584279889,
22.7511318639887));
#25513=CARTESIAN_POINT('Ctrl Pts',(-0.52374905937927,-3.95173187129016,
22.8804387096774));
#25514=CARTESIAN_POINT('Ctrl Pts',(3.03803570770629,-2.58085580280275,23.0393306451613));
#25515=CARTESIAN_POINT('Ctrl Pts',(3.81506574631169,1.15563997615671,23.1982225806452));
#25516=CARTESIAN_POINT('Ctrl Pts',(1.095229123157,3.83292171460177,23.357114516129));
#25517=CARTESIAN_POINT('Ctrl Pts',(-2.44517403763626,3.03796695389969,23.508177025279));
#25518=CARTESIAN_POINT('Ctrl Pts',(-3.36646453466052,0.951311047229191,
23.6062755559343));
#25519=CARTESIAN_POINT('Ctrl Pts',(-3.37453254114594,-0.00253033205341877,
23.651410108095));
#25520=CARTESIAN_POINT('Ctrl Pts',(-3.37303860008607,-0.00297413674536527,
22.848589891905));
#25521=CARTESIAN_POINT('Ctrl Pts',(-3.3750546565899,-0.221938484280555,
22.8589387519259));
#25522=CARTESIAN_POINT('Ctrl Pts',(-3.25576106932785,-1.5598586434856,22.9222759006751));
#25523=CARTESIAN_POINT('Ctrl Pts',(-1.46739644894177,-3.70704069007233,
23.0386013381526));
#25524=CARTESIAN_POINT('Ctrl Pts',(2.32262200499063,-3.24046036848089,23.1975662043372));
#25525=CARTESIAN_POINT('Ctrl Pts',(3.98198637087808,0.198816238648098,23.3565310705221));
#25526=CARTESIAN_POINT('Ctrl Pts',(1.98816433058814,3.45581133218519,23.5154959367067));
#25527=CARTESIAN_POINT('Ctrl Pts',(-1.82925354411967,3.5422830008711,23.6744608028915));
#25528=CARTESIAN_POINT('Ctrl Pts',(-3.3238940749889,1.33320070540347,23.7854921212909));
#25529=CARTESIAN_POINT('Ctrl Pts',(-3.37682387017652,0.108596335481547,
23.8435351509621));
#25530=CARTESIAN_POINT('Ctrl Pts',(-3.37610896110192,0.00188753811008135,
23.848589891905));
#25531=CARTESIAN_POINT('Origin',(0.,0.,-1.84858989190503));
#25532=CARTESIAN_POINT('',(-3.37067265489827,0.00306245101284196,21.651410108095));
#25533=CARTESIAN_POINT('',(-3.36620890277955,-0.000259967599581801,21.848589891905));
#25534=CARTESIAN_POINT('',(-3.37175,2.08693528006523E-13,-1.84858989190503));
#25535=CARTESIAN_POINT('Ctrl Pts',(-3.37067265489827,0.00306245101284172,
21.651410108095));
#25536=CARTESIAN_POINT('Ctrl Pts',(-3.36335851690506,-0.822074352869367,
21.6903384591601));
#25537=CARTESIAN_POINT('Ctrl Pts',(-2.64233179033033,-2.78128712935246,
21.7822307887199));
#25538=CARTESIAN_POINT('Ctrl Pts',(0.640333691332285,-3.93451715048184,
21.9270870967742));
#25539=CARTESIAN_POINT('Ctrl Pts',(3.6541284705207,-1.59304681672573,22.0859790322581));
#25540=CARTESIAN_POINT('Ctrl Pts',(3.31849061020388,2.20863464806944,22.2448709677419));
#25541=CARTESIAN_POINT('Ctrl Pts',(-0.058926339166703,3.98584809986529,
22.4037629032258));
#25542=CARTESIAN_POINT('Ctrl Pts',(-2.89333741463138,2.3856381715614,22.5392759500101));
#25543=CARTESIAN_POINT('Ctrl Pts',(-3.36473556800141,0.627981401218202,
22.6218250182999));
#25544=CARTESIAN_POINT('Ctrl Pts',(-3.36651490374044,-0.00106473722420751,
22.651410108095));
#25545=CARTESIAN_POINT('Ctrl Pts',(-3.36620890277955,-0.00025996759958187,
21.848589891905));
#25546=CARTESIAN_POINT('Ctrl Pts',(-3.36658478677126,-0.547939966251195,
21.8743423528898));
#25547=CARTESIAN_POINT('Ctrl Pts',(-2.98121161418831,-2.22202824736231,
21.9530831026028));
#25548=CARTESIAN_POINT('Ctrl Pts',(-0.344707483447601,-3.97197126386073,
22.0848121410441));
#25549=CARTESIAN_POINT('Ctrl Pts',(3.15313982968432,-2.43989387002868,22.2437770072288));
#25550=CARTESIAN_POINT('Ctrl Pts',(3.75834184644668,1.33050740634341,22.4027418734136));
#25551=CARTESIAN_POINT('Ctrl Pts',(0.915689325102905,3.88032175554439,22.5617067395983));
#25552=CARTESIAN_POINT('Ctrl Pts',(-2.52724878310966,2.93612690507347,22.7103227457621));
#25553=CARTESIAN_POINT('Ctrl Pts',(-3.36473203323799,0.899203945410642,
22.8059504631977));
#25554=CARTESIAN_POINT('Ctrl Pts',(-3.37303860008607,-0.00297413674536527,
22.848589891905));
#25555=CARTESIAN_POINT('Origin',(0.,0.,-1.84858989190503));
#25556=CARTESIAN_POINT('',(-3.37717321336486,-0.000594050174885632,20.651410108095));
#25557=CARTESIAN_POINT('',(-3.37207954552848,0.0030841546013495,20.848589891905));
#25558=CARTESIAN_POINT('',(-3.37175,2.08693528006523E-13,-1.84858989190503));
#25559=CARTESIAN_POINT('Ctrl Pts',(-3.37717321336486,-0.000594050174885286,
20.651410108095));
#25560=CARTESIAN_POINT('Ctrl Pts',(-3.37725080892297,-0.0325216746987667,
20.6529239430311));
#25561=CARTESIAN_POINT('Ctrl Pts',(-3.36236902703727,-1.18141504466881,
20.7074017564618));
#25562=CARTESIAN_POINT('Ctrl Pts',(-2.06285714434356,-3.41102216294582,
20.8148435483871));
#25563=CARTESIAN_POINT('Ctrl Pts',(1.74979322227715,-3.58171404391184,20.9737354838709));
#25564=CARTESIAN_POINT('Ctrl Pts',(3.95855555351044,-0.46935037546761,21.1326274193549));
#25565=CARTESIAN_POINT('Ctrl Pts',(2.53884345747981,3.07322723010567,21.2915193548387));
#25566=CARTESIAN_POINT('Ctrl Pts',(-1.20801252978399,3.79883634829061,21.4504112903226));
#25567=CARTESIAN_POINT('Ctrl Pts',(-3.20089281760442,1.71770287259066,21.5703748747413));
#25568=CARTESIAN_POINT('Ctrl Pts',(-3.3733097693157,0.300565747216989,21.6373744806655));
#25569=CARTESIAN_POINT('Ctrl Pts',(-3.37067265489827,0.00306245101284172,
21.651410108095));
#25570=CARTESIAN_POINT('Ctrl Pts',(-3.37207954552848,0.00308415460134954,
20.848589891905));
#25571=CARTESIAN_POINT('Ctrl Pts',(-3.36400797375518,-0.868343092050458,
20.8897459538536));
#25572=CARTESIAN_POINT('Ctrl Pts',(-2.57426217007386,-2.87470778191459,
20.9838903045305));
#25573=CARTESIAN_POINT('Ctrl Pts',(0.806850527235046,-3.9044039261228,21.1310229439355));
#25574=CARTESIAN_POINT('Ctrl Pts',(3.71967457752779,-1.43506051902692,21.2899878101203));
#25575=CARTESIAN_POINT('Ctrl Pts',(3.22012038549849,2.35078763921597,21.448952676305));
#25576=CARTESIAN_POINT('Ctrl Pts',(-0.233528014234224,3.98005560769136,
21.6079175424898));
#25577=CARTESIAN_POINT('Ctrl Pts',(-2.94815289437509,2.2856379957105,21.7411299476898));
#25578=CARTESIAN_POINT('Ctrl Pts',(-3.36581136750493,0.578966930779549,
21.8213540641615));
#25579=CARTESIAN_POINT('Ctrl Pts',(-3.36620890277955,-0.00025996759958187,
21.848589891905));
#25580=CARTESIAN_POINT('Origin',(0.,0.,-1.84858989190503));
#25581=CARTESIAN_POINT('',(-3.36891084971013,-0.00271891470300727,19.651410108095));
#25582=CARTESIAN_POINT('',(-3.37664784145308,-0.00135850975013785,19.848589891905));
#25583=CARTESIAN_POINT('',(-3.37175,2.08693528006523E-13,-1.84858989190503));
#25584=CARTESIAN_POINT('Ctrl Pts',(-3.36891084971013,-0.00271891470300756,
19.651410108095));
#25585=CARTESIAN_POINT('Ctrl Pts',(-3.3716487661365,-0.364876698157186,
19.6684734053967));
#25586=CARTESIAN_POINT('Ctrl Pts',(-3.15091588331813,-1.84791316659487,
19.738500681193));
#25587=CARTESIAN_POINT('Ctrl Pts',(-0.989363022110038,-3.86155572506565,
19.8614919354839));
#25588=CARTESIAN_POINT('Ctrl Pts',(2.71000466929749,-2.92341008068914,20.0203838709678));
#25589=CARTESIAN_POINT('Ctrl Pts',(3.92533937020224,0.694379317983201,20.1792758064516));
#25590=CARTESIAN_POINT('Ctrl Pts',(1.54264613898669,3.6756896897871,20.3381677419355));
#25591=CARTESIAN_POINT('Ctrl Pts',(-2.21788792003282,3.29150051432633,20.4955458424833));
#25592=CARTESIAN_POINT('Ctrl Pts',(-3.37453600206181,1.08451822071036,20.5999599645364));
#25593=CARTESIAN_POINT('Ctrl Pts',(-3.37717321336486,-0.000594050174885286,
20.651410108095));
#25594=CARTESIAN_POINT('Ctrl Pts',(-3.37664784145308,-0.0013585097501378,
19.848589891905));
#25595=CARTESIAN_POINT('Ctrl Pts',(-3.37703253172857,-0.0767120652268113,
19.8521612660892));
#25596=CARTESIAN_POINT('Ctrl Pts',(-3.3405547692736,-1.26970315744226,19.9087209290016));
#25597=CARTESIAN_POINT('Ctrl Pts',(-1.92774697870435,-3.4898666651324,20.0182688806423));
#25598=CARTESIAN_POINT('Ctrl Pts',(1.89086481476229,-3.50998689564495,20.1772337468271));
#25599=CARTESIAN_POINT('Ctrl Pts',(3.97482324267393,-0.310093440809367,
20.3361986130118));
#25600=CARTESIAN_POINT('Ctrl Pts',(2.41233351706024,3.17427546962878,20.4951634791965));
#25601=CARTESIAN_POINT('Ctrl Pts',(-1.36319778790607,3.74660773920425,20.6541283453813));
#25602=CARTESIAN_POINT('Ctrl Pts',(-3.23443909431523,1.62353950510727,20.7719371496175));
#25603=CARTESIAN_POINT('Ctrl Pts',(-3.37440009475423,0.25361650187097,20.8367576651254));
#25604=CARTESIAN_POINT('Ctrl Pts',(-3.37207954552848,0.00308415460134954,
20.848589891905));
#25605=CARTESIAN_POINT('Origin',(0.,0.,-1.84858989190503));
#25606=CARTESIAN_POINT('',(-3.36739896644089,0.00198349937115513,18.651410108095));
#25607=CARTESIAN_POINT('',(-3.36796573513472,-0.00233887403243982,18.848589891905));
#25608=CARTESIAN_POINT('',(-3.37175,2.08693528006523E-13,-1.84858989190503));
#25609=CARTESIAN_POINT('Ctrl Pts',(-3.36739896644089,0.00198349937115483,
18.651410108095));
#25610=CARTESIAN_POINT('Ctrl Pts',(-3.36368984329845,-0.690983280694315,
18.6840228677623));
#25611=CARTESIAN_POINT('Ctrl Pts',(-2.81781374229535,-2.51470704523694,
18.7695996059241));
#25612=CARTESIAN_POINT('Ctrl Pts',(0.168518449156949,-3.98271933982683,
18.9081403225806));
#25613=CARTESIAN_POINT('Ctrl Pts',(3.43906728250426,-2.01575495384355,19.0670322580645));
#25614=CARTESIAN_POINT('Ctrl Pts',(3.55731284355299,1.79888219198906,19.2259241935484));
#25615=CARTESIAN_POINT('Ctrl Pts',(0.41486938743375,3.96463556949202,19.3848161290323));
#25616=CARTESIAN_POINT('Ctrl Pts',(-2.72954745140897,2.65402060505441,19.5266447672144));
#25617=CARTESIAN_POINT('Ctrl Pts',(-3.36315035318836,0.75925052739643,19.615509426902));
#25618=CARTESIAN_POINT('Ctrl Pts',(-3.36891084971013,-0.00271891470300756,
19.651410108095));
#25619=CARTESIAN_POINT('Ctrl Pts',(-3.36796573513472,-0.00233887403243996,
18.848589891905));
#25620=CARTESIAN_POINT('Ctrl Pts',(-3.37053511298134,-0.405354963155371,
18.867564867053));
#25621=CARTESIAN_POINT('Ctrl Pts',(-3.11694291466331,-1.93068155902232,
18.9395281309293));
#25622=CARTESIAN_POINT('Ctrl Pts',(-0.847949117405149,-3.89568479841959,
19.0644796835338));
#25623=CARTESIAN_POINT('Ctrl Pts',(2.81658890100978,-2.82173788950715,19.2234445497186));
#25624=CARTESIAN_POINT('Ctrl Pts',(3.89722701433046,0.840832535700663,19.3824094159033));
#25625=CARTESIAN_POINT('Ctrl Pts',(1.40260268563389,3.73203476143841,19.5413742820881));
#25626=CARTESIAN_POINT('Ctrl Pts',(-2.29379652508948,3.21148336255172,19.6967677740886));
#25627=CARTESIAN_POINT('Ctrl Pts',(-3.37132490258154,1.04130462761393,19.799172977361));
#25628=CARTESIAN_POINT('Ctrl Pts',(-3.37664784145308,-0.0013585097501378,
19.848589891905));
#25629=CARTESIAN_POINT('Origin',(0.,0.,-1.84858989190503));
#25630=CARTESIAN_POINT('',(-3.3761529784003,0.00176635805113218,17.651410108095));
#25631=CARTESIAN_POINT('',(-3.36813340603362,0.00242210091315795,17.848589891905));
#25632=CARTESIAN_POINT('',(-3.37175,2.08693528006523E-13,-1.84858989190503));
#25633=CARTESIAN_POINT('Ctrl Pts',(-3.3761529784003,0.00176635805113214,
17.651410108095));
#25634=CARTESIAN_POINT('Ctrl Pts',(-3.36968839136432,-1.01481764775316,
17.6995723301278));
#25635=CARTESIAN_POINT('Ctrl Pts',(-2.33957623769215,-3.16069067030928,
17.8006985306553));
#25636=CARTESIAN_POINT('Ctrl Pts',(1.31202620257783,-3.7641784032229,17.9547887096774));
#25637=CARTESIAN_POINT('Ctrl Pts',(3.87479594250582,-0.936166764781103,
18.1136806451613));
#25638=CARTESIAN_POINT('Ctrl Pts',(2.88586665310525,2.74995008464444,18.2725725806452));
#25639=CARTESIAN_POINT('Ctrl Pts',(-0.748293493014444,3.91541934610488,
18.431464516129));
#25640=CARTESIAN_POINT('Ctrl Pts',(-3.09142162050251,1.98937278233,18.5577436919457));
#25641=CARTESIAN_POINT('Ctrl Pts',(-3.36971355672701,0.434412975597321,
18.6310588892676));
#25642=CARTESIAN_POINT('Ctrl Pts',(-3.36739896644089,0.00198349937115483,
18.651410108095));
#25643=CARTESIAN_POINT('Ctrl Pts',(-3.36813340603362,0.00242210091315778,
17.848589891905));
#25644=CARTESIAN_POINT('Ctrl Pts',(-3.36329734613199,-0.727665112355139,
17.8829684680169));
#25645=CARTESIAN_POINT('Ctrl Pts',(-2.77110248260437,-2.59019431375764,
17.970335332857));
#25646=CARTESIAN_POINT('Ctrl Pts',(0.302833216085013,-3.97538297495793,
18.1106904864254));
#25647=CARTESIAN_POINT('Ctrl Pts',(3.5065275226793,-1.89727238082542,18.2696553526101));
#25648=CARTESIAN_POINT('Ctrl Pts',(3.49338172535042,1.92136979140851,18.4286202187948));
#25649=CARTESIAN_POINT('Ctrl Pts',(0.275455597698851,3.97737375262188,18.5875850849796));
#25650=CARTESIAN_POINT('Ctrl Pts',(-2.78089559275923,2.57471376007135,18.7275749760163));
#25651=CARTESIAN_POINT('Ctrl Pts',(-3.36336003453583,0.720081709408907,
18.8145765783248));
#25652=CARTESIAN_POINT('Ctrl Pts',(-3.36796573513472,-0.00233887403243996,
18.848589891905));
#25653=CARTESIAN_POINT('Origin',(0.,0.,-1.84858989190503));
#25654=CARTESIAN_POINT('',(-3.37277477193024,-0.0030073171892592,16.651410108095));
#25655=CARTESIAN_POINT('',(-3.37676993930056,0.00122898291704077,16.848589891905));
#25656=CARTESIAN_POINT('',(-3.37175,2.08693528006523E-13,-1.84858989190503));
#25657=CARTESIAN_POINT('Ctrl Pts',(-3.37277477193024,-0.0030073171892591,
16.651410108095));
#25658=CARTESIAN_POINT('Ctrl Pts',(-3.3748752325093,-0.230456048008689,
16.6621578139988));
#25659=CARTESIAN_POINT('Ctrl Pts',(-3.25015286697033,-1.5764664391,16.7258694983973));
#25660=CARTESIAN_POINT('Ctrl Pts',(-1.44097876042837,-3.71672329068694,
16.8425451612903));
#25661=CARTESIAN_POINT('Ctrl Pts',(2.34362517346463,-3.22457328244272,17.0014370967742));
#25662=CARTESIAN_POINT('Ctrl Pts',(3.980025336833,0.223271417131382,17.1603290322581));
#25663=CARTESIAN_POINT('Ctrl Pts',(1.96827154957251,3.46646201691059,17.3192209677419));
#25664=CARTESIAN_POINT('Ctrl Pts',(-1.84763096082072,3.53223889907763,17.4781129032258));
#25665=CARTESIAN_POINT('Ctrl Pts',(-3.32665838484882,1.32176305576882,17.5888426166768));
#25666=CARTESIAN_POINT('Ctrl Pts',(-3.3767974954359,0.103119423021283,17.6466083516332));
#25667=CARTESIAN_POINT('Ctrl Pts',(-3.3761529784003,0.00176635805113214,
17.651410108095));
#25668=CARTESIAN_POINT('Ctrl Pts',(-3.37676993930056,0.00122898291704094,
16.848589891905));
#25669=CARTESIAN_POINT('Ctrl Pts',(-3.37185165056191,-1.0490400428621,16.8983720689807));
#25670=CARTESIAN_POINT('Ctrl Pts',(-2.28032799824397,-3.22603625281427,
17.0011425347847));
#25671=CARTESIAN_POINT('Ctrl Pts',(1.42826443406275,-3.7222894112013,17.1569012893169));
#25672=CARTESIAN_POINT('Ctrl Pts',(3.90292376012977,-0.813980268166524,
17.3158661555016));
#25673=CARTESIAN_POINT('Ctrl Pts',(2.79709452794753,2.84106317354542,17.4748310216864));
#25674=CARTESIAN_POINT('Ctrl Pts',(-0.87475073969136,3.88975434928213,17.6337958878711));
#25675=CARTESIAN_POINT('Ctrl Pts',(-3.12356865319579,1.91496539554474,17.758382177944));
#25676=CARTESIAN_POINT('Ctrl Pts',(-3.37075124816507,0.397630825661392,
17.8299801792886));
#25677=CARTESIAN_POINT('Ctrl Pts',(-3.36813340603362,0.00242210091315778,
17.848589891905));
#25678=CARTESIAN_POINT('Origin',(0.,0.,-1.84858989190503));
#25679=CARTESIAN_POINT('',(-3.36620324934232,-6.47284927745773E-5,15.651410108095));
#25680=CARTESIAN_POINT('',(-3.37184361771993,-0.00309624629213801,15.848589891905));
#25681=CARTESIAN_POINT('',(-3.37175,2.08693528006523E-13,-1.84858989190503));
#25682=CARTESIAN_POINT('Ctrl Pts',(-3.36620324934232,-6.47284927745434E-5,
15.651410108095));
#25683=CARTESIAN_POINT('Ctrl Pts',(-3.36629886637731,-0.559331950050314,
15.6777072763644));
#25684=CARTESIAN_POINT('Ctrl Pts',(-2.969304704679,-2.24486717295088,15.7569684231284));
#25685=CARTESIAN_POINT('Ctrl Pts',(-0.30568234557457,-3.97454527098943,
15.8891935483871));
#25686=CARTESIAN_POINT('Ctrl Pts',(3.17532551476257,-2.40992939374543,16.048085483871));
#25687=CARTESIAN_POINT('Ctrl Pts',(3.74577996379122,1.36366574731522,16.2069774193548));
#25688=CARTESIAN_POINT('Ctrl Pts',(0.882793462927545,3.88730337243608,16.3658693548387));
#25689=CARTESIAN_POINT('Ctrl Pts',(-2.54098403241842,2.91809266432718,16.5140135844188));
#25690=CARTESIAN_POINT('Ctrl Pts',(-3.36452430274498,0.890396140872364,
16.6091938355042));
#25691=CARTESIAN_POINT('Ctrl Pts',(-3.37277477193024,-0.0030073171892591,
16.651410108095));
#25692=CARTESIAN_POINT('Ctrl Pts',(-3.37184361771993,-0.00309624629213769,
15.848589891905));
#25693=CARTESIAN_POINT('Ctrl Pts',(-3.37422938253555,-0.261408813023958,
15.8607873812163));
#25694=CARTESIAN_POINT('Ctrl Pts',(-3.22903130121081,-1.63922767409008,
15.9259731592558));
#25695=CARTESIAN_POINT('Ctrl Pts',(-1.33737014962086,-3.75590452983738,
16.0441472260236));
#25696=CARTESIAN_POINT('Ctrl Pts',(2.43413116992486,-3.15759136082396,16.2031120922084));
#25697=CARTESIAN_POINT('Ctrl Pts',(3.97259404474729,0.337452678146523,16.3620769583931));
#25698=CARTESIAN_POINT('Ctrl Pts',(1.86665380078734,3.52292227310739,16.5210418245779));
#25699=CARTESIAN_POINT('Ctrl Pts',(-1.95172895721992,3.47651144567355,16.6800066907626));
#25700=CARTESIAN_POINT('Ctrl Pts',(-3.34455787065121,1.25410828714709,16.7891893798717));
#25701=CARTESIAN_POINT('Ctrl Pts',(-3.37708669087234,0.0688692501706657,
16.8453837802525));
#25702=CARTESIAN_POINT('Ctrl Pts',(-3.37676993930056,0.00122898291704094,
16.848589891905));
#25703=CARTESIAN_POINT('Origin',(0.,0.,-1.84858989190503));
#25704=CARTESIAN_POINT('',(-3.37253669875649,0.00303677565441225,14.651410108095));
#25705=CARTESIAN_POINT('',(-3.36623102492646,0.000387483300791081,14.848589891905));
#25706=CARTESIAN_POINT('',(-3.37175,2.08693528006523E-13,-1.84858989190503));
#25707=CARTESIAN_POINT('Ctrl Pts',(-3.37253669875649,0.00303677565441206,
14.651410108095));
#25708=CARTESIAN_POINT('Ctrl Pts',(-3.36433888251516,-0.882704764956481,
14.69325673873));
#25709=CARTESIAN_POINT('Ctrl Pts',(-2.55272847437535,-2.90279523765218,
14.7880673478596));
#25710=CARTESIAN_POINT('Ctrl Pts',(0.8556871302199,-3.8933599040824,14.9358419354839));
#25711=CARTESIAN_POINT('Ctrl Pts',(3.73618765800463,-1.38973148187494,15.0947338709677));
#25712=CARTESIAN_POINT('Ctrl Pts',(3.19203969455987,2.38774671937678,15.2536258064516));
#25713=CARTESIAN_POINT('Ctrl Pts',(-0.277982160818163,3.97657864574653,
15.4125177419355));
#25714=CARTESIAN_POINT('Ctrl Pts',(-2.9610712487067,2.26071800063538,15.54511250915));
#25715=CARTESIAN_POINT('Ctrl Pts',(-3.3661062882817,0.567063743655371,15.6247432978698));
#25716=CARTESIAN_POINT('Ctrl Pts',(-3.36620324934232,-6.47284927745434E-5,
15.651410108095));
#25717=CARTESIAN_POINT('Ctrl Pts',(-3.36623102492646,0.000387483300790976,
14.848589891905));
#25718=CARTESIAN_POINT('Ctrl Pts',(-3.36563039823437,-0.58659786734821,
14.8761909821801));
#25719=CARTESIAN_POINT('Ctrl Pts',(-2.93982168940875,-2.30128717837213,
14.9567803611835));
#25720=CARTESIAN_POINT('Ctrl Pts',(-0.206119829211681,-3.98156908396121,
15.0903580289152));
#25721=CARTESIAN_POINT('Ctrl Pts',(3.23622917375625,-2.32856146349605,15.2493228950999));
#25722=CARTESIAN_POINT('Ctrl Pts',(3.70970605913983,1.46063640552025,15.4082877612846));
#25723=CARTESIAN_POINT('Ctrl Pts',(0.779949646731194,3.90986653262151,15.5672526274694));
#25724=CARTESIAN_POINT('Ctrl Pts',(-2.58561751919903,2.85952988987219,15.7140200043429));
#25725=CARTESIAN_POINT('Ctrl Pts',(-3.36386515169579,0.8607517004072,15.8077990924881));
#25726=CARTESIAN_POINT('Ctrl Pts',(-3.37184361771993,-0.00309624629213769,
15.848589891905));
#25727=CARTESIAN_POINT('Origin',(0.,0.,-1.84858989190503));
#25728=CARTESIAN_POINT('',(-3.37630962516523,-0.00164737155311467,13.651410108095));
#25729=CARTESIAN_POINT('',(-3.37326960455653,0.00293423317535069,13.848589891905));
#25730=CARTESIAN_POINT('',(-3.37175,2.08693528006523E-13,-1.84858989190503));
#25731=CARTESIAN_POINT('Ctrl Pts',(-3.37630962516523,-0.00164737155311456,
13.651410108095));
#25732=CARTESIAN_POINT('Ctrl Pts',(-3.3768714611022,-0.0951867578458431,
13.6558422226009));
#25733=CARTESIAN_POINT('Ctrl Pts',(-3.33090125004588,-1.30596569148795,
13.7132383156015));
#25734=CARTESIAN_POINT('Ctrl Pts',(-1.87219709398698,-3.51927973437849,
13.8235983870968));
#25735=CARTESIAN_POINT('Ctrl Pts',(1.94407109338865,-3.48009186536664,13.9824903225806));
#25736=CARTESIAN_POINT('Ctrl Pts',(3.97837307717912,-0.25099694483561,14.1413822580645));
#25737=CARTESIAN_POINT('Ctrl Pts',(2.36603559757979,3.20816573115008,14.3002741935484));
#25738=CARTESIAN_POINT('Ctrl Pts',(-1.41504740048591,3.7266731359107,14.4591661290323));
#25739=CARTESIAN_POINT('Ctrl Pts',(-3.24486867351568,1.59233323105557,14.5762114338811));
#25740=CARTESIAN_POINT('Ctrl Pts',(-3.37471460348768,0.238350746486947,
14.6402927602354));
#25741=CARTESIAN_POINT('Ctrl Pts',(-3.37253669875649,0.00303677565441206,
14.651410108095));
#25742=CARTESIAN_POINT('Ctrl Pts',(-3.37326960455653,0.00293423317535065,
13.848589891905));
#25743=CARTESIAN_POINT('Ctrl Pts',(-3.36494392394814,-0.906810168463347,
13.891594583144));
#25744=CARTESIAN_POINT('Ctrl Pts',(-2.51545460624217,-2.95119723051152,
13.9875875631112));
#25745=CARTESIAN_POINT('Ctrl Pts',(0.942385426660244,-3.87392403926152,
14.1365688318067));
#25746=CARTESIAN_POINT('Ctrl Pts',(3.76741231340739,-1.30460040439068,14.2955336979914));
#25747=CARTESIAN_POINT('Ctrl Pts',(3.1362669786623,2.46154569181692,14.4544985641762));
#25748=CARTESIAN_POINT('Ctrl Pts',(-0.372046531241306,3.96950363810656,
14.6134634303609));
#25749=CARTESIAN_POINT('Ctrl Pts',(-2.98916250729706,2.20635255558199,14.7448272062705));
#25750=CARTESIAN_POINT('Ctrl Pts',(-3.36678347516941,0.540290560949759,
14.8232026934519));
#25751=CARTESIAN_POINT('Ctrl Pts',(-3.36623102492646,0.000387483300790976,
14.848589891905));
#25752=CARTESIAN_POINT('Origin',(0.,0.,-1.84858989190503));
#25753=CARTESIAN_POINT('',(-3.36754256765694,-0.00208193686516585,12.651410108095));
#25754=CARTESIAN_POINT('',(-3.3758812610584,-0.00196014188030613,12.848589891905));
#25755=CARTESIAN_POINT('',(-3.37175,2.08693528006523E-13,-1.84858989190503));
#25756=CARTESIAN_POINT('Ctrl Pts',(-3.36754256765694,-0.00208193686516537,
12.651410108095));
#25757=CARTESIAN_POINT('Ctrl Pts',(-3.36993408573054,-0.426611763038696,
12.6713916849665));
#25758=CARTESIAN_POINT('Ctrl Pts',(-3.09838828538505,-1.97347045721629,
12.7443372403327));
#25759=CARTESIAN_POINT('Ctrl Pts',(-0.775556132376715,-3.9101105474236,
12.8702467741936));
#25760=CARTESIAN_POINT('Ctrl Pts',(2.86663624227273,-2.76999069710151,13.0291387096774));
#25761=CARTESIAN_POINT('Ctrl Pts',(3.88122465785174,0.909146282412278,13.1880306451613));
#25762=CARTESIAN_POINT('Ctrl Pts',(1.33822138229676,3.75494545093591,13.3469225806451));
#25763=CARTESIAN_POINT('Ctrl Pts',(-2.32626682514693,3.17552839905125,13.5013824016231));
#25764=CARTESIAN_POINT('Ctrl Pts',(-3.37015749501604,1.02261334351231,13.6028782441063));
#25765=CARTESIAN_POINT('Ctrl Pts',(-3.37630962516523,-0.00164737155311456,
13.651410108095));
#25766=CARTESIAN_POINT('Ctrl Pts',(-3.3758812610584,-0.00196014188030577,
12.848589891905));
#25767=CARTESIAN_POINT('Ctrl Pts',(-3.37667181942981,-0.11638712350615,
12.8540098953796));
#25768=CARTESIAN_POINT('Ctrl Pts',(-3.31942395404611,-1.34870119310656,
12.9124181875824));
#25769=CARTESIAN_POINT('Ctrl Pts',(-1.80499399926681,-3.5549084962852,13.0238147685134));
#25770=CARTESIAN_POINT('Ctrl Pts',(2.01200065152342,-3.44198069904803,13.1827796346982));
#25771=CARTESIAN_POINT('Ctrl Pts',(3.98321358718988,-0.171427165804589,
13.3417445008829));
#25772=CARTESIAN_POINT('Ctrl Pts',(2.30028118194861,3.25639129072706,13.5007093670677));
#25773=CARTESIAN_POINT('Ctrl Pts',(-1.49289753065309,3.69684118097057,13.6596742332524));
#25774=CARTESIAN_POINT('Ctrl Pts',(-3.26085313565002,1.54418744509758,13.7756344081982));
#25775=CARTESIAN_POINT('Ctrl Pts',(-3.37520242261949,0.214132631825097,
13.8386062944157));
#25776=CARTESIAN_POINT('Ctrl Pts',(-3.37326960455653,0.00293423317535065,
13.848589891905));
#25777=CARTESIAN_POINT('Origin',(0.,0.,-1.84858989190503));
#25778=CARTESIAN_POINT('',(-3.36871665678573,0.00265343926576773,11.651410108095));
#25779=CARTESIAN_POINT('',(-3.36722041330275,-0.00185992061757206,11.848589891905));
#25780=CARTESIAN_POINT('',(-3.37175,2.08693528006523E-13,-1.84858989190503));
#25781=CARTESIAN_POINT('Ctrl Pts',(-3.36871665678573,0.00265343926576761,
11.651410108095));
#25782=CARTESIAN_POINT('Ctrl Pts',(-3.36317444447066,-0.751580168678052,
11.6869411473321));
#25783=CARTESIAN_POINT('Ctrl Pts',(-2.7398020033052,-2.63841079513441,11.7754361650639));
#25784=CARTESIAN_POINT('Ctrl Pts',(0.38723559847199,-3.96742994882286,11.9168951612903));
#25785=CARTESIAN_POINT('Ctrl Pts',(3.54469272874429,-1.82362421192741,12.0757870967742));
#25786=CARTESIAN_POINT('Ctrl Pts',(3.45302863798842,1.9917442187119,12.2346790322581));
#25787=CARTESIAN_POINT('Ctrl Pts',(0.196264076456207,3.98144850774605,12.3935709677419));
#25788=CARTESIAN_POINT('Ctrl Pts',(-2.80821900811,2.53041799939006,12.5324813263542));
#25789=CARTESIAN_POINT('Ctrl Pts',(-3.36359503087846,0.698664221349558,
12.6184277064719));
#25790=CARTESIAN_POINT('Ctrl Pts',(-3.36754256765694,-0.00208193686516537,
12.651410108095));
#25791=CARTESIAN_POINT('Ctrl Pts',(-3.36722041330275,-0.00185992061757217,
11.848589891905));
#25792=CARTESIAN_POINT('Ctrl Pts',(-3.36943251646156,-0.444385182068521,
11.8694134963434));
#25793=CARTESIAN_POINT('Ctrl Pts',(-3.08234983495276,-2.01021544013623,
11.9432253895101));
#25794=CARTESIAN_POINT('Ctrl Pts',(-0.711713421966334,-3.92286142494773,
12.0700255714049));
#25795=CARTESIAN_POINT('Ctrl Pts',(2.91318501009988,-2.72189839106446,12.2289904375897));
#25796=CARTESIAN_POINT('Ctrl Pts',(3.86556759564105,0.976096776902648,12.3879553037744));
#25797=CARTESIAN_POINT('Ctrl Pts',(1.27173165426137,3.77863419159615,12.5469201699592));
#25798=CARTESIAN_POINT('Ctrl Pts',(-2.36055670961755,3.13734167043916,12.7004650326694));
#25799=CARTESIAN_POINT('Ctrl Pts',(-3.36894298024411,1.00230034028648,12.8010216066513));
#25800=CARTESIAN_POINT('Ctrl Pts',(-3.3758812610584,-0.00196014188030577,
12.848589891905));
#25801=CARTESIAN_POINT('Origin',(0.,0.,-1.84858989190503));
#25802=CARTESIAN_POINT('',(-3.37710546106046,0.000736094683953019,10.651410108095));
#25803=CARTESIAN_POINT('',(-3.36907238740032,0.00277677980771746,10.848589891905));
#25804=CARTESIAN_POINT('',(-3.37175,2.08693528006523E-13,-1.84858989190503));
#25805=CARTESIAN_POINT('Ctrl Pts',(-3.37710546106046,0.000736094683952996,
10.651410108095));
#25806=CARTESIAN_POINT('Ctrl Pts',(-3.37391321273993,-1.07663815669567,
10.7024906096977));
#25807=CARTESIAN_POINT('Ctrl Pts',(-2.23194165802167,-3.27693130018453,
10.8065350897951));
#25808=CARTESIAN_POINT('Ctrl Pts',(1.51699821428175,-3.68634890174633,10.9635435483871));
#25809=CARTESIAN_POINT('Ctrl Pts',(3.92040597926993,-0.721712384018116,
11.122435483871));
#25810=CARTESIAN_POINT('Ctrl Pts',(2.73030783639792,2.90445707939446,11.2813274193548));
#25811=CARTESIAN_POINT('Ctrl Pts',(-0.962433500126168,3.86835540835836,
11.4402193548387));
#25812=CARTESIAN_POINT('Ctrl Pts',(-3.1445024192473,1.86381595651157,11.5635802510854));
#25813=CARTESIAN_POINT('Ctrl Pts',(-3.37143588630209,0.372710407919653,
11.6339771688375));
#25814=CARTESIAN_POINT('Ctrl Pts',(-3.36871665678573,0.00265343926576761,
11.651410108095));
#25815=CARTESIAN_POINT('Ctrl Pts',(-3.36907238740032,0.00277677980771742,
10.848589891905));
#25816=CARTESIAN_POINT('Ctrl Pts',(-3.36312082444251,-0.766029392039194,
10.8848170973072));
#25817=CARTESIAN_POINT('Ctrl Pts',(-2.72027913252513,-2.66834094208117,
10.9740325914377));
#25818=CARTESIAN_POINT('Ctrl Pts',(0.441146911493231,-3.96241935650807,
11.1162363742964));
#25819=CARTESIAN_POINT('Ctrl Pts',(3.57049754163045,-1.77395745708877,11.2752012404812));
#25820=CARTESIAN_POINT('Ctrl Pts',(3.42432285260543,2.04190860605321,11.4341661066659));
#25821=CARTESIAN_POINT('Ctrl Pts',(0.136721492950909,3.98455580808139,11.5931309728507));
#25822=CARTESIAN_POINT('Ctrl Pts',(-2.82921667119627,2.49618535096433,11.7312722345971));
#25823=CARTESIAN_POINT('Ctrl Pts',(-3.36380354088135,0.681676177418306,
11.8164252076152));
#25824=CARTESIAN_POINT('Ctrl Pts',(-3.36722041330275,-0.00185992061757217,
11.848589891905));
#25825=CARTESIAN_POINT('Origin',(0.,0.,-1.84858989190503));
#25826=CARTESIAN_POINT('',(-3.37090359896229,-0.00307926823583696,9.65141010809498));
#25827=CARTESIAN_POINT('',(-3.37720911693329,0.000534521222638907,9.84858989190502));
#25828=CARTESIAN_POINT('',(-3.37175,2.08693528006523E-13,-1.84858989190503));
#25829=CARTESIAN_POINT('Ctrl Pts',(-3.37090359896229,-0.0030792682358368,
9.65141010809498));
#25830=CARTESIAN_POINT('Ctrl Pts',(-3.37349992290045,-0.292697043198134,
9.6650760935687));
#25831=CARTESIAN_POINT('Ctrl Pts',(-3.20668744219234,-1.70181407180786,
9.73170605753704));
#25832=CARTESIAN_POINT('Ctrl Pts',(-1.23445173354738,-3.79032725830928,
9.85129999999999));
#25833=CARTESIAN_POINT('Ctrl Pts',(2.51736903674626,-3.09084210861242,10.0101919354839));
#25834=CARTESIAN_POINT('Ctrl Pts',(3.96172967315432,0.441757630821415,10.1690838709677));
#25835=CARTESIAN_POINT('Ctrl Pts',(1.77470645260886,3.56943536355667,10.3279758064516));
#25836=CARTESIAN_POINT('Ctrl Pts',(-2.03904067252446,3.42531238624034,10.4868677419355));
#25837=CARTESIAN_POINT('Ctrl Pts',(-3.35858003390563,1.1971743885357,10.5946791758166));
#25838=CARTESIAN_POINT('Ctrl Pts',(-3.37722316793013,0.0404618108125119,
10.6495266312031));
#25839=CARTESIAN_POINT('Ctrl Pts',(-3.37710546106046,0.000736094683952996,
10.651410108095));
#25840=CARTESIAN_POINT('Ctrl Pts',(-3.37720911693329,0.000534521222638742,
9.84858989190502));
#25841=CARTESIAN_POINT('Ctrl Pts',(-3.37481325646777,-1.08835732049462,
9.90022069827108));
#25842=CARTESIAN_POINT('Ctrl Pts',(-2.21074657312113,-3.29916896326091,
10.0048397933654));
#25843=CARTESIAN_POINT('Ctrl Pts',(1.55707745747673,-3.67027077281332,10.1624471771879));
#25844=CARTESIAN_POINT('Ctrl Pts',(3.928912558612,-0.677512997019795,10.3214120433727));
#25845=CARTESIAN_POINT('Ctrl Pts',(2.69641733534343,2.93678588051791,10.4803769095574));
#25846=CARTESIAN_POINT('Ctrl Pts',(-1.00973405207762,3.8569177977272,10.6393417757422));
#25847=CARTESIAN_POINT('Ctrl Pts',(-3.15606037844699,1.83542847981608,10.7620794365247));
#25848=CARTESIAN_POINT('Ctrl Pts',(-3.37182597111036,0.358476982592217,
10.831828808579));
#25849=CARTESIAN_POINT('Ctrl Pts',(-3.36907238740032,0.00277677980771742,
10.848589891905));
#25850=CARTESIAN_POINT('Origin',(0.,0.,-1.84858989190503));
#25851=CARTESIAN_POINT('',(-3.36644585084492,0.000942668595409863,8.65141010809498));
#25852=CARTESIAN_POINT('',(-3.37066808100933,-0.00306963188584058,8.84858989190501));
#25853=CARTESIAN_POINT('',(-3.37175,2.08693528006523E-13,-1.84858989190503));
#25854=CARTESIAN_POINT('Ctrl Pts',(-3.36644585084492,0.000942668595410034,
8.65141010809498));
#25855=CARTESIAN_POINT('Ctrl Pts',(-3.36489256340397,-0.620276501159167,
8.68062555593429));
#25856=CARTESIAN_POINT('Ctrl Pts',(-2.90218694538986,-2.36984060140867,
8.76280498226821));
#25857=CARTESIAN_POINT('Ctrl Pts',(-0.086697347329244,-3.9853400579507,
8.89794838709678));
#25858=CARTESIAN_POINT('Ctrl Pts',(3.30302181201077,-2.23170309784288,9.05684032258065));
#25859=CARTESIAN_POINT('Ctrl Pts',(3.66513912143678,1.56754809433529,9.21573225806451));
#25860=CARTESIAN_POINT('Ctrl Pts',(0.667732148006428,3.92995999802278,9.3746241935484));
#25861=CARTESIAN_POINT('Ctrl Pts',(-2.63128595375923,2.79674582771393,9.51985014355854));
#25862=CARTESIAN_POINT('Ctrl Pts',(-3.36343759366045,0.829747410900375,
9.61211211507407));
#25863=CARTESIAN_POINT('Ctrl Pts',(-3.37090359896229,-0.0030792682358368,
9.65141010809498));
#25864=CARTESIAN_POINT('Ctrl Pts',(-3.37066808100933,-0.0030696318858409,
8.84858989190502));
#25865=CARTESIAN_POINT('Ctrl Pts',(-3.37331082414,-0.300796169438093,8.86263601050667));
#25866=CARTESIAN_POINT('Ctrl Pts',(-3.20068977672434,-1.71866740211794,
8.92967041783657));
#25867=CARTESIAN_POINT('Ctrl Pts',(-1.20570712414377,-3.80021684712055,
9.04969311389473));
#25868=CARTESIAN_POINT('Ctrl Pts',(2.54266018034211,-3.07087234538534,9.20865798007948));
#25869=CARTESIAN_POINT('Ctrl Pts',(3.95842601916979,0.47564819468749,9.36762284626423));
#25870=CARTESIAN_POINT('Ctrl Pts',(1.74278629094578,3.58581562527152,9.52658771244896));
#25871=CARTESIAN_POINT('Ctrl Pts',(-2.07166160205713,3.40640513751843,9.68555257863373));
#25872=CARTESIAN_POINT('Ctrl Pts',(-3.36396169301834,1.17525404838138,9.7928866384524));
#25873=CARTESIAN_POINT('Ctrl Pts',(-3.377272109138,0.0291637752183697,9.84723240954283));
#25874=CARTESIAN_POINT('Ctrl Pts',(-3.37720911693329,0.000534521222638742,
9.84858989190502));
#25875=CARTESIAN_POINT('Origin',(0.,0.,-1.84858989190503));
#25876=CARTESIAN_POINT('',(-3.37436653161969,0.00264543560195785,7.65141010809498));
#25877=CARTESIAN_POINT('',(-3.36647579863201,0.00101859643942465,7.84858989190502));
#25878=CARTESIAN_POINT('',(-3.37175,2.08693528006523E-13,-1.84858989190503));
#25879=CARTESIAN_POINT('Ctrl Pts',(-3.37436653161969,0.00264543560195811,
7.65141010809498));
#25880=CARTESIAN_POINT('Ctrl Pts',(-3.36621424622869,-0.943539301975876,
7.69617501829988));
#25881=CARTESIAN_POINT('Ctrl Pts',(-2.45755376938072,-3.02292340440546,
7.7939039069994));
#25882=CARTESIAN_POINT('Ctrl Pts',(1.06845185659111,-3.84042477308012,7.94459677419355));
#25883=CARTESIAN_POINT('Ctrl Pts',(3.80694458147109,-1.18221180891932,8.10348870967742));
#25884=CARTESIAN_POINT('Ctrl Pts',(3.0559319039131,2.55963513145653,8.2623806451613));
#25885=CARTESIAN_POINT('Ctrl Pts',(-0.49619611955484,3.95528016940384,8.42127258064515));
#25886=CARTESIAN_POINT('Ctrl Pts',(-3.02400139141134,2.13545120331948,8.55094906828973));
#25887=CARTESIAN_POINT('Ctrl Pts',(-3.36770848062251,0.505916700748885,
8.62766157743967));
#25888=CARTESIAN_POINT('Ctrl Pts',(-3.36644585084492,0.000942668595410034,
8.65141010809498));
#25889=CARTESIAN_POINT('Ctrl Pts',(-3.36647579863201,0.00101859643942433,
7.84858989190502));
#25890=CARTESIAN_POINT('Ctrl Pts',(-3.36478428770786,-0.625167485996831,
7.87803961147051));
#25891=CARTESIAN_POINT('Ctrl Pts',(-2.8964828528491,-2.38038813746449,7.96047761976425));
#25892=CARTESIAN_POINT('Ctrl Pts',(-0.0672816548149041,-3.98633301836102,
8.09590391678625));
#25893=CARTESIAN_POINT('Ctrl Pts',(3.31538886833258,-2.21440159096907,8.25486878297098));
#25894=CARTESIAN_POINT('Ctrl Pts',(3.65656725922866,1.58899138861319,8.41383364915575));
#25895=CARTESIAN_POINT('Ctrl Pts',(0.643261156248369,3.93466553079316,8.57279851534047));
#25896=CARTESIAN_POINT('Ctrl Pts',(-2.64176562949924,2.78241271369441,8.71771726292358));
#25897=CARTESIAN_POINT('Ctrl Pts',(-3.36334120619684,0.822362489639698,
8.80964772177842));
#25898=CARTESIAN_POINT('Ctrl Pts',(-3.37066808100933,-0.0030696318858409,
8.84858989190502));
#25899=CARTESIAN_POINT('Origin',(0.,0.,-1.84858989190503));
#25900=CARTESIAN_POINT('',(-3.3748606436688,-0.00246557707590639,6.65141010809498));
#25901=CARTESIAN_POINT('',(-3.37441250761161,0.00263846066578283,6.84858989190502));
#25902=CARTESIAN_POINT('',(-3.37175,2.08693528006523E-13,-1.84858989190503));
#25903=CARTESIAN_POINT('Ctrl Pts',(-3.3748606436688,-0.00246557707590626,
6.65141010809497));
#25904=CARTESIAN_POINT('Ctrl Pts',(-3.37613613582624,-0.157769830059076,
6.65876050217084));
#25905=CARTESIAN_POINT('Ctrl Pts',(-3.29579272315184,-1.43080711580639,
6.71907487474133));
#25906=CARTESIAN_POINT('Ctrl Pts',(-1.67587337027072,-3.61689096522939,
6.83235322580646));
#25907=CARTESIAN_POINT('Ctrl Pts',(2.13246786040229,-3.36794189853266,6.99124516129032));
#25908=CARTESIAN_POINT('Ctrl Pts',(3.98615544163244,-0.0318842074478251,
7.15013709677419));
#25909=CARTESIAN_POINT('Ctrl Pts',(2.18607012156152,3.33339905069232,7.30902903225807));
#25910=CARTESIAN_POINT('Ctrl Pts',(-1.61780152532516,3.64323620318475,7.46792096774193));
#25911=CARTESIAN_POINT('Ctrl Pts',(-3.28487995770484,1.46716325720085,7.58204799302091));
#25912=CARTESIAN_POINT('Ctrl Pts',(-3.37585969097893,0.175947096268433,
7.64321103980526));
#25913=CARTESIAN_POINT('Ctrl Pts',(-3.37436653161969,0.00264543560195811,
7.65141010809498));
#25914=CARTESIAN_POINT('Ctrl Pts',(-3.37441250761161,0.00263846066578258,
6.84858989190502));
#25915=CARTESIAN_POINT('Ctrl Pts',(-3.36625911376211,-0.945381294583835,
6.89344321243435));
#25916=CARTESIAN_POINT('Ctrl Pts',(-2.45439078883877,-3.02709322103295,
6.99128482169193));
#25917=CARTESIAN_POINT('Ctrl Pts',(1.07677617223565,-3.83874078693202,7.14211471967776));
#25918=CARTESIAN_POINT('Ctrl Pts',(3.81057598656871,-1.17255635469506,7.3010795858625));
#25919=CARTESIAN_POINT('Ctrl Pts',(3.04860581952888,2.56931514444696,7.46004445204726));
#25920=CARTESIAN_POINT('Ctrl Pts',(-0.510113381387115,3.95413228059959,
7.619009318232));
#25921=CARTESIAN_POINT('Ctrl Pts',(-3.02827174132543,2.12695452322279,7.74852446485126));
#25922=CARTESIAN_POINT('Ctrl Pts',(-3.36782778932888,0.501516551178981,
7.82505132274226));
#25923=CARTESIAN_POINT('Ctrl Pts',(-3.36647579863201,0.00101859643942433,
7.84858989190502));
#25924=CARTESIAN_POINT('Origin',(0.,0.,-1.84858989190503));
#25925=CARTESIAN_POINT('',(-3.36661890683212,-0.00122158962200572,5.65141010809498));
#25926=CARTESIAN_POINT('',(-3.37491538366506,-0.00245188971244759,5.84858989190502));
#25927=CARTESIAN_POINT('',(-3.37175,2.08693528006523E-13,-1.84858989190503));
#25928=CARTESIAN_POINT('Ctrl Pts',(-3.36661890683212,-0.00122158962200539,
5.65141010809498));
#25929=CARTESIAN_POINT('Ctrl Pts',(-3.36820126338182,-0.488087448628749,
5.67430996453643));
#25930=CARTESIAN_POINT('Ctrl Pts',(-3.04142339082007,-2.09897775501084,
5.75017379947252));
#25931=CARTESIAN_POINT('Ctrl Pts',(-0.559403071098495,-3.94683670951677,
5.87900161290323));
#25932=CARTESIAN_POINT('Ctrl Pts',(3.01459581839321,-2.60819168376593,6.03789354838709));
#25933=CARTESIAN_POINT('Ctrl Pts',(3.82536866943663,1.12116294553142,6.19678548387097));
#25934=CARTESIAN_POINT('Ctrl Pts',(1.12974830864147,3.82284194895142,6.35567741935484));
#25935=CARTESIAN_POINT('Ctrl Pts',(-2.42881219485455,3.0575629803579,6.50721896076285));
#25936=CARTESIAN_POINT('Ctrl Pts',(-3.3669454531908,0.961290050298803,6.60579652367622));
#25937=CARTESIAN_POINT('Ctrl Pts',(-3.3748606436688,-0.00246557707590626,
6.65141010809497));
#25938=CARTESIAN_POINT('Ctrl Pts',(-3.37491538366506,-0.00245188971244781,
5.84858989190502));
#25939=CARTESIAN_POINT('Ctrl Pts',(-3.37617143803668,-0.156022125643285,
5.85585852466994));
#25940=CARTESIAN_POINT('Ctrl Pts',(-3.29681403413222,-1.42781289481916,
5.91611544616311));
#25941=CARTESIAN_POINT('Ctrl Pts',(-1.68004955900417,-3.61563427819245,
6.02936065638453));
#25942=CARTESIAN_POINT('Ctrl Pts',(2.13069369871068,-3.3697955600636,6.18832552256926));
#25943=CARTESIAN_POINT('Ctrl Pts',(3.98676787287831,-0.032552759256669,
6.34729038875402));
#25944=CARTESIAN_POINT('Ctrl Pts',(2.18543605335013,3.3345534950076,6.50625525493876));
#25945=CARTESIAN_POINT('Ctrl Pts',(-1.62078473268592,3.64258625218979,6.66522012112352));
#25946=CARTESIAN_POINT('Ctrl Pts',(-3.2856992999535,1.4649244081245,6.77933166677893));
#25947=CARTESIAN_POINT('Ctrl Pts',(-3.37589127437617,0.174579143538081,
6.8404549237061));
#25948=CARTESIAN_POINT('Ctrl Pts',(-3.37441250761161,0.00263846066578258,
6.84858989190502));
#25949=CARTESIAN_POINT('Origin',(0.,0.,-1.84858989190503));
#25950=CARTESIAN_POINT('',(-3.37037732776107,0.00303222645661923,4.65141010809497));
#25951=CARTESIAN_POINT('',(-3.36666513788771,-0.00130109466394523,4.84858989190502));
#25952=CARTESIAN_POINT('',(-3.37175,2.08693528006523E-13,-1.84858989190503));
#25953=CARTESIAN_POINT('Ctrl Pts',(-3.37037732776107,0.00303222645661912,
4.65141010809497));
#25954=CARTESIAN_POINT('Ctrl Pts',(-3.36327434274459,-0.812132332425157,
4.68985942690203));
#25955=CARTESIAN_POINT('Ctrl Pts',(-2.65651681547025,-2.76122659154967,
4.7812727242037));
#25956=CARTESIAN_POINT('Ctrl Pts',(0.604781303071069,-3.94013849796468,
4.92565));
#25957=CARTESIAN_POINT('Ctrl Pts',(3.63959495745868,-1.6259767381985,5.08454193548388));
#25958=CARTESIAN_POINT('Ctrl Pts',(3.3382985122726,2.17858092584818,5.24343387096774));
#25959=CARTESIAN_POINT('Ctrl Pts',(-0.0229349622598251,3.98621697792136,
5.40232580645161));
#25960=CARTESIAN_POINT('Ctrl Pts',(-2.88174731779988,2.40610117021057,5.53831788549402));
#25961=CARTESIAN_POINT('Ctrl Pts',(-3.36454150689018,0.637961221244742,
5.62134598604181));
#25962=CARTESIAN_POINT('Ctrl Pts',(-3.36661890683212,-0.00122158962200539,
5.65141010809498));
#25963=CARTESIAN_POINT('Ctrl Pts',(-3.36666513788771,-0.00130109466394548,
4.84858989190502));
#25964=CARTESIAN_POINT('Ctrl Pts',(-3.36833385037662,-0.483310565759833,
4.87126212563378));
#25965=CARTESIAN_POINT('Ctrl Pts',(-3.04595737613669,-2.0897168735396,4.94692264809078));
#25966=CARTESIAN_POINT('Ctrl Pts',(-0.574613628296617,-3.94527526701846,
5.07557145927603));
#25967=CARTESIAN_POINT('Ctrl Pts',(3.0062441927532,-2.61875420913902,5.2345363254608));
#25968=CARTESIAN_POINT('Ctrl Pts',(3.8292149534867,1.11017592945447,5.39350119164552));
#25969=CARTESIAN_POINT('Ctrl Pts',(1.13931660104628,3.82064594498541,5.55246605783029));
#25970=CARTESIAN_POINT('Ctrl Pts',(-2.42498889622798,3.06243800957472,5.7041622912501));
#25971=CARTESIAN_POINT('Ctrl Pts',(-3.36701480929308,0.963503961964746,
5.80287023594169));
#25972=CARTESIAN_POINT('Ctrl Pts',(-3.37491538366506,-0.00245188971244781,
5.84858989190502));
#25973=CARTESIAN_POINT('Origin',(0.,0.,-1.84858989190503));
#25974=CARTESIAN_POINT('',(-3.37724050405987,-0.000407706007126927,3.65141010809498));
#25975=CARTESIAN_POINT('',(-3.37013695473896,0.00300786229786701,3.84858989190502));
#25976=CARTESIAN_POINT('',(-3.37175,2.08693528006523E-13,-1.84858989190503));
#25977=CARTESIAN_POINT('Ctrl Pts',(-3.37724050405987,-0.000407706007126926,
3.65141010809498));
#25978=CARTESIAN_POINT('Ctrl Pts',(-3.37727770925144,-0.0222311044065494,
3.652444910773));
#25979=CARTESIAN_POINT('Ctrl Pts',(-3.36719553771294,-1.16099931030625,
3.70644369194564));
#25980=CARTESIAN_POINT('Ctrl Pts',(-2.09357261161725,-3.39225669930255,
3.8134064516129));
#25981=CARTESIAN_POINT('Ctrl Pts',(1.71738108280889,-3.59736765289132,3.97229838709678));
#25982=CARTESIAN_POINT('Ctrl Pts',(3.95415621068438,-0.505074716519562,
4.13119032258065));
#25983=CARTESIAN_POINT('Ctrl Pts',(2.56648943634972,3.05017766348832,4.29008225806451));
#25984=CARTESIAN_POINT('Ctrl Pts',(-1.17366200413909,3.8095891259482,4.44897419354839));
#25985=CARTESIAN_POINT('Ctrl Pts',(-3.19328501843251,1.73829700144105,4.56941681022521));
#25986=CARTESIAN_POINT('Ctrl Pts',(-3.37305871233378,0.310757734440618,
4.6368954484074));
#25987=CARTESIAN_POINT('Ctrl Pts',(-3.37037732776107,0.00303222645661912,
4.65141010809497));
#25988=CARTESIAN_POINT('Ctrl Pts',(-3.37013695473896,0.00300786229786694,
3.84858989190502));
#25989=CARTESIAN_POINT('Ctrl Pts',(-3.36320369751902,-0.804384073785939,
3.88666572659761));
#25990=CARTESIAN_POINT('Ctrl Pts',(-2.66732523950674,-2.7461115272218,3.97772985001845));
#25991=CARTESIAN_POINT('Ctrl Pts',(0.57892500607099,-3.94464492605495,4.12178226216755));
#25992=CARTESIAN_POINT('Ctrl Pts',(3.63013258458704,-1.64848875417016,4.2807471283523));
#25993=CARTESIAN_POINT('Ctrl Pts',(3.35110647594949,2.15996831943484,4.43971199453705));
#25994=CARTESIAN_POINT('Ctrl Pts',(-0.00217860669321579,3.9869001753454,
4.59867686072179));
#25995=CARTESIAN_POINT('Ctrl Pts',(-2.87549058156321,2.41739184906724,4.73496949317778));
#25996=CARTESIAN_POINT('Ctrl Pts',(-3.36443382798691,0.643215268868607,
4.81827383690552));
#25997=CARTESIAN_POINT('Ctrl Pts',(-3.36666513788771,-0.00130109466394548,
4.84858989190502));
#25998=CARTESIAN_POINT('Origin',(0.,0.,-1.84858989190503));
#25999=CARTESIAN_POINT('',(-3.36917031630593,-0.00279652979204336,2.65141010809498));
#26000=CARTESIAN_POINT('',(-3.37729882489346,-0.000194430141600699,2.84858989190502));
#26001=CARTESIAN_POINT('',(-3.37175,2.08693528006523E-13,-1.84858989190503));
#26002=CARTESIAN_POINT('Ctrl Pts',(-3.36917031630593,-0.00279652979204365,
2.65141010809498));
#26003=CARTESIAN_POINT('Ctrl Pts',(-3.37192195751912,-0.354718783760072,
2.66799437313859));
#26004=CARTESIAN_POINT('Ctrl Pts',(-3.15912528101716,-1.82730552094877,
2.73754261667682));
#26005=CARTESIAN_POINT('Ctrl Pts',(-1.02419029239979,-3.85246484135621,
2.86005483870968));
#26006=CARTESIAN_POINT('Ctrl Pts',(2.68349747959669,-2.94776072747231,3.01894677419354));
#26007=CARTESIAN_POINT('Ctrl Pts',(3.9314491981565,0.658907486316316,3.17783870967743));
#26008=CARTESIAN_POINT('Ctrl Pts',(1.57577260497388,3.66161063015511,3.33673064516129));
#26009=CARTESIAN_POINT('Ctrl Pts',(-2.19953367602677,3.310326581852,3.49458777796714));
#26010=CARTESIAN_POINT('Ctrl Pts',(-3.37537344768752,1.09474900016628,3.59948093227837));
#26011=CARTESIAN_POINT('Ctrl Pts',(-3.37724050405987,-0.000407706007126926,
3.65141010809498));
#26012=CARTESIAN_POINT('Ctrl Pts',(-3.37729882489346,-0.000194430141600942,
2.84858989190502));
#26013=CARTESIAN_POINT('Ctrl Pts',(-3.37730745906329,-0.0105519609168573,
2.8490810388332));
#26014=CARTESIAN_POINT('Ctrl Pts',(-3.3725690581147,-1.13834260190552,2.90256047448963));
#26015=CARTESIAN_POINT('Ctrl Pts',(-2.12700963248002,-3.37212213291773,
3.00902819887431));
#26016=CARTESIAN_POINT('Ctrl Pts',(1.68400001564517,-3.61379602896036,3.16799306505907));
#26017=CARTESIAN_POINT('Ctrl Pts',(3.95013122707835,-0.540223147458982,
3.32695793124381));
#26018=CARTESIAN_POINT('Ctrl Pts',(2.59246639543577,3.02894300530038,3.48592279742856));
#26019=CARTESIAN_POINT('Ctrl Pts',(-1.14349143614182,3.81939852540782,3.6448876636133));
#26020=CARTESIAN_POINT('Ctrl Pts',(-3.18684176799334,1.75591563149786,3.76577669510546));
#26021=CARTESIAN_POINT('Ctrl Pts',(-3.37285237464884,0.31922404594331,3.83367743786936));
#26022=CARTESIAN_POINT('Ctrl Pts',(-3.37013695473896,0.00300786229786694,
3.84858989190502));
#26023=CARTESIAN_POINT('Origin',(0.,0.,-1.84858989190503));
#26024=CARTESIAN_POINT('',(-3.36722314734446,0.00185482314707379,1.65141010809497));
#26025=CARTESIAN_POINT('',(-3.3695578818617,-0.00290129534754852,1.84858989190502));
#26026=CARTESIAN_POINT('',(-3.37175,2.08693528006523E-13,-1.84858989190503));
#26027=CARTESIAN_POINT('Ctrl Pts',(-3.36722314734446,0.00185482314707382,
1.65141010809497));
#26028=CARTESIAN_POINT('Ctrl Pts',(-3.36382382620938,-0.68102387856646,
1.68354383550418));
#26029=CARTESIAN_POINT('Ctrl Pts',(-2.83012682104856,-2.49433668358649,
1.768641541408));
#26030=CARTESIAN_POINT('Ctrl Pts',(0.13255069832671,-3.98407441119242,1.90670322580645));
#26031=CARTESIAN_POINT('Ctrl Pts',(3.42072557595435,-2.04672776701011,2.06559516129032));
#26032=CARTESIAN_POINT('Ctrl Pts',(3.57341090601276,1.76668952717683,2.2244870967742));
#26033=CARTESIAN_POINT('Ctrl Pts',(0.45065073371557,3.96072731387378,2.38337903225806));
#26034=CARTESIAN_POINT('Ctrl Pts',(-2.71613180302817,2.67422828685271,2.52568670269832));
#26035=CARTESIAN_POINT('Ctrl Pts',(-3.36313423821671,0.769190092631348,
2.61503039464396));
#26036=CARTESIAN_POINT('Ctrl Pts',(-3.36917031630593,-0.00279652979204365,
2.65141010809498));
#26037=CARTESIAN_POINT('Ctrl Pts',(-3.3695578818617,-0.00290129534754862,
1.84858989190502));
#26038=CARTESIAN_POINT('Ctrl Pts',(-3.37231432811694,-0.34009370411539,
1.86448463979704));
#26039=CARTESIAN_POINT('Ctrl Pts',(-3.1706964344189,-1.79816219768021,1.93336767641731));
#26040=CARTESIAN_POINT('Ctrl Pts',(-1.07258002819951,-3.83991470812214,
2.05523900176583));
#26041=CARTESIAN_POINT('Ctrl Pts',(2.6481020123777,-2.98042525524821,2.21420386795058));
#26042=CARTESIAN_POINT('Ctrl Pts',(3.9394520872816,0.613266379946328,2.37316873413532));
#26043=CARTESIAN_POINT('Ctrl Pts',(1.61680281711694,3.64435532093595,2.53213360032008));
#26044=CARTESIAN_POINT('Ctrl Pts',(-2.17732013669245,3.33312768965276,2.69060731957663));
#26045=CARTESIAN_POINT('Ctrl Pts',(-3.37637594578823,1.10688927659692,2.79609275010495));
#26046=CARTESIAN_POINT('Ctrl Pts',(-3.37729882489346,-0.000194430141600942,
2.84858989190502));
#26047=CARTESIAN_POINT('Origin',(0.,0.,-1.84858989190503));
#26048=CARTESIAN_POINT('',(-3.37589447807987,0.00214364281095937,0.651410108094974));
#26049=CARTESIAN_POINT('',(-3.36692593843476,0.00163208592380837,0.848589891905015));
#26050=CARTESIAN_POINT('',(-3.37175,2.08693528006523E-13,-1.84858989190503));
#26051=CARTESIAN_POINT('Ctrl Pts',(-3.37589447807987,0.0021436428109594,
0.651410108094974));
#26052=CARTESIAN_POINT('Ctrl Pts',(-3.36905382598057,-1.00443485423249,
0.699093297869767));
#26053=CARTESIAN_POINT('Ctrl Pts',(-2.35675364226999,-3.1417842761117,0.799740466139185));
#26054=CARTESIAN_POINT('Ctrl Pts',(1.27802196869812,-3.77566833700333,0.953351612903227));
#26055=CARTESIAN_POINT('Ctrl Pts',(3.86616524359544,-0.97122229991515,1.1122435483871));
#26056=CARTESIAN_POINT('Ctrl Pts',(2.91058978102209,2.72383605033175,1.27113548387097));
#26057=CARTESIAN_POINT('Ctrl Pts',(-0.71291441141164,3.92198718064885,1.43002741935484));
#26058=CARTESIAN_POINT('Ctrl Pts',(-3.08228566582866,2.00998594685298,1.55678562742951));
#26059=CARTESIAN_POINT('Ctrl Pts',(-3.36942671096663,0.444521639742584,
1.63057985700955));
#26060=CARTESIAN_POINT('Ctrl Pts',(-3.36722314734446,0.00185482314707382,
1.65141010809497));
#26061=CARTESIAN_POINT('Ctrl Pts',(-3.36692593843476,0.00163208592380858,
0.848589891905015));
#26062=CARTESIAN_POINT('Ctrl Pts',(-3.36407240691806,-0.663645509172373,
0.879888240760876));
#26063=CARTESIAN_POINT('Ctrl Pts',(-2.85117022634889,-2.45933226824664,
0.964174878344985));
#26064=CARTESIAN_POINT('Ctrl Pts',(0.0716483833591926,-3.98622915634864,
1.10144980465734));
#26065=CARTESIAN_POINT('Ctrl Pts',(3.39051798866077,-2.09756782602768,1.26041467084209));
#26066=CARTESIAN_POINT('Ctrl Pts',(3.59899177492058,1.71542482386315,1.41937953702684));
#26067=CARTESIAN_POINT('Ctrl Pts',(0.505790215469384,3.95468340129096,1.57834440321159));
#26068=CARTESIAN_POINT('Ctrl Pts',(-2.69572995999776,2.70483870003466,1.72141452150431));
#26069=CARTESIAN_POINT('Ctrl Pts',(-3.36312516884065,0.784003943368042,
1.81149635106879));
#26070=CARTESIAN_POINT('Ctrl Pts',(-3.3695578818617,-0.00290129534754862,
1.84858989190502));
#26071=CARTESIAN_POINT('Origin',(0.,0.,24.5));
#26072=CARTESIAN_POINT('',(-3.87097280197699,0.00213832761144025,24.1339652975667));
#26073=CARTESIAN_POINT('Ctrl Pts',(-0.624728334461281,3.3133687646595,24.62825));
#26074=CARTESIAN_POINT('Ctrl Pts',(-0.520138250042208,3.33634852849099,
24.625046902956));
#26075=CARTESIAN_POINT('Ctrl Pts',(-0.414648098080521,3.35389705620374,
24.6218539025135));
#26076=CARTESIAN_POINT('Ctrl Pts',(-0.308613703672553,3.36622114122732,
24.6186673709615));
#26077=CARTESIAN_POINT('Ctrl Pts',(-0.199986616426575,3.37884656778403,
24.6154029241484));
#26078=CARTESIAN_POINT('Ctrl Pts',(-0.0907876447210383,3.38598894312879,
24.6121452664408));
#26079=CARTESIAN_POINT('Ctrl Pts',(0.018614620750679,3.38781780937344,24.6088904974597));
#26080=CARTESIAN_POINT('Ctrl Pts',(0.0805633655032933,3.38885340006882,
24.6070474930945));
#26081=CARTESIAN_POINT('Ctrl Pts',(0.142577487054791,3.38818433590453,24.6052054149592));
#26082=CARTESIAN_POINT('Ctrl Pts',(0.204590631758452,3.38583417858992,24.6033635549037));
#26083=CARTESIAN_POINT('Ctrl Pts',(0.254638036250335,3.38393749564785,24.6018770907733));
#26084=CARTESIAN_POINT('Ctrl Pts',(0.304684819171919,3.38094577981049,24.600390768683));
#26085=CARTESIAN_POINT('Ctrl Pts',(0.354695913393206,3.3768690300029,24.5989042163964));
#26086=CARTESIAN_POINT('Ctrl Pts',(0.372494580510141,3.37541813767843,24.5983751607996));
#26087=CARTESIAN_POINT('Ctrl Pts',(0.39028796136771,3.37382978973891,24.5978460986132));
#26088=CARTESIAN_POINT('Ctrl Pts',(0.408061433233138,3.37210587416845,24.5973174010591));
#26089=CARTESIAN_POINT('Ctrl Pts',(0.519404457290808,3.36130629745725,24.5940053422263));
#26090=CARTESIAN_POINT('Ctrl Pts',(0.630100011901245,3.34518038635334,24.5907036020021));
#26091=CARTESIAN_POINT('Ctrl Pts',(0.739763436768937,3.32391000487198,24.5874081616821));
#26092=CARTESIAN_POINT('Ctrl Pts',(0.850257666159321,3.3024784800636,24.5840877552741));
#26093=CARTESIAN_POINT('Ctrl Pts',(0.95970493776685,3.27582407416606,24.5807737445874));
#26094=CARTESIAN_POINT('Ctrl Pts',(1.06770973553523,3.24407969544398,24.5774620188875));
#26095=CARTESIAN_POINT('Ctrl Pts',(1.1361584697924,3.22396149154746,24.5753631914553));
#26096=CARTESIAN_POINT('Ctrl Pts',(1.20402775637168,3.20179785912252,24.5732652817816));
#26097=CARTESIAN_POINT('Ctrl Pts',(1.27121405220256,3.17761217468148,24.5711672434934));
#26098=CARTESIAN_POINT('Ctrl Pts',(1.29774075436021,3.16806310757318,24.5703388894951));
#26099=CARTESIAN_POINT('Ctrl Pts',(1.32416095392457,3.15819874582631,24.5695105154476));
#26100=CARTESIAN_POINT('Ctrl Pts',(1.35046812449935,3.14802019412801,24.5686820569498));
#26101=CARTESIAN_POINT('Ctrl Pts',(1.36653976589062,3.14180188827438,24.5681759330454));
#26102=CARTESIAN_POINT('Ctrl Pts',(1.38256076287534,3.13546957145725,24.5676700437565));
#26103=CARTESIAN_POINT('Ctrl Pts',(1.39852700263983,3.12902498441374,24.5671644619047));
#26104=CARTESIAN_POINT('Ctrl Pts',(1.5038400459978,3.08651659892363,24.5638296526902));
#26105=CARTESIAN_POINT('Ctrl Pts',(1.60681042310701,3.03911282071154,24.5605069879339));
#26106=CARTESIAN_POINT('Ctrl Pts',(1.70704837153172,2.98697613057657,24.5571923886324));
#26107=CARTESIAN_POINT('Ctrl Pts',(1.80670371564138,2.935142469994,24.5538970544882));
#26108=CARTESIAN_POINT('Ctrl Pts',(1.90365915425284,2.87863046313165,24.5506096923149));
#26109=CARTESIAN_POINT('Ctrl Pts',(1.99751737945406,2.81755070396422,24.5473262938205));
#26110=CARTESIAN_POINT('Ctrl Pts',(2.09219867451912,2.7559353187613,24.5440141022572));
#26111=CARTESIAN_POINT('Ctrl Pts',(2.18372913512715,2.68967155408011,24.5407059441949));
#26112=CARTESIAN_POINT('Ctrl Pts',(2.271672791588,2.61882611527755,24.5373977049647));
#26113=CARTESIAN_POINT('Ctrl Pts',(2.31564461981842,2.58340339587627,24.5357435853496));
#26114=CARTESIAN_POINT('Ctrl Pts',(2.3587192214935,2.54683454512376,24.5340894454425));
#26115=CARTESIAN_POINT('Ctrl Pts',(2.40083835867941,2.50912376524234,24.5324347709098));
#26116=CARTESIAN_POINT('Ctrl Pts',(2.4199270309962,2.49203298969322,24.5316848614374));
#26117=CARTESIAN_POINT('Ctrl Pts',(2.43881941610424,2.47470762973993,24.5309348421549));
#26118=CARTESIAN_POINT('Ctrl Pts',(2.45750989027674,2.45714789797131,24.5301846651845));
#26119=CARTESIAN_POINT('Ctrl Pts',(2.47259728190695,2.4429732682819,24.5295791046386));
#26120=CARTESIAN_POINT('Ctrl Pts',(2.48755582869293,2.42864311414144,24.5289733271752));
#26121=CARTESIAN_POINT('Ctrl Pts',(2.50236326380812,2.41417672018039,24.528368102554));
#26122=CARTESIAN_POINT('Ctrl Pts',(2.5096874370137,2.40702123550619,24.5280687414615));
#26123=CARTESIAN_POINT('Ctrl Pts',(2.51697555679688,2.39983158202503,24.5277694793085));
#26124=CARTESIAN_POINT('Ctrl Pts',(2.52422733942721,2.39260786015533,24.5274703131481));
#26125=CARTESIAN_POINT('Ctrl Pts',(2.60073745914298,2.31639379621843,24.5243139528543));
#26126=CARTESIAN_POINT('Ctrl Pts',(2.67320522179129,2.23639118372509,24.5211682778273));
#26127=CARTESIAN_POINT('Ctrl Pts',(2.74161153441807,2.15302978874429,24.5180298269183));
#26128=CARTESIAN_POINT('Ctrl Pts',(2.81186762190031,2.06741421857952,24.5148065091695));
#26129=CARTESIAN_POINT('Ctrl Pts',(2.87784002551868,1.97825519814193,24.511590811516));
#26130=CARTESIAN_POINT('Ctrl Pts',(2.93947332195402,1.88597569204873,24.5083789843694));
#26131=CARTESIAN_POINT('Ctrl Pts',(3.00543439044467,1.78721649574186,24.5049416288708));
#26132=CARTESIAN_POINT('Ctrl Pts',(3.06642646008642,1.68488265861663,24.5015087065221));
#26133=CARTESIAN_POINT('Ctrl Pts',(3.12233208000985,1.57945276379857,24.4980756211074));
#26134=CARTESIAN_POINT('Ctrl Pts',(3.14679078872635,1.53332718481566,24.4965736462384));
#26135=CARTESIAN_POINT('Ctrl Pts',(3.1702752276744,1.48660856181708,24.4950716401576));
#26136=CARTESIAN_POINT('Ctrl Pts',(3.19277220676191,1.43933527974668,24.4935692179767));
#26137=CARTESIAN_POINT('Ctrl Pts',(3.20843753613705,1.40641745858516,24.4925230358101));
#26138=CARTESIAN_POINT('Ctrl Pts',(3.2236240268298,1.3732306769969,24.4914766518865));
#26139=CARTESIAN_POINT('Ctrl Pts',(3.23832660560595,1.33978769663366,24.4904299362547));
#26140=CARTESIAN_POINT('Ctrl Pts',(3.24466706730076,1.32536546913318,24.489978541947));
#26141=CARTESIAN_POINT('Ctrl Pts',(3.25091694288974,1.31089679039211,24.489527124135));
#26142=CARTESIAN_POINT('Ctrl Pts',(3.25707117071328,1.29639411279135,24.4890760252508));
#26143=CARTESIAN_POINT('Ctrl Pts',(3.30189883440903,1.19075597705509,24.4857902013176));
#26144=CARTESIAN_POINT('Ctrl Pts',(3.34172661274634,1.08315538243838,24.4825162404531));
#26145=CARTESIAN_POINT('Ctrl Pts',(3.37649898345667,0.974036565393082,24.4792502460069));
#26146=CARTESIAN_POINT('Ctrl Pts',(3.41163056334322,0.863790517745426,24.4759505128437));
#26147=CARTESIAN_POINT('Ctrl Pts',(3.44160210056879,0.751993878752548,24.47265891154));
#26148=CARTESIAN_POINT('Ctrl Pts',(3.46631080319639,0.639077130310462,24.4693714234329));
#26149=CARTESIAN_POINT('Ctrl Pts',(3.4909156460234,0.526635012655473,24.4660977538522));
#26150=CARTESIAN_POINT('Ctrl Pts',(3.51030206328578,0.41308129028903,24.4628281629622));
#26151=CARTESIAN_POINT('Ctrl Pts',(3.5243192195213,0.298826837120347,24.4595586825629));
#26152=CARTESIAN_POINT('Ctrl Pts',(3.5361116521245,0.202706203521802,24.4568081155714));
#26153=CARTESIAN_POINT('Ctrl Pts',(3.54410317841348,0.106089103613188,24.4540576267811));
#26154=CARTESIAN_POINT('Ctrl Pts',(3.54817462918724,0.00921931232785102,
24.451304853408));
#26155=CARTESIAN_POINT('Ctrl Pts',(3.54887956636703,-0.00755287067786807,
24.4508282340391));
#26156=CARTESIAN_POINT('Ctrl Pts',(3.54946687335721,-0.0243333324170402,
24.4503515260614));
#26157=CARTESIAN_POINT('Ctrl Pts',(3.5499355914206,-0.0411046474494315,
24.4498751757144));
#26158=CARTESIAN_POINT('Ctrl Pts',(3.55318741783251,-0.157459039234995,
24.4465703987905));
#26159=CARTESIAN_POINT('Ctrl Pts',(3.55074422185484,-0.273556149324447,
24.4432776009626));
#26160=CARTESIAN_POINT('Ctrl Pts',(3.54250561679224,-0.388968852721143,
24.4399928190226));
#26161=CARTESIAN_POINT('Ctrl Pts',(3.53438980253945,-0.502661408204027,
24.4367569945253));
#26162=CARTESIAN_POINT('Ctrl Pts',(3.52065018301948,-0.615690678667281,
24.4335289487538));
#26163=CARTESIAN_POINT('Ctrl Pts',(3.50114108221864,-0.727654569046081,
24.430304893079));
#26164=CARTESIAN_POINT('Ctrl Pts',(3.49384800416623,-0.769509977961124,
24.42909964585));
#26165=CARTESIAN_POINT('Ctrl Pts',(3.48574813528587,-0.811216498584334,
24.427894956231));
#26166=CARTESIAN_POINT('Ctrl Pts',(3.47683197850714,-0.852752977896645,
24.4266906262961));
#26167=CARTESIAN_POINT('Ctrl Pts',(3.4529871352566,-0.963835685722627,24.4234698374258));
#26168=CARTESIAN_POINT('Ctrl Pts',(3.42330774908946,-1.07370337125384,24.4202516210517));
#26169=CARTESIAN_POINT('Ctrl Pts',(3.38809113649622,-1.1820724034292,24.4170321914123));
#26170=CARTESIAN_POINT('Ctrl Pts',(3.37495661955853,-1.22249011495268,24.4158314611315));
#26171=CARTESIAN_POINT('Ctrl Pts',(3.36105136220375,-1.26269920199182,24.4146305620831));
#26172=CARTESIAN_POINT('Ctrl Pts',(3.34638908048464,-1.30268427759558,24.4134292978622));
#26173=CARTESIAN_POINT('Ctrl Pts',(3.33893812623189,-1.32300355496479,24.4128188495754));
#26174=CARTESIAN_POINT('Ctrl Pts',(3.33129166525305,-1.3432649771586,24.412208306987));
#26175=CARTESIAN_POINT('Ctrl Pts',(3.32345141301749,-1.36346647925837,24.411597644323));
#26176=CARTESIAN_POINT('Ctrl Pts',(3.31733644758331,-1.37922253956704,24.4111213610389));
#26177=CARTESIAN_POINT('Ctrl Pts',(3.31110676245958,-1.39493393196613,24.4106452528772));
#26178=CARTESIAN_POINT('Ctrl Pts',(3.30476515852903,-1.41059588192003,24.4101694268982));
#26179=CARTESIAN_POINT('Ctrl Pts',(3.26241982156158,-1.51517676644526,24.4069921531923));
#26180=CARTESIAN_POINT('Ctrl Pts',(3.21506671129281,-1.61761018296196,24.4038257550006));
#26181=CARTESIAN_POINT('Ctrl Pts',(3.16305493267433,-1.71764249367417,24.4006667076014));
#26182=CARTESIAN_POINT('Ctrl Pts',(3.10936292149889,-1.82090633289145,24.3974056076588));
#26183=CARTESIAN_POINT('Ctrl Pts',(3.05070610897566,-1.92161214375833,24.3941523411125));
#26184=CARTESIAN_POINT('Ctrl Pts',(2.98741482167415,-2.01946701686137,24.3909030304897));
#26185=CARTESIAN_POINT('Ctrl Pts',(2.92378476042904,-2.11784566950304,24.3876363275557));
#26186=CARTESIAN_POINT('Ctrl Pts',(2.85546994313465,-2.2133435033276,24.3843736230076));
#26187=CARTESIAN_POINT('Ctrl Pts',(2.78275913579883,-2.30563818528626,24.3811109767752));
#26188=CARTESIAN_POINT('Ctrl Pts',(2.73115118701869,-2.37114618050358,24.3787952484011));
#26189=CARTESIAN_POINT('Ctrl Pts',(2.67732765960473,-2.4350400215934,24.3764795494049));
#26190=CARTESIAN_POINT('Ctrl Pts',(2.62137984513178,-2.49719390809692,24.3741624709621));
#26191=CARTESIAN_POINT('Ctrl Pts',(2.60733587761121,-2.51279571795411,24.3735808401209));
#26192=CARTESIAN_POINT('Ctrl Pts',(2.59315801395097,-2.52828784255011,24.3729991223601));
#26193=CARTESIAN_POINT('Ctrl Pts',(2.5788476135988,-2.54366818796195,24.3724172953964));
#26194=CARTESIAN_POINT('Ctrl Pts',(2.56780240058981,-2.55553921791534,24.3719682232117));
#26195=CARTESIAN_POINT('Ctrl Pts',(2.55668178857907,-2.56733978704972,24.3715192315499));
#26196=CARTESIAN_POINT('Ctrl Pts',(2.54549189058683,-2.5790635828598,24.3710705218887));
#26197=CARTESIAN_POINT('Ctrl Pts',(2.46377857881438,-2.6646756396319,24.367793856412));
#26198=CARTESIAN_POINT('Ctrl Pts',(2.37828958660479,-2.74628708545935,24.3645287774285));
#26199=CARTESIAN_POINT('Ctrl Pts',(2.28935576945552,-2.82360475294287,24.3612714210233));
#26200=CARTESIAN_POINT('Ctrl Pts',(2.2004312170102,-2.9009143658379,24.358014403954));
#26201=CARTESIAN_POINT('Ctrl Pts',(2.10806196086699,-2.97393178300944,24.354765107854));
#26202=CARTESIAN_POINT('Ctrl Pts',(2.01253765634337,-3.04233309530011,24.3515196700154));
#26203=CARTESIAN_POINT('Ctrl Pts',(1.91831994223422,-3.10979880801304,24.3483186235807));
#26204=CARTESIAN_POINT('Ctrl Pts',(1.82103227216761,-3.17277441103138,24.345121330582));
#26205=CARTESIAN_POINT('Ctrl Pts',(1.72092180235263,-3.23090982550694,24.3419240846569));
#26206=CARTESIAN_POINT('Ctrl Pts',(1.63731823238491,-3.27945947471638,24.3392540225356));
#26207=CARTESIAN_POINT('Ctrl Pts',(1.55174530961941,-3.32463302100756,24.3365839932441));
#26208=CARTESIAN_POINT('Ctrl Pts',(1.46433480530475,-3.3662006160568,24.3339118381243));
#26209=CARTESIAN_POINT('Ctrl Pts',(1.44360953039847,-3.37605640903435,24.3332782626761));
#26210=CARTESIAN_POINT('Ctrl Pts',(1.42277595537401,-3.38571149112601,24.3326444189594));
#26211=CARTESIAN_POINT('Ctrl Pts',(1.40186473452666,-3.39514984035219,24.3320111514667));
#26212=CARTESIAN_POINT('Ctrl Pts',(1.33458120918284,-3.42551848377093,24.3299735626666));
#26213=CARTESIAN_POINT('Ctrl Pts',(1.2664465713012,-3.45366766831798,24.3279404681835));
#26214=CARTESIAN_POINT('Ctrl Pts',(1.19753254997869,-3.47952152342011,24.3259109394442));
#26215=CARTESIAN_POINT('Ctrl Pts',(1.09102290473056,-3.51947979145293,24.3227742136821));
#26216=CARTESIAN_POINT('Ctrl Pts',(0.982652679880705,-3.55395790982246,
24.3196460054332));
#26217=CARTESIAN_POINT('Ctrl Pts',(0.872822247400536,-3.58310705179026,
24.3165228865437));
#26218=CARTESIAN_POINT('Ctrl Pts',(0.760371906501168,-3.61295152091583,
24.3133252683986));
#26219=CARTESIAN_POINT('Ctrl Pts',(0.646390155341705,-3.6372098459968,24.3101329853132));
#26220=CARTESIAN_POINT('Ctrl Pts',(0.53128616178814,-3.6559936831665,24.3069423579087));
#26221=CARTESIAN_POINT('Ctrl Pts',(0.41453738712084,-3.67504593240137,24.3037061379619));
#26222=CARTESIAN_POINT('Ctrl Pts',(0.296633230443278,-3.68846615738096,
24.3004716213517));
#26223=CARTESIAN_POINT('Ctrl Pts',(0.177991630975357,-3.69631848981734,
24.2972349687049));
#26224=CARTESIAN_POINT('Ctrl Pts',(0.142360760405031,-3.69867673045107,
24.2962629255763));
#26225=CARTESIAN_POINT('Ctrl Pts',(0.1066633636693,-3.70053242315808,24.2952906897893));
#26226=CARTESIAN_POINT('Ctrl Pts',(0.0709107847277581,-3.70188639298558,
24.2943181573453));
#26227=CARTESIAN_POINT('Ctrl Pts',(0.0511417931589634,-3.70263505556873,
24.2937804063283));
#26228=CARTESIAN_POINT('Ctrl Pts',(0.0313540742527653,-3.70323026849973,
24.2932425143369));
#26229=CARTESIAN_POINT('Ctrl Pts',(0.0115717980804544,-3.70367187863094,
24.2927050676203));
#26230=CARTESIAN_POINT('Ctrl Pts',(-0.107433551546183,-3.70632849749549,
24.2894719192276));
#26231=CARTESIAN_POINT('Ctrl Pts',(-0.226418918411982,-3.7034386910525,
24.2862500321799));
#26232=CARTESIAN_POINT('Ctrl Pts',(-0.344959013740293,-3.6951464558983,
24.2830356970017));
#26233=CARTESIAN_POINT('Ctrl Pts',(-0.464907323931171,-3.68675571189142,
24.2797831766461));
#26234=CARTESIAN_POINT('Ctrl Pts',(-0.584400592051045,-3.67283340149898,
24.2765383886529));
#26235=CARTESIAN_POINT('Ctrl Pts',(-0.703006950795025,-3.65347561626452,
24.2732974897681));
#26236=CARTESIAN_POINT('Ctrl Pts',(-0.821420460393264,-3.63414930600648,
24.2700618604539));
#26237=CARTESIAN_POINT('Ctrl Pts',(-0.938950841911184,-3.6094050645999,
24.2668301076113));
#26238=CARTESIAN_POINT('Ctrl Pts',(-1.05516365811085,-3.57928709699041,
24.2635984067028));
#26239=CARTESIAN_POINT('Ctrl Pts',(-1.11307514573956,-3.56427862920126,
24.261987976689));
#26240=CARTESIAN_POINT('Ctrl Pts',(-1.17065929149193,-3.5479349386455,24.2603775595719));
#26241=CARTESIAN_POINT('Ctrl Pts',(-1.22786083460473,-3.53025684653982,
24.258766682079));
#26242=CARTESIAN_POINT('Ctrl Pts',(-1.27025654792723,-3.5171544845367,24.2575727579877));
#26243=CARTESIAN_POINT('Ctrl Pts',(-1.31244206756123,-3.50331904033182,
24.256378581001));
#26244=CARTESIAN_POINT('Ctrl Pts',(-1.35439435742328,-3.48874976896511,
24.2551839584315));
#26245=CARTESIAN_POINT('Ctrl Pts',(-1.37450122726203,-3.48176701679641,
24.2546114003997));
#26246=CARTESIAN_POINT('Ctrl Pts',(-1.39455787836581,-3.47461436152618,
24.2540386428268));
#26247=CARTESIAN_POINT('Ctrl Pts',(-1.4145370881139,-3.46730094250551,24.2534663728415));
#26248=CARTESIAN_POINT('Ctrl Pts',(-1.52840519986039,-3.42561935325375,
24.2502048172814));
#26249=CARTESIAN_POINT('Ctrl Pts',(-1.63991365982444,-3.37866812586214,
24.2469546926609));
#26250=CARTESIAN_POINT('Ctrl Pts',(-1.74863318528068,-3.32654324532194,
24.2437121916767));
#26251=CARTESIAN_POINT('Ctrl Pts',(-1.85558872732241,-3.27526409533814,
24.2405223005429));
#26252=CARTESIAN_POINT('Ctrl Pts',(-1.95984592910298,-3.2189775652086,24.2373397876639));
#26253=CARTESIAN_POINT('Ctrl Pts',(-2.06098377301333,-3.15772709883281,
24.2341610280672));
#26254=CARTESIAN_POINT('Ctrl Pts',(-2.15682437201784,-3.09968471667599,
24.2311487607293));
#26255=CARTESIAN_POINT('Ctrl Pts',(-2.24986433245661,-3.03718433413316,
24.2281398638026));
#26256=CARTESIAN_POINT('Ctrl Pts',(-2.33972491633012,-2.97022484402709,
24.2251312525923));
#26257=CARTESIAN_POINT('Ctrl Pts',(-2.39708388099203,-2.9274838906389,24.2232108241167));
#26258=CARTESIAN_POINT('Ctrl Pts',(-2.45314695486067,-2.88292530873872,
24.2212905120536));
#26259=CARTESIAN_POINT('Ctrl Pts',(-2.50788173230019,-2.8366336564438,24.2193695141552));
#26260=CARTESIAN_POINT('Ctrl Pts',(-2.53563831690701,-2.81315866990653,
24.2183953558013));
#26261=CARTESIAN_POINT('Ctrl Pts',(-2.56305323963533,-2.78923792330051,
24.2174210210771));
#26262=CARTESIAN_POINT('Ctrl Pts',(-2.59012178635459,-2.76488197889541,
24.2164464053624));
#26263=CARTESIAN_POINT('Ctrl Pts',(-2.60345465688749,-2.75288522647173,
24.2159663491083));
#26264=CARTESIAN_POINT('Ctrl Pts',(-2.61670472847459,-2.74078173073675,
24.2154861793416));
#26265=CARTESIAN_POINT('Ctrl Pts',(-2.62986751863965,-2.72857633888938,
24.2150060254729));
#26266=CARTESIAN_POINT('Ctrl Pts',(-2.71508215755265,-2.6495598047031,24.2118975554583));
#26267=CARTESIAN_POINT('Ctrl Pts',(-2.79636860051037,-2.56653035928709,
24.2087997059384));
#26268=CARTESIAN_POINT('Ctrl Pts',(-2.87364584295152,-2.47991615691849,
24.2057091871955));
#26269=CARTESIAN_POINT('Ctrl Pts',(-2.95372207710542,-2.39016477694134,
24.2025067294641));
#26270=CARTESIAN_POINT('Ctrl Pts',(-3.02949395217132,-2.29656378485085,
24.1993121431703));
#26271=CARTESIAN_POINT('Ctrl Pts',(-3.10083927390671,-2.19954365518354,
24.1961217680305));
#26272=CARTESIAN_POINT('Ctrl Pts',(-3.1729388167544,-2.1014978853154,24.1928976661062));
#26273=CARTESIAN_POINT('Ctrl Pts',(-3.24051817780072,-1.99995957525359,
24.1896778648424));
#26274=CARTESIAN_POINT('Ctrl Pts',(-3.30341172612255,-1.89533643715524,
24.1864585866407));
#26275=CARTESIAN_POINT('Ctrl Pts',(-3.34638934220069,-1.82384336382643,
24.1842587282087));
#26276=CARTESIAN_POINT('Ctrl Pts',(-3.38717808530971,-1.7509090628703,24.1820591140217));
#26277=CARTESIAN_POINT('Ctrl Pts',(-3.42571297641979,-1.67665668248674,
24.1798585386985));
#26278=CARTESIAN_POINT('Ctrl Pts',(-3.445014281687,-1.63946524845605,24.1787563174426));
#26279=CARTESIAN_POINT('Ctrl Pts',(-3.46374997985981,-1.60194306216562,
24.1776538550573));
#26280=CARTESIAN_POINT('Ctrl Pts',(-3.48191088985649,-1.56410523444394,
24.1765510000744));
#26281=CARTESIAN_POINT('Ctrl Pts',(-3.49096642636183,-1.54523823767566,
24.1760010858047));
#26282=CARTESIAN_POINT('Ctrl Pts',(-3.4998801459806,-1.52629016625364,24.1754509999921));
#26283=CARTESIAN_POINT('Ctrl Pts',(-3.50864077925426,-1.5072853111527,24.174901369431));
#26284=CARTESIAN_POINT('Ctrl Pts',(-3.56003841051657,-1.39578600463474,
24.171676749928));
#26285=CARTESIAN_POINT('Ctrl Pts',(-3.60624692934267,-1.28217850112835,
24.1684632179365));
#26286=CARTESIAN_POINT('Ctrl Pts',(-3.6471387300781,-1.1668916502069,24.1652570948759));
#26287=CARTESIAN_POINT('Ctrl Pts',(-3.6882879122029,-1.05087916017607,24.1620307918185));
#26288=CARTESIAN_POINT('Ctrl Pts',(-3.72405366249247,-0.933165324275529,
24.1588119912523));
#26289=CARTESIAN_POINT('Ctrl Pts',(-3.75426180619985,-0.814159485558989,
24.1555969446976));
#26290=CARTESIAN_POINT('Ctrl Pts',(-3.7841716362032,-0.696328862138458,
24.1524136476093));
#26291=CARTESIAN_POINT('Ctrl Pts',(-3.80863339059432,-0.577230809008665,
24.1492340307549));
#26292=CARTESIAN_POINT('Ctrl Pts',(-3.8274295805391,-0.457247749762826,
24.1460544556133));
#26293=CARTESIAN_POINT('Ctrl Pts',(-3.83933667583213,-0.381240339527709,
24.1440402439932));
#26294=CARTESIAN_POINT('Ctrl Pts',(-3.84896918346273,-0.304877515113294,
24.1420260491124));
#26295=CARTESIAN_POINT('Ctrl Pts',(-3.85626072121049,-0.2282555949368,24.14001094599));
#26296=CARTESIAN_POINT('Ctrl Pts',(-3.85942265273046,-0.195028959773208,
24.1391371086324));
#26297=CARTESIAN_POINT('Ctrl Pts',(-3.86214425712046,-0.161753603333563,
24.1382631004825));
#26298=CARTESIAN_POINT('Ctrl Pts',(-3.86441958153066,-0.128437410079632,
24.1373888461123));
#26299=CARTESIAN_POINT('Ctrl Pts',(-3.86591347492261,-0.106563236566722,
24.1368148432051));
#26300=CARTESIAN_POINT('Ctrl Pts',(-3.86721509040623,-0.0846675012688186,
24.1362406305225));
#26301=CARTESIAN_POINT('Ctrl Pts',(-3.86832155925171,-0.0627797067798542,
24.1356669009074));
#26302=CARTESIAN_POINT('Ctrl Pts',(-3.86941608558997,-0.0411281549512009,
24.1350993637576));
#26303=CARTESIAN_POINT('Ctrl Pts',(-3.87032006240666,-0.0194794249965481,
24.1345321693282));
#26304=CARTESIAN_POINT('Ctrl Pts',(-3.87103266938659,0.00216425178203038,
24.1339652975667));
#26305=CARTESIAN_POINT('',(0.349572399382967,3.92005776261121,24.058));
#26306=CARTESIAN_POINT('Ctrl Pts',(0.349418900843753,3.91916189049795,24.058));
#26307=CARTESIAN_POINT('Ctrl Pts',(0.226012228632792,3.91828850060595,24.0696807256992));
#26308=CARTESIAN_POINT('Ctrl Pts',(0.102952431902507,3.91191927543051,24.0813859465783));
#26309=CARTESIAN_POINT('Ctrl Pts',(-0.0193397180673949,3.90006603014558,
24.0931306202039));
#26310=CARTESIAN_POINT('Ctrl Pts',(-0.140580622517234,3.88831467750876,
24.1047743344831));
#26311=CARTESIAN_POINT('Ctrl Pts',(-0.261067870571708,3.87117297838718,
24.1164568261384));
#26312=CARTESIAN_POINT('Ctrl Pts',(-0.380377476123202,3.84860347157658,
24.1281926703091));
#26313=CARTESIAN_POINT('Ctrl Pts',(-0.496161715673067,3.82670084964599,
24.1395817431879));
#26314=CARTESIAN_POINT('Ctrl Pts',(-0.610837511562959,3.79968611836398,
24.1510210622381));
#26315=CARTESIAN_POINT('Ctrl Pts',(-0.723993462162786,3.76748283972913,
24.1625239483983));
#26316=CARTESIAN_POINT('Ctrl Pts',(-0.796757989013667,3.74677463728383,
24.1699208379514));
#26317=CARTESIAN_POINT('Ctrl Pts',(-0.868893538246561,3.72392009045816,
24.177344013056));
#26318=CARTESIAN_POINT('Ctrl Pts',(-0.940283456718533,3.69889010045098,
24.1847970158196));
#26319=CARTESIAN_POINT('Ctrl Pts',(-0.958852956027486,3.69237945592175,
24.1867356443071));
#26320=CARTESIAN_POINT('Ctrl Pts',(-0.977371972215163,3.6857215872702,24.188676290909));
#26321=CARTESIAN_POINT('Ctrl Pts',(-0.995838377017294,3.67891590798256,
24.1906190179632));
#26322=CARTESIAN_POINT('Ctrl Pts',(-1.01171569758055,3.67306441967942,24.1922893647652));
#26323=CARTESIAN_POINT('Ctrl Pts',(-1.0275456693922,3.66710676559807,24.1939603606721));
#26324=CARTESIAN_POINT('Ctrl Pts',(-1.04332469128769,3.6610438482036,24.1956317888384));
#26325=CARTESIAN_POINT('Ctrl Pts',(-1.15165978098886,3.619417269311,24.2071074253844));
#26326=CARTESIAN_POINT('Ctrl Pts',(-1.25763328276278,3.57281828211811,24.2186074516257));
#26327=CARTESIAN_POINT('Ctrl Pts',(-1.36087067794145,3.52121736057027,24.2301462409952));
#26328=CARTESIAN_POINT('Ctrl Pts',(-1.42681061365643,3.48825874665126,24.2375163129341));
#26329=CARTESIAN_POINT('Ctrl Pts',(-1.49163388388109,3.45325861360399,24.2449021988746));
#26330=CARTESIAN_POINT('Ctrl Pts',(-1.55523660610354,3.41620000588947,24.2523076441887));
#26331=CARTESIAN_POINT('Ctrl Pts',(-1.65681419035516,3.35701505726094,24.2641346103786));
#26332=CARTESIAN_POINT('Ctrl Pts',(-1.75528075449242,3.2925810923405,24.276011464936));
#26333=CARTESIAN_POINT('Ctrl Pts',(-1.8504118158475,3.22325698482629,24.2879534645915));
#26334=CARTESIAN_POINT('Ctrl Pts',(-1.94589009699015,3.15367985057672,24.2999390514679));
#26335=CARTESIAN_POINT('Ctrl Pts',(-2.03800893445419,3.07917596454707,24.3119902598576));
#26336=CARTESIAN_POINT('Ctrl Pts',(-2.12649675572721,3.00008130698686,24.3241225141588));
#26337=CARTESIAN_POINT('Ctrl Pts',(-2.15464819134299,2.97491820399908,24.3279822585951));
#26338=CARTESIAN_POINT('Ctrl Pts',(-2.18243175770649,2.94929030687597,24.3318502058895));
#26339=CARTESIAN_POINT('Ctrl Pts',(-2.20983765373967,2.92320808164845,24.3357268527022));
#26340=CARTESIAN_POINT('Ctrl Pts',(-2.22035441337321,2.91319926846847,24.3372144801333));
#26341=CARTESIAN_POINT('Ctrl Pts',(-2.23081386252428,2.90312511161636,24.3387031532638));
#26342=CARTESIAN_POINT('Ctrl Pts',(-2.24120927897093,2.89299245114185,24.3401919995702));
#26343=CARTESIAN_POINT('Ctrl Pts',(-2.32385350748897,2.81243714948096,24.3520284233442));
#26344=CARTESIAN_POINT('Ctrl Pts',(-2.40257000364209,2.72807711715171,24.3638921677319));
#26345=CARTESIAN_POINT('Ctrl Pts',(-2.47717616028223,2.64027648475023,24.3757991858546));
#26346=CARTESIAN_POINT('Ctrl Pts',(-2.55187618325755,2.55236538527792,24.3877211848877));
#26347=CARTESIAN_POINT('Ctrl Pts',(-2.62245590857137,2.46100416174114,24.3996865666148));
#26348=CARTESIAN_POINT('Ctrl Pts',(-2.68868744355177,2.36653097722017,24.4117113444476));
#26349=CARTESIAN_POINT('Ctrl Pts',(-2.75414075468922,2.27316785733437,24.4235948305405));
#26350=CARTESIAN_POINT('Ctrl Pts',(-2.81534772258566,2.17676464445494,24.4355363251252));
#26351=CARTESIAN_POINT('Ctrl Pts',(-2.8720401475082,2.07763370148774,24.4475512837449));
#26352=CARTESIAN_POINT('Ctrl Pts',(-2.90668546327039,2.01705377699881,24.4548937467957));
#26353=CARTESIAN_POINT('Ctrl Pts',(-2.93964383947717,1.95545494636204,24.462263645402));
#26354=CARTESIAN_POINT('Ctrl Pts',(-2.97084438937695,1.89290785453322,24.4696645068668));
#26355=CARTESIAN_POINT('Ctrl Pts',(-2.98845779797902,1.85759862156167,24.4738424587748));
#26356=CARTESIAN_POINT('Ctrl Pts',(-3.00551087593063,1.82198719162217,24.4780302780973));
#26357=CARTESIAN_POINT('Ctrl Pts',(-3.02198977071177,1.78608635326393,24.4822285994141));
#26358=CARTESIAN_POINT('Ctrl Pts',(-3.02877383007556,1.77130663521446,24.4839569714572));
#26359=CARTESIAN_POINT('Ctrl Pts',(-3.03545687173813,1.75648588102819,24.4856861859929));
#26360=CARTESIAN_POINT('Ctrl Pts',(-3.04203688563128,1.74162824455868,24.4874159221199));
#26361=CARTESIAN_POINT('Ctrl Pts',(-3.08710741956134,1.63985921800425,24.4992639412984));
#26362=CARTESIAN_POINT('Ctrl Pts',(-3.12737033179139,1.53631268431983,24.5111420689289));
#26363=CARTESIAN_POINT('Ctrl Pts',(-3.16262066493997,1.43129464400087,24.5230664886917));
#26364=CARTESIAN_POINT('Ctrl Pts',(-3.19738804194613,1.32771543001649,24.534827534913));
#26365=CARTESIAN_POINT('Ctrl Pts',(-3.22727942618041,1.22270400117247,24.5466336134818));
#26366=CARTESIAN_POINT('Ctrl Pts',(-3.2520488351859,1.1165476391786,24.5585002519648));
#26367=CARTESIAN_POINT('Ctrl Pts',(-3.27606482816892,1.01362025628536,24.5700059405533));
#26368=CARTESIAN_POINT('Ctrl Pts',(-3.29526569753493,0.909615922196257,
24.5815685609605));
#26369=CARTESIAN_POINT('Ctrl Pts',(-3.3093795070715,0.804800410213191,24.5932022664991));
#26370=CARTESIAN_POINT('Ctrl Pts',(-3.32346107752391,0.700224320202117,
24.6048093980635));
#26371=CARTESIAN_POINT('Ctrl Pts',(-3.33247901104835,0.594840172393064,
24.6164872903817));
#26372=CARTESIAN_POINT('Ctrl Pts',(-3.33611311329483,0.488924695430968,
24.62825));
#26373=CARTESIAN_POINT('',(-2.87185821835411,2.69480181882395,24.058));
#26374=CARTESIAN_POINT('Origin',(0.,0.,24.058));
#26375=CARTESIAN_POINT('Ctrl Pts',(-3.87103266938659,0.00216425178203038,
24.1339652975667));
#26376=CARTESIAN_POINT('Ctrl Pts',(-3.87507260628243,0.124867355795072,
24.1307515679672));
#26377=CARTESIAN_POINT('Ctrl Pts',(-3.87296594485587,0.247407050622043,
24.1275482085216));
#26378=CARTESIAN_POINT('Ctrl Pts',(-3.86453408452217,0.369385378863034,
24.1243515657403));
#26379=CARTESIAN_POINT('Ctrl Pts',(-3.85627040623579,0.488930725038259,
24.1212186832571));
#26380=CARTESIAN_POINT('Ctrl Pts',(-3.84193179212873,0.607937675272044,
24.1180922521689));
#26381=CARTESIAN_POINT('Ctrl Pts',(-3.82181791447054,0.726086832854309,
24.1149688332722));
#26382=CARTESIAN_POINT('Ctrl Pts',(-3.80134858411548,0.846323923823187,
24.1117902172779));
#26383=CARTESIAN_POINT('Ctrl Pts',(-3.77489779988944,0.965673358591756,
24.1086147208788));
#26384=CARTESIAN_POINT('Ctrl Pts',(-3.74272692791689,1.08379247292844,24.1054387192973));
#26385=CARTESIAN_POINT('Ctrl Pts',(-3.72259049299425,1.15772574589009,24.1034507921682));
#26386=CARTESIAN_POINT('Ctrl Pts',(-3.70021198877918,1.23117684933353,24.1014626671201));
#26387=CARTESIAN_POINT('Ctrl Pts',(-3.67564568396927,1.30405861901184,24.099473455278));
#26388=CARTESIAN_POINT('Ctrl Pts',(-3.66863540268018,1.32485628110409,24.0989058105034));
#26389=CARTESIAN_POINT('Ctrl Pts',(-3.66144692163609,1.3456075617141,24.0983380772297));
#26390=CARTESIAN_POINT('Ctrl Pts',(-3.65408139767167,1.36631038395308,24.097770234802));
#26391=CARTESIAN_POINT('Ctrl Pts',(-3.64822216373193,1.38277936556212,24.0973185192633));
#26392=CARTESIAN_POINT('Ctrl Pts',(-3.64225062386782,1.39921823302553,24.0968667189574));
#26393=CARTESIAN_POINT('Ctrl Pts',(-3.63617302699739,1.41561112341376,24.0964152327823));
#26394=CARTESIAN_POINT('Ctrl Pts',(-3.59274946073352,1.53273599648544,24.0931894281991));
#26395=CARTESIAN_POINT('Ctrl Pts',(-3.54385270980084,1.6476965516567,24.0899746657265));
#26396=CARTESIAN_POINT('Ctrl Pts',(-3.48981414813695,1.76015005122282,24.0867672641288));
#26397=CARTESIAN_POINT('Ctrl Pts',(-3.43581118825365,1.87252946397587,24.0835619756371));
#26398=CARTESIAN_POINT('Ctrl Pts',(-3.37667270383973,1.98240587688454,24.0803640383244));
#26399=CARTESIAN_POINT('Ctrl Pts',(-3.31267597495322,2.08942561654219,24.0771697782258));
#26400=CARTESIAN_POINT('Ctrl Pts',(-3.24861596071611,2.19655118632369,24.0739723593741));
#26401=CARTESIAN_POINT('Ctrl Pts',(-3.17968763174453,2.30081519811777,24.0707786250127));
#26402=CARTESIAN_POINT('Ctrl Pts',(-3.10612258128374,2.40183988004365,24.0675848902668));
#26403=CARTESIAN_POINT('Ctrl Pts',(-3.03255753082295,2.50286456196954,24.0643911555208));
#26404=CARTESIAN_POINT('Ctrl Pts',(-2.95435530373159,2.60065069905013,24.0611974203902));
#26405=CARTESIAN_POINT('Ctrl Pts',(-2.87170785494336,2.69478584831407,24.058));
#26406=CARTESIAN_POINT('',(-3.,-3.67394039744206E-16,25.));
#26407=CARTESIAN_POINT('',(-3.5,-4.28626379701574E-16,24.5));
#26408=CARTESIAN_POINT('Origin',(0.,0.,25.));
#26409=CARTESIAN_POINT('Ctrl Pts',(2.28870316125076,-3.20954854141214,-0.329233991005384));
#26410=CARTESIAN_POINT('Ctrl Pts',(3.35678472141098,-2.44790820113649,-0.27627001251076));
#26411=CARTESIAN_POINT('Ctrl Pts',(4.65420965805454,0.212376298523761,-0.170342055521513));
#26412=CARTESIAN_POINT('Ctrl Pts',(2.33824086975704,4.03501766412881,-0.011450120037642));
#26413=CARTESIAN_POINT('Ctrl Pts',(-2.12304297015552,4.14730362817999,0.147441815446229));
#26414=CARTESIAN_POINT('Ctrl Pts',(-4.6372363620278,0.464007918031343,0.3063337509301));
#26415=CARTESIAN_POINT('Ctrl Pts',(-2.9014296726223,-3.64766420030675,0.46522568641397));
#26416=CARTESIAN_POINT('Ctrl Pts',(1.49416848835415,-4.41423135892847,0.624117621897843));
#26417=CARTESIAN_POINT('Ctrl Pts',(4.52003362949604,-1.13548107251883,0.783009557381712));
#26418=CARTESIAN_POINT('Ctrl Pts',(3.40284567859094,3.18450706915039,0.941901492865584));
#26419=CARTESIAN_POINT('Ctrl Pts',(-0.833486649302243,4.58529649769934,
1.10079342834945));
#26420=CARTESIAN_POINT('Ctrl Pts',(-4.30580977810473,1.78325097864793,1.25968536383333));
#26421=CARTESIAN_POINT('Ctrl Pts',(-3.83137142736725,-2.65341337269076,
1.4185772993172));
#26422=CARTESIAN_POINT('Ctrl Pts',(0.154968444518143,-4.65788428232239,
1.57746923480107));
#26423=CARTESIAN_POINT('Ctrl Pts',(3.99925861063605,-2.3928822888867,1.73636117028494));
#26424=CARTESIAN_POINT('Ctrl Pts',(4.17776697308586,2.065482350747,1.89525310576881));
#26425=CARTESIAN_POINT('Ctrl Pts',(0.526867410782717,4.63058858791146,2.05414504125268));
#26426=CARTESIAN_POINT('Ctrl Pts',(-3.60696666633743,2.95122682044694,2.21303697673655));
#26427=CARTESIAN_POINT('Ctrl Pts',(-4.43459848935502,-1.43327725922984,
2.37192891222043));
#26428=CARTESIAN_POINT('Ctrl Pts',(-1.19740732042406,-4.50401613542707,
2.53082084770429));
#26429=CARTESIAN_POINT('Ctrl Pts',(3.13734620436576,-3.44630319202068,2.68971278318817));
#26430=CARTESIAN_POINT('Ctrl Pts',(4.59635878672289,0.770345758451563,2.84860471867204));
#26431=CARTESIAN_POINT('Ctrl Pts',(1.84227644659507,4.28088354832699,3.00749665415591));
#26432=CARTESIAN_POINT('Ctrl Pts',(-2.60046551010954,3.86749606027826,3.16638858963978));
#26433=CARTESIAN_POINT('Ctrl Pts',(-4.65957980074616,-0.0908992967115246,
3.32528052512365));
#26434=CARTESIAN_POINT('Ctrl Pts',(-2.44764980647886,-3.96597491173744,
3.48417246060752));
#26435=CARTESIAN_POINT('Ctrl Pts',(2.00783457505236,-4.20577542454142,3.64306439609139));
#26436=CARTESIAN_POINT('Ctrl Pts',(4.62290614147485,-0.590495894571063,
3.80195633157526));
#26437=CARTESIAN_POINT('Ctrl Pts',(3.00054907928836,3.56604147682096,3.96084826705914));
#26438=CARTESIAN_POINT('Ctrl Pts',(-1.37215855870585,4.45388902928383,4.119740202543));
#26439=CARTESIAN_POINT('Ctrl Pts',(-4.48712403609106,1.2592317017741,4.27863213802688));
#26440=CARTESIAN_POINT('Ctrl Pts',(-3.48912090296361,-3.08965724931931,
4.43752407351074));
#26441=CARTESIAN_POINT('Ctrl Pts',(0.707065439817984,-4.60651767152865,
4.59641600899462));
#26442=CARTESIAN_POINT('Ctrl Pts',(4.25514445682574,-1.9009713952631,4.75530794447848));
#26443=CARTESIAN_POINT('Ctrl Pts',(3.90289100181761,2.54703522197484,4.91419987996237));
#26444=CARTESIAN_POINT('Ctrl Pts',(-0.0268138566703869,4.6603892124167,
5.07309181544622));
#26445=CARTESIAN_POINT('Ctrl Pts',(-3.93194071153866,2.50195700103508,5.23198375093011));
#26446=CARTESIAN_POINT('Ctrl Pts',(-4.23298874115587,-1.9498084293931,5.39087568641397));
#26447=CARTESIAN_POINT('Ctrl Pts',(-0.654012576931896,-4.61434872363465,
5.54976762189785));
#26448=CARTESIAN_POINT('Ctrl Pts',(3.52444182282379,-3.04930425369769,5.70865955738171));
#26449=CARTESIAN_POINT('Ctrl Pts',(4.47233730108079,1.31078055350635,5.86755149286558));
#26450=CARTESIAN_POINT('Ctrl Pts',(1.32081792323409,4.46938324690933,6.02644342834946));
#26451=CARTESIAN_POINT('Ctrl Pts',(-3.04138397969982,3.531278816819,6.18533536383333));
#26452=CARTESIAN_POINT('Ctrl Pts',(-4.61580539333909,-0.643651431219671,
6.3442272993172));
#26453=CARTESIAN_POINT('Ctrl Pts',(-1.95930683639269,-4.22860063318286,
6.50311923480107));
#26454=CARTESIAN_POINT('Ctrl Pts',(2.4931232462982,-3.93754785023079,6.66201117028494));
#26455=CARTESIAN_POINT('Ctrl Pts',(4.66031726875216,-0.037276650332675,
6.82090310576881));
#26456=CARTESIAN_POINT('Ctrl Pts',(2.55579103409072,3.8971629147562,6.97979504125268));
#26457=CARTESIAN_POINT('Ctrl Pts',(-1.89141354276916,4.25940153123874,7.13868697673655));
#26458=CARTESIAN_POINT('Ctrl Pts',(-4.60491865684703,0.717405574212831,
7.29757891222042));
#26459=CARTESIAN_POINT('Ctrl Pts',(-3.09748275458741,-3.48217563875277,
7.45647084770429));
#26460=CARTESIAN_POINT('Ctrl Pts',(1.24915465816929,-4.48993978067229,7.61536278318817));
#26461=CARTESIAN_POINT('Ctrl Pts',(4.45079722404066,-1.38215435627192,7.77425471867203));
#26462=CARTESIAN_POINT('Ctrl Pts',(3.57276890790401,2.99253553442627,7.93314665415592));
#26463=CARTESIAN_POINT('Ctrl Pts',(-0.580115697571088,4.62422019063984,
8.09203858963977));
#26464=CARTESIAN_POINT('Ctrl Pts',(-4.20125711178304,2.01727174044104,8.25093052512366));
#26465=CARTESIAN_POINT('Ctrl Pts',(-3.97146004374031,-2.43873978010442,
8.40982246060752));
#26466=CARTESIAN_POINT('Ctrl Pts',(-0.101360107710164,-4.65936398263266,
8.56871439609139));
#26467=CARTESIAN_POINT('Ctrl Pts',(3.86164810052541,-2.60914172512687,8.72760633157527));
#26468=CARTESIAN_POINT('Ctrl Pts',(4.28500879860717,1.83266095881065,8.88649826705913));
#26469=CARTESIAN_POINT('Ctrl Pts',(0.78066289832912,4.59461772438818,9.04539020254301));
#26470=CARTESIAN_POINT('Ctrl Pts',(-3.43925091813584,3.14507547066701,9.20428213802687));
#26471=CARTESIAN_POINT('Ctrl Pts',(-4.50669313898401,-1.18729252719113,
9.36317407351076));
#26472=CARTESIAN_POINT('Ctrl Pts',(-1.44322940124376,-4.431369482392,9.52206600899461));
#26473=CARTESIAN_POINT('Ctrl Pts',(2.94312115158416,-3.61358332976944,9.6809579444785));
#26474=CARTESIAN_POINT('Ctrl Pts',(4.63176047203213,0.516470254526036,9.83984987996235));
#26475=CARTESIAN_POINT('Ctrl Pts',(2.07485514530555,4.17311906373262,9.99874181544625));
#26476=CARTESIAN_POINT('Ctrl Pts',(-2.3838951082054,4.00462116899514,10.1576337509301));
#26477=CARTESIAN_POINT('Ctrl Pts',(-4.65752953433707,0.165424396228235,
10.316525686414));
#26478=CARTESIAN_POINT('Ctrl Pts',(-2.6619989846541,-3.82540298528012,10.4754176218978));
#26479=CARTESIAN_POINT('Ctrl Pts',(1.77356178859607,-4.30980570050686,10.6343095573817));
#26480=CARTESIAN_POINT('Ctrl Pts',(4.58344787433293,-0.843772586282874,
10.7932014928656));
#26481=CARTESIAN_POINT('Ctrl Pts',(3.19207340137333,3.39567577874192,10.9520934283495));
#26482=CARTESIAN_POINT('Ctrl Pts',(-1.12520585971602,4.52259420768106,11.1109853638333));
#26483=CARTESIAN_POINT('Ctrl Pts',(-4.41110369606797,1.50403150785647,11.2698772993172));
#26484=CARTESIAN_POINT('Ctrl Pts',(-3.65371436373851,-2.89315017624395,
11.4287692348011));
#26485=CARTESIAN_POINT('Ctrl Pts',(0.452727138482009,-4.63842481152508,
11.5876611702849));
#26486=CARTESIAN_POINT('Ctrl Pts',(4.14419181039819,-2.13204616101957,11.7465531057688));
#26487=CARTESIAN_POINT('Ctrl Pts',(4.03702495468236,2.32859960262844,11.9054450412527));
#26488=CARTESIAN_POINT('Ctrl Pts',(0.229457400278859,4.65481427078963,12.0643369767365));
#26489=CARTESIAN_POINT('Ctrl Pts',(-3.78843442356625,2.7143528164975,12.2232289122204));
#26490=CARTESIAN_POINT('Ctrl Pts',(-4.33378754743687,-1.71412720874813,
12.3821208477043));
#26491=CARTESIAN_POINT('Ctrl Pts',(-0.906722702996628,-4.57141121908323,
12.5410127831882));
#26492=CARTESIAN_POINT('Ctrl Pts',(3.35145846134476,-3.23846765862655,12.699904718672));
#26493=CARTESIAN_POINT('Ctrl Pts',(4.53763997961045,1.06290639735133,12.8587966541559));
#26494=CARTESIAN_POINT('Ctrl Pts',(1.56454917743418,4.39000369766127,13.0176885896398));
#26495=CARTESIAN_POINT('Ctrl Pts',(-2.84263205873703,3.69315442037428,13.1765805251236));
#26496=CARTESIAN_POINT('Ctrl Pts',(-4.6442119487827,-0.388898404308158,
13.3354724606075));
#26497=CARTESIAN_POINT('Ctrl Pts',(-2.1888339718237,-4.11448082239789,13.4943643960914));
#26498=CARTESIAN_POINT('Ctrl Pts',(2.27286372066084,-4.06866527271454,13.6532563315753));
#26499=CARTESIAN_POINT('Ctrl Pts',(4.65121870549125,-0.293447010170337,
13.8121482670591));
#26500=CARTESIAN_POINT('Ctrl Pts',(2.76619331968842,3.75074940674537,13.971040202543));
#26501=CARTESIAN_POINT('Ctrl Pts',(-1.65436845932101,4.35694980403646,14.1299321380269));
#26502=CARTESIAN_POINT('Ctrl Pts',(-4.55851003496805,0.969501343570532,
14.2888240735108));
#26503=CARTESIAN_POINT('Ctrl Pts',(-3.28424946851144,-3.30660732816461,
14.4477160089946));
#26504=CARTESIAN_POINT('Ctrl Pts',(1.00040592194765,-4.55182760936985,14.6066079444785));
#26505=CARTESIAN_POINT('Ctrl Pts',(4.36807347752778,-1.62477096509257,14.7654998799624));
#26506=CARTESIAN_POINT('Ctrl Pts',(3.73189604091493,2.79157635286821,14.9243918154462));
#26507=CARTESIAN_POINT('Ctrl Pts',(-0.324996123065272,4.64912078936244,
15.0832837509301));
#26508=CARTESIAN_POINT('Ctrl Pts',(-4.08399171856711,2.24520783821119,15.242175686414));
#26509=CARTESIAN_POINT('Ctrl Pts',(-4.09953613938831,-2.21669800287246,
15.4010676218978));
#26510=CARTESIAN_POINT('Ctrl Pts',(-0.357381124417536,-4.64674351842229,
15.5599595573817));
#26511=CARTESIAN_POINT('Ctrl Pts',(3.71235506167248,-2.81751069033718,15.7188514928656));
#26512=CARTESIAN_POINT('Ctrl Pts',(4.37928808994288,1.59429684167472,15.8777434283495));
#26513=CARTESIAN_POINT('Ctrl Pts',(1.03209663553355,4.54474676181302,16.0366353638333));
#26514=CARTESIAN_POINT('Ctrl Pts',(-3.26113086128664,3.32941017293654,16.1955272993172));
#26515=CARTESIAN_POINT('Ctrl Pts',(-4.56515441384568,-0.937716253370267,
16.3544192348011));
#26516=CARTESIAN_POINT('Ctrl Pts',(-1.68468548190361,-4.34531718303195,
16.5133111702849));
#26517=CARTESIAN_POINT('Ctrl Pts',(2.7399927141092,-3.76993189868439,16.6722031057688));
#26518=CARTESIAN_POINT('Ctrl Pts',(4.65315040492198,0.261032379723303,16.8310950412527));
#26519=CARTESIAN_POINT('Ctrl Pts',(2.30115709895892,4.05273026489556,16.9899869767366));
#26520=CARTESIAN_POINT('Ctrl Pts',(-2.16011307112194,4.12963171651633,17.1488789122204));
#26521=CARTESIAN_POINT('Ctrl Pts',(-4.64138955591407,0.421247652030533,
17.3077708477043));
#26522=CARTESIAN_POINT('Ctrl Pts',(-2.86829522348703,-3.67325864934817,
17.4666627831881));
#26523=CARTESIAN_POINT('Ctrl Pts',(1.53392371633779,-4.40079818061975,17.6255547186721));
#26524=CARTESIAN_POINT('Ctrl Pts',(4.53012400247882,-1.09449674108904,17.7844466541559));
#26525=CARTESIAN_POINT('Ctrl Pts',(3.37394123127184,3.21503766105686,17.9433385896398));
#26526=CARTESIAN_POINT('Ctrl Pts',(-0.874849247264209,4.57761787272052,
18.1022305251236));
#26527=CARTESIAN_POINT('Ctrl Pts',(-4.32173911776226,1.7442813970492,18.2611224606075));
#26528=CARTESIAN_POINT('Ctrl Pts',(-3.80725480047823,-2.68789089777271,
18.4200143960914));
#26529=CARTESIAN_POINT('Ctrl Pts',(0.197019270876202,-4.65630003339433,
18.5789063315753));
#26530=CARTESIAN_POINT('Ctrl Pts',(4.02070237343572,-2.35667117314485,18.7377982670591));
#26531=CARTESIAN_POINT('Ctrl Pts',(4.15894631253379,2.10311962655031,18.896690202543));
#26532=CARTESIAN_POINT('Ctrl Pts',(0.485034514796087,4.63515783048493,19.0555821380269));
#26533=CARTESIAN_POINT('Ctrl Pts',(-3.63346756353596,2.9185373149568,19.2144740735107));
#26534=CARTESIAN_POINT('Ctrl Pts',(-4.42147600817412,-1.47326050087259,
19.3733660089946));
#26535=CARTESIAN_POINT('Ctrl Pts',(-1.15668985931864,-4.51464452234266,
19.5322579444785));
#26536=CARTESIAN_POINT('Ctrl Pts',(3.16833644438965,-3.41783422201423,19.6911498799624));
#26537=CARTESIAN_POINT('Ctrl Pts',(4.58921562907606,0.811816792908698,19.8500418154462));
#26538=CARTESIAN_POINT('Ctrl Pts',(1.80354743972281,4.29734374053261,20.0089337509301));
#26539=CARTESIAN_POINT('Ctrl Pts',(-2.63528075670629,3.84385768827679,20.167825686414));
#26540=CARTESIAN_POINT('Ctrl Pts',(-4.65856908001299,-0.132968903128038,
20.3267176218978));
#26541=CARTESIAN_POINT('Ctrl Pts',(-2.41173956046629,-3.98791409989842,
20.4856095573818));
#26542=CARTESIAN_POINT('Ctrl Pts',(2.04572844434392,-4.18747438603111,20.6445014928655));
#26543=CARTESIAN_POINT('Ctrl Pts',(4.62804952678526,-0.548729644870818,
20.8033934283495));
#26544=CARTESIAN_POINT('Ctrl Pts',(2.96822745143777,3.59298932040533,20.9622853638333));
#26545=CARTESIAN_POINT('Ctrl Pts',(-1.4123186453351,4.44131767923527,21.1211772993172));
#26546=CARTESIAN_POINT('Ctrl Pts',(-4.49831129151882,1.21866419573831,21.2800692348011));
#26547=CARTESIAN_POINT('Ctrl Pts',(-3.46108076274892,-3.12103598071567,
21.438961170285));
#26548=CARTESIAN_POINT('Ctrl Pts',(0.748630655069918,-4.59994560901591,
21.5978531057688));
#26549=CARTESIAN_POINT('Ctrl Pts',(4.2721359622726,-1.86247217365839,21.7567450412527));
#26550=CARTESIAN_POINT('Ctrl Pts',(3.8797330719726,2.58217180475713,21.9156369767366));
#26551=CARTESIAN_POINT('Ctrl Pts',(-0.0688923048847857,4.65995794755513,
22.0745289122204));
#26552=CARTESIAN_POINT('Ctrl Pts',(-3.95437371638077,2.46635025785298,22.2334208477043));
#26553=CARTESIAN_POINT('Ctrl Pts',(-4.21520658614674,-1.98794734397253,
22.3923127831882));
#26554=CARTESIAN_POINT('Ctrl Pts',(-0.612328551070793,-4.62007178368083,
22.551204718672));
#26555=CARTESIAN_POINT('Ctrl Pts',(3.55184600275178,-3.01734516931811,22.7100966541559));
#26556=CARTESIAN_POINT('Ctrl Pts',(4.46029188758379,1.35108854037515,22.8689885896398));
#26557=CARTESIAN_POINT('Ctrl Pts',(1.28046065203078,4.48116776123978,23.0278805251236));
#26558=CARTESIAN_POINT('Ctrl Pts',(-3.07324571308582,3.50359559093557,23.1867724606075));
#26559=CARTESIAN_POINT('Ctrl Pts',(-4.60961384635985,-0.685155565682453,
23.3456643960914));
#26560=CARTESIAN_POINT('Ctrl Pts',(-1.9214110817744,-4.24640173773129,23.5045563315753));
#26561=CARTESIAN_POINT('Ctrl Pts',(2.52927486439223,-3.91433686410129,23.6634482670591));
#26562=CARTESIAN_POINT('Ctrl Pts',(4.65912272890548,0.00377285541425606,
23.822340202543));
#26563=CARTESIAN_POINT('Ctrl Pts',(2.52310591890791,3.92207527169042,23.9812321380269));
#26564=CARTESIAN_POINT('Ctrl Pts',(-1.93519005785514,4.23813764208779,24.1401240735107));
#26565=CARTESIAN_POINT('Ctrl Pts',(-3.71011270200011,1.86957801804229,24.2460520305));
#26566=CARTESIAN_POINT('Ctrl Pts',(-3.90033599543508,0.571614487844223,
24.2990160089946));
#26567=CARTESIAN_POINT('Ctrl Pts',(2.17834184062643,-3.05478403475391,-0.219489327336923));
#26568=CARTESIAN_POINT('Ctrl Pts',(3.19492048266714,-2.32987000971945,-0.166525348842299));
#26569=CARTESIAN_POINT('Ctrl Pts',(4.42978355814708,0.202135508380576,-0.0605973918530519));
#26570=CARTESIAN_POINT('Ctrl Pts',(2.22549083965568,3.84044901682883,0.0982945436308193));
#26571=CARTESIAN_POINT('Ctrl Pts',(-2.02066978786809,3.94732054903492,0.25718647911469));
#26572=CARTESIAN_POINT('Ctrl Pts',(-4.41362871485661,0.441633445237732,
0.416078414598561));
#26573=CARTESIAN_POINT('Ctrl Pts',(-2.76152266511234,-3.4717737462035,0.574970350082432));
#26574=CARTESIAN_POINT('Ctrl Pts',(1.42211964846881,-4.20137701828676,0.733862285566304));
#26575=CARTESIAN_POINT('Ctrl Pts',(4.30207750086251,-1.08072814831761,0.892754221050174));
#26576=CARTESIAN_POINT('Ctrl Pts',(3.23876037940132,3.03095006287751,1.05164615653404));
#26577=CARTESIAN_POINT('Ctrl Pts',(-0.793295903338713,4.36419339201584,
1.21053809201792));
#26578=CARTESIAN_POINT('Ctrl Pts',(-4.09818352865738,1.69726257423614,1.36943002750179));
#26579=CARTESIAN_POINT('Ctrl Pts',(-3.64662260642559,-2.52546571703568,
1.52832196298566));
#26580=CARTESIAN_POINT('Ctrl Pts',(0.147495862454333,-4.43328099194573,
1.68721389846953));
#26581=CARTESIAN_POINT('Ctrl Pts',(3.80641426574215,-2.27749744826117,1.8461058339534));
#26582=CARTESIAN_POINT('Ctrl Pts',(3.97631495072816,1.96588474289028,2.00499776943727));
#26583=CARTESIAN_POINT('Ctrl Pts',(0.501461851760338,4.40730149656556,2.16388970492114));
#26584=CARTESIAN_POINT('Ctrl Pts',(-3.43303864828577,2.80891859328985,2.32278164040501));
#26585=CARTESIAN_POINT('Ctrl Pts',(-4.22076204520191,-1.36416459585457,
2.48167357588889));
#26586=CARTESIAN_POINT('Ctrl Pts',(-1.13966831108264,-4.28683237073678,
2.64056551137275));
#26587=CARTESIAN_POINT('Ctrl Pts',(2.98606329610941,-3.28012237050456,2.79945744685663));
#26588=CARTESIAN_POINT('Ctrl Pts',(4.37472225720076,0.733199667739815,2.9583493823405));
#26589=CARTESIAN_POINT('Ctrl Pts',(1.75344183272134,4.07445924226969,3.11724131782437));
#26590=CARTESIAN_POINT('Ctrl Pts',(-2.47507100164175,3.68100530868232,3.27613325330824));
#26591=CARTESIAN_POINT('Ctrl Pts',(-4.43489475243097,-0.0865161304718975,
3.43502518879211));
#26592=CARTESIAN_POINT('Ctrl Pts',(-2.32962407485832,-3.77473550759247,
3.59391712427598));
#26593=CARTESIAN_POINT('Ctrl Pts',(1.91101674430454,-4.00297283399139,3.75280905975985));
#26594=CARTESIAN_POINT('Ctrl Pts',(4.39998949787803,-0.562022168553895,
3.91170099524372));
#26595=CARTESIAN_POINT('Ctrl Pts',(2.85586253164215,3.39408687237674,4.07059293072759));
#26596=CARTESIAN_POINT('Ctrl Pts',(-1.30599304051693,4.23912239483862,4.22948486621146));
#26597=CARTESIAN_POINT('Ctrl Pts',(-4.27075480883071,1.19851151930018,4.38837680169534));
#26598=CARTESIAN_POINT('Ctrl Pts',(-3.32087541041203,-2.94067390360441,
4.5472687371792));
#26599=CARTESIAN_POINT('Ctrl Pts',(0.672970727569009,-4.38439128034066,
4.70616067266308));
#26600=CARTESIAN_POINT('Ctrl Pts',(4.04996129037005,-1.8093065095749,4.86505260814695));
#26601=CARTESIAN_POINT('Ctrl Pts',(3.7146935053026,2.42421712326595,5.02394454363082));
#26602=CARTESIAN_POINT('Ctrl Pts',(-0.0255208918668632,4.43566513425159,
5.18283647911469));
#26603=CARTESIAN_POINT('Ctrl Pts',(-3.7423424373331,2.38131257520723,5.34172841459856));
#26604=CARTESIAN_POINT('Ctrl Pts',(-4.02887392383437,-1.85578862076283,
5.50062035008243));
#26605=CARTESIAN_POINT('Ctrl Pts',(-0.622476074987428,-4.39184471892869,
5.6595122855663));
#26606=CARTESIAN_POINT('Ctrl Pts',(3.35449315468027,-2.90226673038711,5.81840422105018));
#26607=CARTESIAN_POINT('Ctrl Pts',(4.25668109053274,1.24757468418137,5.97729615653404));
#26608=CARTESIAN_POINT('Ctrl Pts',(1.25712805170321,4.25386948092336,6.13618809201792));
#26609=CARTESIAN_POINT('Ctrl Pts',(-2.89472837218891,3.36100046866316,6.29508002750178));
#26610=CARTESIAN_POINT('Ctrl Pts',(-4.3932311479855,-0.61261454396674,6.45397196298565));
#26611=CARTESIAN_POINT('Ctrl Pts',(-1.86482901435204,-4.0246974105317,6.61286389846953));
#26612=CARTESIAN_POINT('Ctrl Pts',(2.37290478433289,-3.74767919966474,6.77175583395341));
#26613=CARTESIAN_POINT('Ctrl Pts',(4.43559665971225,-0.0354791693710577,
6.93064776943726));
#26614=CARTESIAN_POINT('Ctrl Pts',(2.43255072991432,3.7092416267349,7.08953970492115));
#26615=CARTESIAN_POINT('Ctrl Pts',(-1.80020953695449,4.05401308855407,7.248431640405));
#26616=CARTESIAN_POINT('Ctrl Pts',(-4.38286937018484,0.682812260438543,
7.40732357588889));
#26617=CARTESIAN_POINT('Ctrl Pts',(-2.94812206282321,-3.31426504700587,
7.56621551137276));
#26618=CARTESIAN_POINT('Ctrl Pts',(1.18892039097656,-4.27343477814157,7.72510744685661));
#26619=CARTESIAN_POINT('Ctrl Pts',(4.23617967651747,-1.31550684048772,7.88399938234051));
#26620=CARTESIAN_POINT('Ctrl Pts',(3.40048990657371,2.84823540010302,8.04289131782437));
#26621=CARTESIAN_POINT('Ctrl Pts',(-0.552142504899003,4.40124018356118,
8.20178325330824));
#26622=CARTESIAN_POINT('Ctrl Pts',(-3.99867239438119,1.91999884935475,8.36067518879212));
#26623=CARTESIAN_POINT('Ctrl Pts',(-3.7799561464003,-2.3211436901666,8.51956712427598));
#26624=CARTESIAN_POINT('Ctrl Pts',(-0.0964725209165242,-4.43468934107201,
8.67845905975986));
#26625=CARTESIAN_POINT('Ctrl Pts',(3.67543933768719,-2.48332884936554,8.83735099524372));
#26626=CARTESIAN_POINT('Ctrl Pts',(4.0783855728837,1.74429000398553,8.9962429307276));
#26627=CARTESIAN_POINT('Ctrl Pts',(0.743019314888223,4.37306514893305,9.15513486621146));
#26628=CARTESIAN_POINT('Ctrl Pts',(-3.2734101574334,2.99341985700662,9.31402680169534));
#26629=CARTESIAN_POINT('Ctrl Pts',(-4.28938028911884,-1.13004125341886,
9.4729187371792));
#26630=CARTESIAN_POINT('Ctrl Pts',(-1.37363684534497,-4.2176887410311,9.63181067266308));
#26631=CARTESIAN_POINT('Ctrl Pts',(2.80120377997153,-3.43933625605043,9.79070260814695));
#26632=CARTESIAN_POINT('Ctrl Pts',(4.40841687240619,0.491566046624494,9.94959454363082));
#26633=CARTESIAN_POINT('Ctrl Pts',(1.97480558107332,3.97189116367397,10.1084864791147));
#26634=CARTESIAN_POINT('Ctrl Pts',(-2.26894362964508,3.81151824141021,10.2673784145986));
#26635=CARTESIAN_POINT('Ctrl Pts',(-4.43294334991667,0.157447627925427,
10.4262703500824));
#26636=CARTESIAN_POINT('Ctrl Pts',(-2.53363733058688,-3.6409419627572,10.5851622855663));
#26637=CARTESIAN_POINT('Ctrl Pts',(1.68804059715796,-4.10198676758668,10.7440542210502));
#26638=CARTESIAN_POINT('Ctrl Pts',(4.36243390931193,-0.803085852194621,
10.902946156534));
#26639=CARTESIAN_POINT('Ctrl Pts',(3.03815154638153,3.23193621229276,11.0618380920179));
#26640=CARTESIAN_POINT('Ctrl Pts',(-1.07094840651941,4.30451460790682,11.2207300275018));
#26641=CARTESIAN_POINT('Ctrl Pts',(-4.19840017140343,1.43150707293723,11.3796219629857));
#26642=CARTESIAN_POINT('Ctrl Pts',(-3.47753217061135,-2.75364240624537,
11.5385138984695));
#26643=CARTESIAN_POINT('Ctrl Pts',(0.430896625145342,-4.41475985729101,
11.6974058339534));
#26644=CARTESIAN_POINT('Ctrl Pts',(3.94435878318021,-2.02923884465551,11.8562977694373));
#26645=CARTESIAN_POINT('Ctrl Pts',(3.84235951578439,2.21631447465625,12.0151897049212));
#26646=CARTESIAN_POINT('Ctrl Pts',(0.218392959004639,4.43035901644177,12.174081640405));
#26647=CARTESIAN_POINT('Ctrl Pts',(-3.60575602596446,2.58346665941922,12.3329735758889));
#26648=CARTESIAN_POINT('Ctrl Pts',(-4.12481220928992,-1.63147195415751,
12.4918655113728));
#26649=CARTESIAN_POINT('Ctrl Pts',(-0.86300051278999,-4.35097766186335,
12.6507574468566));
#26650=CARTESIAN_POINT('Ctrl Pts',(3.18985105498742,-3.08230867145154,12.8096493823405));
#26651=CARTESIAN_POINT('Ctrl Pts',(4.31883487235755,1.01165302570498,12.9685413178244));
#26652=CARTESIAN_POINT('Ctrl Pts',(1.48910657905504,4.17831761541948,13.1274332533082));
#26653=CARTESIAN_POINT('Ctrl Pts',(-2.70556027356073,3.51507042678234,13.2863251887921));
#26654=CARTESIAN_POINT('Ctrl Pts',(-4.42026793865305,-0.3701457140446,13.445217124276));
#26655=CARTESIAN_POINT('Ctrl Pts',(-2.08328834587812,-3.91608045972475,
13.6041090597598));
#26656=CARTESIAN_POINT('Ctrl Pts',(2.16326617823678,-3.87247413693191,13.7630009952437));
#26657=CARTESIAN_POINT('Ctrl Pts',(4.4269368293872,-0.279296988392094,13.9218929307276));
#26658=CARTESIAN_POINT('Ctrl Pts',(2.63280741231888,3.56988818154694,14.0807848662115));
#26659=CARTESIAN_POINT('Ctrl Pts',(-1.57459477304264,4.14685758132787,14.2396768016953));
#26660=CARTESIAN_POINT('Ctrl Pts',(-4.33869857315167,0.922751965829036,
14.3985687371792));
#26661=CARTESIAN_POINT('Ctrl Pts',(-3.12588288137982,-3.14716264451114,
14.5574606726631));
#26662=CARTESIAN_POINT('Ctrl Pts',(0.952166324705068,-4.33233837427404,
14.716352608147));
#26663=CARTESIAN_POINT('Ctrl Pts',(4.15744487102007,-1.54642447068669,14.8752445436308));
#26664=CARTESIAN_POINT('Ctrl Pts',(3.55194392546324,2.65696647503773,15.0341364791147));
#26665=CARTESIAN_POINT('Ctrl Pts',(-0.309324802316237,4.4249400748238,15.1930284145986));
#26666=CARTESIAN_POINT('Ctrl Pts',(-3.88706154120257,2.13694386309366,15.3519203500824));
#26667=CARTESIAN_POINT('Ctrl Pts',(-3.90185640968376,-2.10980877268997,
15.5108122855663));
#26668=CARTESIAN_POINT('Ctrl Pts',(-0.340148198136544,-4.42267743594467,
15.6697042210502));
#26669=CARTESIAN_POINT('Ctrl Pts',(3.53334521270251,-2.68165025813993,15.8285961565341));
#26670=CARTESIAN_POINT('Ctrl Pts',(4.168118714559,1.51741981022156,15.9874880920179));
#26671=CARTESIAN_POINT('Ctrl Pts',(0.982328911331549,4.32559896535404,16.1463800275018));
#26672=CARTESIAN_POINT('Ctrl Pts',(-3.10387905394275,3.16886593556829,16.3052719629857));
#26673=CARTESIAN_POINT('Ctrl Pts',(-4.3450225599225,-0.892499553430768,
16.4641638984695));
#26674=CARTESIAN_POINT('Ctrl Pts',(-1.60344990807853,-4.13578588558361,
16.6230558339534));
#26675=CARTESIAN_POINT('Ctrl Pts',(2.60787020056101,-3.5881456932705,16.7819477694373));
#26676=CARTESIAN_POINT('Ctrl Pts',(4.42877538222566,0.248445392192659,16.9408397049211));
#26677=CARTESIAN_POINT('Ctrl Pts',(2.19019524916345,3.85730751556724,17.099731640405));
#26678=CARTESIAN_POINT('Ctrl Pts',(-2.0559523676882,3.9305007773701,17.2586235758889));
#26679=CARTESIAN_POINT('Ctrl Pts',(-4.41758164163537,0.400935080275903,
17.4175155113728));
#26680=CARTESIAN_POINT('Ctrl Pts',(-2.72998595989888,-3.49613403030616,
17.5764074468566));
#26681=CARTESIAN_POINT('Ctrl Pts',(1.4599578784178,-4.18859158815413,17.7352993823405));
#26682=CARTESIAN_POINT('Ctrl Pts',(4.31168131582116,-1.04172008231973,17.8941913178244));
#26683=CARTESIAN_POINT('Ctrl Pts',(3.2112497052163,3.06000846891939,18.0530832533082));
#26684=CARTESIAN_POINT('Ctrl Pts',(-0.832663995847618,4.35688503051531,
18.2119751887921));
#26685=CARTESIAN_POINT('Ctrl Pts',(-4.11334475517948,1.66017210678477,18.370867124276));
#26686=CARTESIAN_POINT('Ctrl Pts',(-3.62366888385615,-2.55828073504186,
18.5297590597599));
#26687=CARTESIAN_POINT('Ctrl Pts',(0.187518996969786,-4.4317731355385,18.6886509952437));
#26688=CARTESIAN_POINT('Ctrl Pts',(3.82682400979189,-2.24303243337775,18.8475429307276));
#26689=CARTESIAN_POINT('Ctrl Pts',(3.95840182287352,2.00170714836323,19.0064348662115));
#26690=CARTESIAN_POINT('Ctrl Pts',(0.461646139008639,4.41165041015396,19.1653268016953));
#26691=CARTESIAN_POINT('Ctrl Pts',(-3.45826167159393,2.77780537652842,19.3242187371792));
#26692=CARTESIAN_POINT('Ctrl Pts',(-4.20827233037425,-1.40221984463863,
19.4831106726631));
#26693=CARTESIAN_POINT('Ctrl Pts',(-1.10091424691577,-4.29694825658366,
19.6420026081469));
#26694=CARTESIAN_POINT('Ctrl Pts',(3.01555918602559,-3.25302617490586,19.8008945436308));
#26695=CARTESIAN_POINT('Ctrl Pts',(4.36792354278479,0.772670967933531,19.9597864791147));
#26696=CARTESIAN_POINT('Ctrl Pts',(1.71658033947744,4.09012572361745,20.1186784145985));
#26697=CARTESIAN_POINT('Ctrl Pts',(-2.5082074562233,3.65850677953844,20.2775703500824));
#26698=CARTESIAN_POINT('Ctrl Pts',(-4.43393276867548,-0.126557139470934,
20.4364622855663));
#26699=CARTESIAN_POINT('Ctrl Pts',(-2.29544542175872,-3.79561678758089,
20.5953542210502));
#26700=CARTESIAN_POINT('Ctrl Pts',(1.94708337032167,-3.98555427199136,20.7542461565341));
#26701=CARTESIAN_POINT('Ctrl Pts',(4.40488486902698,-0.52226988840308,20.9131380920179));
#26702=CARTESIAN_POINT('Ctrl Pts',(2.82509945345179,3.41973529030544,21.0720300275018));
#26703=CARTESIAN_POINT('Ctrl Pts',(-1.34421660681807,4.22715723558706,21.2309219629857));
#26704=CARTESIAN_POINT('Ctrl Pts',(-4.28140261453686,1.15990017936594,21.3898138984695));
#26705=CARTESIAN_POINT('Ctrl Pts',(-3.29418736642239,-2.97053955182989,
21.5487058339534));
#26706=CARTESIAN_POINT('Ctrl Pts',(0.712531667157375,-4.37813612283788,
21.7075977694373));
#26707=CARTESIAN_POINT('Ctrl Pts',(4.06613346502197,-1.7726637213475,21.8664897049211));
#26708=CARTESIAN_POINT('Ctrl Pts',(3.69265225138302,2.45765941919457,22.025381640405));
#26709=CARTESIAN_POINT('Ctrl Pts',(-0.0655703163120924,4.43525466499184,
22.1842735758889));
#26710=CARTESIAN_POINT('Ctrl Pts',(-3.76369372215058,2.34742279002442,22.3431655113728));
#26711=CARTESIAN_POINT('Ctrl Pts',(-4.0119492247608,-1.89208847597824,22.5020574468566));
#26712=CARTESIAN_POINT('Ctrl Pts',(-0.582802053840284,-4.39729181288394,
22.6609493823405));
#26713=CARTESIAN_POINT('Ctrl Pts',(3.38057590440328,-2.87184871381299,22.8198413178244));
#26714=CARTESIAN_POINT('Ctrl Pts',(4.24521650715976,1.285939018969,22.9787332533082));
#26715=CARTESIAN_POINT('Ctrl Pts',(1.21871680907285,4.26508574569377,23.1376251887921));
#26716=CARTESIAN_POINT('Ctrl Pts',(-2.92505373203667,3.33465212858728,23.296517124276));
#26717=CARTESIAN_POINT('Ctrl Pts',(-4.38733815754819,-0.652117348083053,
23.4554090597599));
#26718=CARTESIAN_POINT('Ctrl Pts',(-1.82876059391868,-4.04164014539733,
23.6143009952437));
#26719=CARTESIAN_POINT('Ctrl Pts',(2.40731317054649,-3.72558744783597,23.7731929307276));
#26720=CARTESIAN_POINT('Ctrl Pts',(4.43445972060527,0.00359092823684341,
23.9320848662115));
#26721=CARTESIAN_POINT('Ctrl Pts',(2.4014416917595,3.73295270922791,24.0909768016953));
#26722=CARTESIAN_POINT('Ctrl Pts',(-1.84187514744654,4.03377454464145,24.2498687371792));
#26723=CARTESIAN_POINT('Ctrl Pts',(-3.53121097966664,1.77942692174697,24.3557966941685));
#26724=CARTESIAN_POINT('Ctrl Pts',(-3.71226170138833,0.544051223706471,
24.4087606726631));
#26725=CARTESIAN_POINT('Ctrl Pts',(2.06798052000209,-2.90001952809568,-0.109744663668461));
#26726=CARTESIAN_POINT('Ctrl Pts',(3.0330562439233,-2.2118318183024,-0.0567806851738377));
#26727=CARTESIAN_POINT('Ctrl Pts',(4.20535745823963,0.191894718237391,0.0491472718154096));
#26728=CARTESIAN_POINT('Ctrl Pts',(2.1127408095543,3.64588036952885,0.20803920729928));
#26729=CARTESIAN_POINT('Ctrl Pts',(-1.91829660558064,3.74733746988985,0.366931142783152));
#26730=CARTESIAN_POINT('Ctrl Pts',(-4.19002106768543,0.419258972444119,
0.525823078267022));
#26731=CARTESIAN_POINT('Ctrl Pts',(-2.62161565760238,-3.29588329210025,
0.684715013750895));
#26732=CARTESIAN_POINT('Ctrl Pts',(1.35007080858346,-3.98852267764505,0.843606949234764));
#26733=CARTESIAN_POINT('Ctrl Pts',(4.08412137222898,-1.02597522411638,1.00249888471864));
#26734=CARTESIAN_POINT('Ctrl Pts',(3.07467508021171,2.87739305660463,1.16139082020251));
#26735=CARTESIAN_POINT('Ctrl Pts',(-0.753105157375175,4.14309028633234,
1.32028275568638));
#26736=CARTESIAN_POINT('Ctrl Pts',(-3.89055727921005,1.61127416982435,1.47917469117025));
#26737=CARTESIAN_POINT('Ctrl Pts',(-3.46187378548392,-2.39751806138059,
1.63806662665412));
#26738=CARTESIAN_POINT('Ctrl Pts',(0.14002328039052,-4.20867770156907,1.79695856213799));
#26739=CARTESIAN_POINT('Ctrl Pts',(3.61356992084825,-2.16211260763564,1.95585049762186));
#26740=CARTESIAN_POINT('Ctrl Pts',(3.77486292837046,1.86628713503355,2.11474243310573));
#26741=CARTESIAN_POINT('Ctrl Pts',(0.476056292737952,4.18401440521967,2.27363436858961));
#26742=CARTESIAN_POINT('Ctrl Pts',(-3.2591106302341,2.66661036613276,2.43252630407347));
#26743=CARTESIAN_POINT('Ctrl Pts',(-4.0069256010488,-1.2950519324793,2.59141823955734));
#26744=CARTESIAN_POINT('Ctrl Pts',(-1.08192930174121,-4.0696486060465,2.75031017504122));
#26745=CARTESIAN_POINT('Ctrl Pts',(2.83478038785305,-3.11394154898843,2.90920211052509));
#26746=CARTESIAN_POINT('Ctrl Pts',(4.15308572767863,0.696053577028067,3.06809404600896));
#26747=CARTESIAN_POINT('Ctrl Pts',(1.66460721884761,3.8680349362124,3.22698598149283));
#26748=CARTESIAN_POINT('Ctrl Pts',(-2.34967649317396,3.49451455708637,3.3858779169767));
#26749=CARTESIAN_POINT('Ctrl Pts',(-4.21020970411577,-0.0821329642322605,
3.54476985246057));
#26750=CARTESIAN_POINT('Ctrl Pts',(-2.21159834323779,-3.58349610344751,
3.70366178794445));
#26751=CARTESIAN_POINT('Ctrl Pts',(1.81419891355671,-3.80017024344135,3.86255372342831));
#26752=CARTESIAN_POINT('Ctrl Pts',(4.1770728542812,-0.53354844253673,4.02144565891219));
#26753=CARTESIAN_POINT('Ctrl Pts',(2.71117598399594,3.22213226793253,4.18033759439605));
#26754=CARTESIAN_POINT('Ctrl Pts',(-1.23982752232801,4.02435576039341,4.33922952987993));
#26755=CARTESIAN_POINT('Ctrl Pts',(-4.05438558157035,1.13779133682627,4.4981214653638));
#26756=CARTESIAN_POINT('Ctrl Pts',(-3.15262991786046,-2.79169055788951,
4.65701340084767));
#26757=CARTESIAN_POINT('Ctrl Pts',(0.638876015320037,-4.16226488915267,
4.81590533633154));
#26758=CARTESIAN_POINT('Ctrl Pts',(3.84477812391437,-1.7176416238867,4.97479727181542));
#26759=CARTESIAN_POINT('Ctrl Pts',(3.5264960087876,2.30139902455706,5.13368920729927));
#26760=CARTESIAN_POINT('Ctrl Pts',(-0.0242279270633424,4.21094105608648,
5.29258114278316));
#26761=CARTESIAN_POINT('Ctrl Pts',(-3.55274416312754,2.26066814937938,5.45147307826701));
#26762=CARTESIAN_POINT('Ctrl Pts',(-3.82475910651287,-1.76176881213256,
5.61036501375091));
#26763=CARTESIAN_POINT('Ctrl Pts',(-0.590939573042961,-4.16934071422273,
5.76925694923476));
#26764=CARTESIAN_POINT('Ctrl Pts',(3.18454448653674,-2.75522920707652,5.92814888471864));
#26765=CARTESIAN_POINT('Ctrl Pts',(4.04102487998468,1.1843688148564,6.0870408202025));
#26766=CARTESIAN_POINT('Ctrl Pts',(1.19343818017234,4.03835571493739,6.24593275568638));
#26767=CARTESIAN_POINT('Ctrl Pts',(-2.74807276467801,3.19072212050733,6.40482469117025));
#26768=CARTESIAN_POINT('Ctrl Pts',(-4.17065690263191,-0.581577656713809,
6.56371662665412));
#26769=CARTESIAN_POINT('Ctrl Pts',(-1.77035119231138,-3.82079418788054,
6.72260856213799));
#26770=CARTESIAN_POINT('Ctrl Pts',(2.25268632236759,-3.5578105490987,6.88150049762186));
#26771=CARTESIAN_POINT('Ctrl Pts',(4.21087605067235,-0.033681688409442,
7.04039243310573));
#26772=CARTESIAN_POINT('Ctrl Pts',(2.30931042573792,3.52132033871361,7.19928436858961));
#26773=CARTESIAN_POINT('Ctrl Pts',(-1.70900553113983,3.84862464586941,7.35817630407347));
#26774=CARTESIAN_POINT('Ctrl Pts',(-4.16082008352265,0.648218946664257,
7.51706823955734));
#26775=CARTESIAN_POINT('Ctrl Pts',(-2.79876137105901,-3.14635445525897,
7.67596017504123));
#26776=CARTESIAN_POINT('Ctrl Pts',(1.12868612378383,-4.05692977561084,7.83485211052507));
#26777=CARTESIAN_POINT('Ctrl Pts',(4.02156212899428,-1.24885932470353,7.99374404600897));
#26778=CARTESIAN_POINT('Ctrl Pts',(3.2282109052434,2.70393526577978,8.15263598149282));
#26779=CARTESIAN_POINT('Ctrl Pts',(-0.524169312226923,4.1782601764825,8.3115279169767));
#26780=CARTESIAN_POINT('Ctrl Pts',(-3.79608767697933,1.82272595826847,8.47041985246058));
#26781=CARTESIAN_POINT('Ctrl Pts',(-3.5884522490603,-2.20354760022878,8.62931178794444));
#26782=CARTESIAN_POINT('Ctrl Pts',(-0.0915849341228856,-4.21001469951135,
8.78820372342831));
#26783=CARTESIAN_POINT('Ctrl Pts',(3.48923057484898,-2.35751597360421,8.94709565891219));
#26784=CARTESIAN_POINT('Ctrl Pts',(3.87176234716024,1.65591904916041,9.10598759439605));
#26785=CARTESIAN_POINT('Ctrl Pts',(0.705375731447328,4.15151257347791,9.26487952987993));
#26786=CARTESIAN_POINT('Ctrl Pts',(-3.10756939673095,2.84176424334623,9.42377146536379));
#26787=CARTESIAN_POINT('Ctrl Pts',(-4.07206743925366,-1.07278997964659,
9.58266340084768));
#26788=CARTESIAN_POINT('Ctrl Pts',(-1.30404428944617,-4.00400799967019,
9.74155533633153));
#26789=CARTESIAN_POINT('Ctrl Pts',(2.65928640835889,-3.26508918233143,9.90044727181542));
#26790=CARTESIAN_POINT('Ctrl Pts',(4.18507327278026,0.466661838722957,10.0593392072993));
#26791=CARTESIAN_POINT('Ctrl Pts',(1.87475601684109,3.77066326361532,10.2182311427832));
#26792=CARTESIAN_POINT('Ctrl Pts',(-2.15399215108477,3.61841531382528,10.377123078267));
#26793=CARTESIAN_POINT('Ctrl Pts',(-4.20835716549627,0.149470859622617,
10.5360150137509));
#26794=CARTESIAN_POINT('Ctrl Pts',(-2.40527567651967,-3.45648094023428,
10.6949069492348));
#26795=CARTESIAN_POINT('Ctrl Pts',(1.60251940571986,-3.89416783466651,10.8537988847186));
#26796=CARTESIAN_POINT('Ctrl Pts',(4.14141994429093,-0.762399118106369,
11.0126908202025));
#26797=CARTESIAN_POINT('Ctrl Pts',(2.88422969138973,3.06819664584361,11.1715827556864));
#26798=CARTESIAN_POINT('Ctrl Pts',(-1.01669095332279,4.08643500813259,11.3304746911703));
#26799=CARTESIAN_POINT('Ctrl Pts',(-3.98569664673889,1.35898263801798,11.4893666266541));
#26800=CARTESIAN_POINT('Ctrl Pts',(-3.30134997748419,-2.61413463624678,
11.648258562138));
#26801=CARTESIAN_POINT('Ctrl Pts',(0.409066111808665,-4.19109490305693,
11.8071504976218));
#26802=CARTESIAN_POINT('Ctrl Pts',(3.74452575596225,-1.92643152829146,11.9660424331058));
#26803=CARTESIAN_POINT('Ctrl Pts',(3.6476940768864,2.10402934668408,12.1249343685896));
#26804=CARTESIAN_POINT('Ctrl Pts',(0.207328517730425,4.20590376209391,12.2838263040735));
#26805=CARTESIAN_POINT('Ctrl Pts',(-3.42307762836267,2.45258050234096,12.4427182395573));
#26806=CARTESIAN_POINT('Ctrl Pts',(-3.91583687114297,-1.54881669956688,
12.6016101750412));
#26807=CARTESIAN_POINT('Ctrl Pts',(-0.819278322583353,-4.13054410464348,
12.7605021105251));
#26808=CARTESIAN_POINT('Ctrl Pts',(3.02824364863007,-2.92614968427652,12.919394046009));
#26809=CARTESIAN_POINT('Ctrl Pts',(4.10002976510464,0.960399654058624,13.0782859814928));
#26810=CARTESIAN_POINT('Ctrl Pts',(1.4136639806759,3.9666315331777,13.2371779169767));
#26811=CARTESIAN_POINT('Ctrl Pts',(-2.56848848838443,3.33698643319039,13.3960698524606));
#26812=CARTESIAN_POINT('Ctrl Pts',(-4.19632392852339,-0.351393023781037,
13.5549617879445));
#26813=CARTESIAN_POINT('Ctrl Pts',(-1.97774271993255,-3.71768009705162,
13.7138537234283));
#26814=CARTESIAN_POINT('Ctrl Pts',(2.05366863581272,-3.67628300114927,13.8727456589122));
#26815=CARTESIAN_POINT('Ctrl Pts',(4.20265495328316,-0.265146966613851,
14.0316375943961));
#26816=CARTESIAN_POINT('Ctrl Pts',(2.49942150494934,3.38902695634851,14.1905295298799));
#26817=CARTESIAN_POINT('Ctrl Pts',(-1.49482108676428,3.93676535861929,14.3494214653638));
#26818=CARTESIAN_POINT('Ctrl Pts',(-4.11888711133529,0.876002588087538,
14.5083134008477));
#26819=CARTESIAN_POINT('Ctrl Pts',(-2.96751629424819,-2.98771796085767,
14.6672053363315));
#26820=CARTESIAN_POINT('Ctrl Pts',(0.903926727462482,-4.11284913917822,
14.8260972718154));
#26821=CARTESIAN_POINT('Ctrl Pts',(3.94681626451235,-1.46807797628081,14.9849892072993));
#26822=CARTESIAN_POINT('Ctrl Pts',(3.37199181001155,2.52235659720725,15.1438811427832));
#26823=CARTESIAN_POINT('Ctrl Pts',(-0.293653481567197,4.20075936028517,
15.302773078267));
#26824=CARTESIAN_POINT('Ctrl Pts',(-3.69013136383804,2.02867988797614,15.4616650137509));
#26825=CARTESIAN_POINT('Ctrl Pts',(-3.7041766799792,-2.00291954250747,15.6205569492348));
#26826=CARTESIAN_POINT('Ctrl Pts',(-0.322915271855557,-4.19861135346705,
15.7794488847186));
#26827=CARTESIAN_POINT('Ctrl Pts',(3.35433536373254,-2.54578982594268,15.9383408202025));
#26828=CARTESIAN_POINT('Ctrl Pts',(3.95694933917511,1.44054277876839,16.0972327556863));
#26829=CARTESIAN_POINT('Ctrl Pts',(0.932561187129547,4.10645116889506,16.2561246911703));
#26830=CARTESIAN_POINT('Ctrl Pts',(-2.94662724659887,3.00832169820004,16.4150166266541));
#26831=CARTESIAN_POINT('Ctrl Pts',(-4.12489070599933,-0.847282853491266,
16.573908562138));
#26832=CARTESIAN_POINT('Ctrl Pts',(-1.52221433425345,-3.92625458813528,
16.7328004976219));
#26833=CARTESIAN_POINT('Ctrl Pts',(2.47574768701282,-3.40635948785661,16.8916924331057));
#26834=CARTESIAN_POINT('Ctrl Pts',(4.20440035952933,0.235858404662022,17.0505843685896));
#26835=CARTESIAN_POINT('Ctrl Pts',(2.07923339936798,3.66188476623891,17.2094763040735));
#26836=CARTESIAN_POINT('Ctrl Pts',(-1.95179166425446,3.73136983822386,17.3683682395573));
#26837=CARTESIAN_POINT('Ctrl Pts',(-4.19377372735666,0.380622508521273,
17.5272601750413));
#26838=CARTESIAN_POINT('Ctrl Pts',(-2.59167669631074,-3.31900941126415,
17.6861521105251));
#26839=CARTESIAN_POINT('Ctrl Pts',(1.38599204049781,-3.97638499568851,17.845044046009));
#26840=CARTESIAN_POINT('Ctrl Pts',(4.09323862916349,-0.988943423550422,
18.0039359814928));
#26841=CARTESIAN_POINT('Ctrl Pts',(3.04855817916078,2.90497927678192,18.1628279169767));
#26842=CARTESIAN_POINT('Ctrl Pts',(-0.79047874443103,4.13615218831009,18.3217198524606));
#26843=CARTESIAN_POINT('Ctrl Pts',(-3.9049503925967,1.57606281652034,18.4806117879444));
#26844=CARTESIAN_POINT('Ctrl Pts',(-3.44008296723408,-2.42867057231101,
18.6395037234283));
#26845=CARTESIAN_POINT('Ctrl Pts',(0.178018723063364,-4.20724623768266,
18.7983956589122));
#26846=CARTESIAN_POINT('Ctrl Pts',(3.63294564614808,-2.12939369361065,18.9572875943961));
#26847=CARTESIAN_POINT('Ctrl Pts',(3.75785733321325,1.90029467017615,19.1161795298799));
#26848=CARTESIAN_POINT('Ctrl Pts',(0.438257763221198,4.18814298982299,19.2750714653638));
#26849=CARTESIAN_POINT('Ctrl Pts',(-3.2830557796519,2.63707343810004,19.4339634008477));
#26850=CARTESIAN_POINT('Ctrl Pts',(-3.99506865257438,-1.33117918840468,
19.5928553363316));
#26851=CARTESIAN_POINT('Ctrl Pts',(-1.04513863451291,-4.07925199082465,
19.7517472718154));
#26852=CARTESIAN_POINT('Ctrl Pts',(2.86278192766154,-3.08821812779751,19.9106392072993));
#26853=CARTESIAN_POINT('Ctrl Pts',(4.14663145649351,0.733525142958367,20.0695311427831));
#26854=CARTESIAN_POINT('Ctrl Pts',(1.62961323923206,3.88290770670228,20.228423078267));
#26855=CARTESIAN_POINT('Ctrl Pts',(-2.3811341557403,3.47315587080009,20.3873150137509));
#26856=CARTESIAN_POINT('Ctrl Pts',(-4.20929645733797,-0.120145375813829,
20.5462069492348));
#26857=CARTESIAN_POINT('Ctrl Pts',(-2.17915128305114,-3.60331947526336,
20.7050988847187));
#26858=CARTESIAN_POINT('Ctrl Pts',(1.8484382962994,-3.78363415795159,20.8639908202025));
#26859=CARTESIAN_POINT('Ctrl Pts',(4.18172021126871,-0.495810131935346,
21.0228827556864));
#26860=CARTESIAN_POINT('Ctrl Pts',(2.6819714554658,3.24648126020556,21.1817746911702));
#26861=CARTESIAN_POINT('Ctrl Pts',(-1.27611456830103,4.01299679193883,21.3406666266541));
#26862=CARTESIAN_POINT('Ctrl Pts',(-4.0644939375549,1.10113616299357,21.499558562138));
#26863=CARTESIAN_POINT('Ctrl Pts',(-3.12729397009587,-2.82004312294412,
21.6584504976218));
#26864=CARTESIAN_POINT('Ctrl Pts',(0.676432679244829,-4.15632663665986,
21.8173424331058));
#26865=CARTESIAN_POINT('Ctrl Pts',(3.86013096777133,-1.68285526903662,21.9762343685896));
#26866=CARTESIAN_POINT('Ctrl Pts',(3.50557143079345,2.33314703363201,22.1351263040735));
#26867=CARTESIAN_POINT('Ctrl Pts',(-0.062248327739398,4.21055138242857,
22.2940182395573));
#26868=CARTESIAN_POINT('Ctrl Pts',(-3.57301372792039,2.22849532219585,22.4529101750413));
#26869=CARTESIAN_POINT('Ctrl Pts',(-3.80869186337486,-1.79622960798394,
22.6118021105251));
#26870=CARTESIAN_POINT('Ctrl Pts',(-0.553275556609776,-4.17451184208706,
22.770694046009));
#26871=CARTESIAN_POINT('Ctrl Pts',(3.20930580605478,-2.72635225830787,22.9295859814928));
#26872=CARTESIAN_POINT('Ctrl Pts',(4.03014112673573,1.22078949756286,23.0884779169767));
#26873=CARTESIAN_POINT('Ctrl Pts',(1.15697296611493,4.04900373014777,23.2473698524606));
#26874=CARTESIAN_POINT('Ctrl Pts',(-2.77686175098751,3.16570866623898,23.4062617879444));
#26875=CARTESIAN_POINT('Ctrl Pts',(-4.16506246873653,-0.619079130483647,
23.5651537234284));
#26876=CARTESIAN_POINT('Ctrl Pts',(-1.73611010606296,-3.83687855306338,
23.7240456589121));
#26877=CARTESIAN_POINT('Ctrl Pts',(2.28535147670074,-3.53683803157065,23.8829375943961));
#26878=CARTESIAN_POINT('Ctrl Pts',(4.20979671230505,0.00340900105942339,
24.0418295298799));
#26879=CARTESIAN_POINT('Ctrl Pts',(2.27977746461109,3.54383014676541,24.2007214653638));
#26880=CARTESIAN_POINT('Ctrl Pts',(-1.74856023703795,3.82941144719509,24.3596134008477));
#26881=CARTESIAN_POINT('Ctrl Pts',(-3.35230925733317,1.68927582545165,24.4655413578369));
#26882=CARTESIAN_POINT('Ctrl Pts',(-3.52418740734158,0.51648795956872,24.5185053363315));
#26883=CARTESIAN_POINT('Ctrl Pts',(1.95761919937776,-2.74525502143746,0.));
#26884=CARTESIAN_POINT('Ctrl Pts',(2.87119200517945,-2.09379362688536,0.0529639784946237));
#26885=CARTESIAN_POINT('Ctrl Pts',(3.98093135833217,0.181653928094203,0.158891935483871));
#26886=CARTESIAN_POINT('Ctrl Pts',(1.99999077945293,3.45131172222888,0.317783870967742));
#26887=CARTESIAN_POINT('Ctrl Pts',(-1.81592342329319,3.54735439074478,0.476675806451613));
#26888=CARTESIAN_POINT('Ctrl Pts',(-3.96641342051426,0.396884499650513,
0.635567741935484));
#26889=CARTESIAN_POINT('Ctrl Pts',(-2.48170865009243,-3.119992837997,0.794459677419355));
#26890=CARTESIAN_POINT('Ctrl Pts',(1.27802196869812,-3.77566833700333,0.953351612903227));
#26891=CARTESIAN_POINT('Ctrl Pts',(3.86616524359544,-0.97122229991515,1.1122435483871));
#26892=CARTESIAN_POINT('Ctrl Pts',(2.91058978102209,2.72383605033175,1.27113548387097));
#26893=CARTESIAN_POINT('Ctrl Pts',(-0.71291441141164,3.92198718064885,1.43002741935484));
#26894=CARTESIAN_POINT('Ctrl Pts',(-3.6829310297627,1.52528576541256,1.58891935483871));
#26895=CARTESIAN_POINT('Ctrl Pts',(-3.27712496454226,-2.26957040572551,
1.74781129032258));
#26896=CARTESIAN_POINT('Ctrl Pts',(0.13255069832671,-3.98407441119242,1.90670322580645));
#26897=CARTESIAN_POINT('Ctrl Pts',(3.42072557595435,-2.04672776701011,2.06559516129032));
#26898=CARTESIAN_POINT('Ctrl Pts',(3.57341090601276,1.76668952717683,2.2244870967742));
#26899=CARTESIAN_POINT('Ctrl Pts',(0.45065073371557,3.96072731387378,2.38337903225806));
#26900=CARTESIAN_POINT('Ctrl Pts',(-3.08518261218244,2.52430213897566,2.54227096774194));
#26901=CARTESIAN_POINT('Ctrl Pts',(-3.79308915689569,-1.22593926910403,
2.70116290322581));
#26902=CARTESIAN_POINT('Ctrl Pts',(-1.02419029239979,-3.85246484135621,
2.86005483870968));
#26903=CARTESIAN_POINT('Ctrl Pts',(2.68349747959669,-2.94776072747231,3.01894677419354));
#26904=CARTESIAN_POINT('Ctrl Pts',(3.9314491981565,0.658907486316316,3.17783870967743));
#26905=CARTESIAN_POINT('Ctrl Pts',(1.57577260497388,3.66161063015511,3.33673064516129));
#26906=CARTESIAN_POINT('Ctrl Pts',(-2.22428198470617,3.30802380549044,3.49562258064516));
#26907=CARTESIAN_POINT('Ctrl Pts',(-3.98552465580058,-0.07774979799263,
3.65451451612903));
#26908=CARTESIAN_POINT('Ctrl Pts',(-2.09357261161725,-3.39225669930255,
3.8134064516129));
#26909=CARTESIAN_POINT('Ctrl Pts',(1.71738108280889,-3.59736765289132,3.97229838709678));
#26910=CARTESIAN_POINT('Ctrl Pts',(3.95415621068438,-0.505074716519562,
4.13119032258065));
#26911=CARTESIAN_POINT('Ctrl Pts',(2.56648943634972,3.05017766348832,4.29008225806451));
#26912=CARTESIAN_POINT('Ctrl Pts',(-1.17366200413909,3.8095891259482,4.44897419354839));
#26913=CARTESIAN_POINT('Ctrl Pts',(-3.83801635431,1.07707115435234,4.60786612903225));
#26914=CARTESIAN_POINT('Ctrl Pts',(-2.98438442530889,-2.6427072121746,4.76675806451613));
#26915=CARTESIAN_POINT('Ctrl Pts',(0.604781303071069,-3.94013849796468,
4.92565));
#26916=CARTESIAN_POINT('Ctrl Pts',(3.63959495745868,-1.6259767381985,5.08454193548388));
#26917=CARTESIAN_POINT('Ctrl Pts',(3.3382985122726,2.17858092584818,5.24343387096774));
#26918=CARTESIAN_POINT('Ctrl Pts',(-0.0229349622598251,3.98621697792136,
5.40232580645161));
#26919=CARTESIAN_POINT('Ctrl Pts',(-3.36314588892197,2.14002372355154,5.56121774193549));
#26920=CARTESIAN_POINT('Ctrl Pts',(-3.62064428919136,-1.6677490035023,5.72010967741935));
#26921=CARTESIAN_POINT('Ctrl Pts',(-0.559403071098495,-3.94683670951677,
5.87900161290323));
#26922=CARTESIAN_POINT('Ctrl Pts',(3.01459581839321,-2.60819168376593,6.03789354838709));
#26923=CARTESIAN_POINT('Ctrl Pts',(3.82536866943663,1.12116294553142,6.19678548387097));
#26924=CARTESIAN_POINT('Ctrl Pts',(1.12974830864147,3.82284194895142,6.35567741935484));
#26925=CARTESIAN_POINT('Ctrl Pts',(-2.60141715716711,3.02044377235149,6.51456935483871));
#26926=CARTESIAN_POINT('Ctrl Pts',(-3.94808265727831,-0.550540769460877,
6.67346129032257));
#26927=CARTESIAN_POINT('Ctrl Pts',(-1.67587337027072,-3.61689096522939,
6.83235322580646));
#26928=CARTESIAN_POINT('Ctrl Pts',(2.13246786040229,-3.36794189853266,6.99124516129032));
#26929=CARTESIAN_POINT('Ctrl Pts',(3.98615544163244,-0.0318842074478251,
7.15013709677419));
#26930=CARTESIAN_POINT('Ctrl Pts',(2.18607012156152,3.33339905069232,7.30902903225807));
#26931=CARTESIAN_POINT('Ctrl Pts',(-1.61780152532516,3.64323620318475,7.46792096774193));
#26932=CARTESIAN_POINT('Ctrl Pts',(-3.93877079686046,0.613625632889965,
7.62681290322582));
#26933=CARTESIAN_POINT('Ctrl Pts',(-2.64940067929482,-2.97844386351206,
7.78570483870967));
#26934=CARTESIAN_POINT('Ctrl Pts',(1.06845185659111,-3.84042477308012,7.94459677419355));
#26935=CARTESIAN_POINT('Ctrl Pts',(3.80694458147109,-1.18221180891932,8.10348870967742));
#26936=CARTESIAN_POINT('Ctrl Pts',(3.0559319039131,2.55963513145653,8.2623806451613));
#26937=CARTESIAN_POINT('Ctrl Pts',(-0.49619611955484,3.95528016940384,8.42127258064515));
#26938=CARTESIAN_POINT('Ctrl Pts',(-3.59350295957747,1.72545306718219,8.58016451612905));
#26939=CARTESIAN_POINT('Ctrl Pts',(-3.39694835172031,-2.08595151029096,
8.7390564516129));
#26940=CARTESIAN_POINT('Ctrl Pts',(-0.086697347329244,-3.9853400579507,
8.89794838709678));
#26941=CARTESIAN_POINT('Ctrl Pts',(3.30302181201077,-2.23170309784288,9.05684032258065));
#26942=CARTESIAN_POINT('Ctrl Pts',(3.66513912143678,1.56754809433529,9.21573225806451));
#26943=CARTESIAN_POINT('Ctrl Pts',(0.667732148006428,3.92995999802278,9.3746241935484));
#26944=CARTESIAN_POINT('Ctrl Pts',(-2.94172863602851,2.69010862968584,9.53351612903225));
#26945=CARTESIAN_POINT('Ctrl Pts',(-3.85475458938848,-1.01553870587432,
9.69240806451614));
#26946=CARTESIAN_POINT('Ctrl Pts',(-1.23445173354738,-3.79032725830928,
9.85129999999999));
#26947=CARTESIAN_POINT('Ctrl Pts',(2.51736903674626,-3.09084210861242,10.0101919354839));
#26948=CARTESIAN_POINT('Ctrl Pts',(3.96172967315432,0.441757630821415,10.1690838709677));
#26949=CARTESIAN_POINT('Ctrl Pts',(1.77470645260886,3.56943536355667,10.3279758064516));
#26950=CARTESIAN_POINT('Ctrl Pts',(-2.03904067252446,3.42531238624034,10.4868677419355));
#26951=CARTESIAN_POINT('Ctrl Pts',(-3.98377098107586,0.14149409131981,10.6457596774194));
#26952=CARTESIAN_POINT('Ctrl Pts',(-2.27691402245245,-3.27201991771136,
10.8046516129032));
#26953=CARTESIAN_POINT('Ctrl Pts',(1.51699821428175,-3.68634890174633,10.9635435483871));
#26954=CARTESIAN_POINT('Ctrl Pts',(3.92040597926993,-0.721712384018116,
11.122435483871));
#26955=CARTESIAN_POINT('Ctrl Pts',(2.73030783639792,2.90445707939446,11.2813274193548));
#26956=CARTESIAN_POINT('Ctrl Pts',(-0.962433500126168,3.86835540835836,
11.4402193548387));
#26957=CARTESIAN_POINT('Ctrl Pts',(-3.77299312207436,1.28645820309873,11.5991112903226));
#26958=CARTESIAN_POINT('Ctrl Pts',(-3.12516778435703,-2.4746268662482,11.7580032258064));
#26959=CARTESIAN_POINT('Ctrl Pts',(0.38723559847199,-3.96742994882286,11.9168951612903));
#26960=CARTESIAN_POINT('Ctrl Pts',(3.54469272874429,-1.82362421192741,12.0757870967742));
#26961=CARTESIAN_POINT('Ctrl Pts',(3.45302863798842,1.9917442187119,12.2346790322581));
#26962=CARTESIAN_POINT('Ctrl Pts',(0.196264076456207,3.98144850774605,12.3935709677419));
#26963=CARTESIAN_POINT('Ctrl Pts',(-3.24039923076088,2.32169434526269,12.5524629032258));
#26964=CARTESIAN_POINT('Ctrl Pts',(-3.70686153299603,-1.46616144497625,
12.7113548387097));
#26965=CARTESIAN_POINT('Ctrl Pts',(-0.775556132376715,-3.9101105474236,
12.8702467741936));
#26966=CARTESIAN_POINT('Ctrl Pts',(2.86663624227273,-2.76999069710151,13.0291387096774));
#26967=CARTESIAN_POINT('Ctrl Pts',(3.88122465785174,0.909146282412278,13.1880306451613));
#26968=CARTESIAN_POINT('Ctrl Pts',(1.33822138229676,3.75494545093591,13.3469225806451));
#26969=CARTESIAN_POINT('Ctrl Pts',(-2.43141670320813,3.15890243959844,13.5058145161291));
#26970=CARTESIAN_POINT('Ctrl Pts',(-3.97237991839373,-0.332640333517474,
13.6647064516129));
#26971=CARTESIAN_POINT('Ctrl Pts',(-1.87219709398698,-3.51927973437849,
13.8235983870968));
#26972=CARTESIAN_POINT('Ctrl Pts',(1.94407109338865,-3.48009186536664,13.9824903225806));
#26973=CARTESIAN_POINT('Ctrl Pts',(3.97837307717912,-0.25099694483561,14.1413822580645));
#26974=CARTESIAN_POINT('Ctrl Pts',(2.36603559757979,3.20816573115008,14.3002741935484));
#26975=CARTESIAN_POINT('Ctrl Pts',(-1.41504740048591,3.7266731359107,14.4591661290323));
#26976=CARTESIAN_POINT('Ctrl Pts',(-3.8990756495189,0.82925321034604,14.6180580645161));
#26977=CARTESIAN_POINT('Ctrl Pts',(-2.80914970711657,-2.8282732772042,14.77695));
#26978=CARTESIAN_POINT('Ctrl Pts',(0.8556871302199,-3.8933599040824,14.9358419354839));
#26979=CARTESIAN_POINT('Ctrl Pts',(3.73618765800463,-1.38973148187494,15.0947338709677));
#26980=CARTESIAN_POINT('Ctrl Pts',(3.19203969455987,2.38774671937678,15.2536258064516));
#26981=CARTESIAN_POINT('Ctrl Pts',(-0.277982160818163,3.97657864574653,
15.4125177419355));
#26982=CARTESIAN_POINT('Ctrl Pts',(-3.4932011864735,1.92041591285862,15.5714096774194));
#26983=CARTESIAN_POINT('Ctrl Pts',(-3.50649695027464,-1.89603031232498,
15.7303016129032));
#26984=CARTESIAN_POINT('Ctrl Pts',(-0.30568234557457,-3.97454527098943,
15.8891935483871));
#26985=CARTESIAN_POINT('Ctrl Pts',(3.17532551476257,-2.40992939374543,16.048085483871));
#26986=CARTESIAN_POINT('Ctrl Pts',(3.74577996379122,1.36366574731522,16.2069774193548));
#26987=CARTESIAN_POINT('Ctrl Pts',(0.882793462927545,3.88730337243608,16.3658693548387));
#26988=CARTESIAN_POINT('Ctrl Pts',(-2.78937543925498,2.84777746083178,16.5247612903226));
#26989=CARTESIAN_POINT('Ctrl Pts',(-3.90475885207616,-0.802066153551767,
16.6836532258065));
#26990=CARTESIAN_POINT('Ctrl Pts',(-1.44097876042837,-3.71672329068694,
16.8425451612903));
#26991=CARTESIAN_POINT('Ctrl Pts',(2.34362517346463,-3.22457328244272,17.0014370967742));
#26992=CARTESIAN_POINT('Ctrl Pts',(3.980025336833,0.223271417131382,17.1603290322581));
#26993=CARTESIAN_POINT('Ctrl Pts',(1.96827154957251,3.46646201691059,17.3192209677419));
#26994=CARTESIAN_POINT('Ctrl Pts',(-1.84763096082072,3.53223889907763,17.4781129032258));
#26995=CARTESIAN_POINT('Ctrl Pts',(-3.96996581307795,0.360309936766638,
17.6370048387097));
#26996=CARTESIAN_POINT('Ctrl Pts',(-2.4533674327226,-3.14188479222213,17.7958967741935));
#26997=CARTESIAN_POINT('Ctrl Pts',(1.31202620257783,-3.7641784032229,17.9547887096774));
#26998=CARTESIAN_POINT('Ctrl Pts',(3.87479594250582,-0.936166764781103,
18.1136806451613));
#26999=CARTESIAN_POINT('Ctrl Pts',(2.88586665310525,2.74995008464444,18.2725725806452));
#27000=CARTESIAN_POINT('Ctrl Pts',(-0.748293493014444,3.91541934610488,
18.431464516129));
#27001=CARTESIAN_POINT('Ctrl Pts',(-3.69655603001392,1.49195352625591,18.5903564516129));
#27002=CARTESIAN_POINT('Ctrl Pts',(-3.25649705061201,-2.29906040958017,
18.7492483870968));
#27003=CARTESIAN_POINT('Ctrl Pts',(0.168518449156949,-3.98271933982683,
18.9081403225806));
#27004=CARTESIAN_POINT('Ctrl Pts',(3.43906728250426,-2.01575495384355,19.0670322580645));
#27005=CARTESIAN_POINT('Ctrl Pts',(3.55731284355299,1.79888219198906,19.2259241935484));
#27006=CARTESIAN_POINT('Ctrl Pts',(0.41486938743375,3.96463556949202,19.3848161290323));
#27007=CARTESIAN_POINT('Ctrl Pts',(-3.10784988770987,2.49634149967166,19.5437080645161));
#27008=CARTESIAN_POINT('Ctrl Pts',(-3.78186497477451,-1.26013853217073,
19.7026));
#27009=CARTESIAN_POINT('Ctrl Pts',(-0.989363022110038,-3.86155572506565,
19.8614919354839));
#27010=CARTESIAN_POINT('Ctrl Pts',(2.71000466929749,-2.92341008068914,20.0203838709678));
#27011=CARTESIAN_POINT('Ctrl Pts',(3.92533937020224,0.694379317983201,20.1792758064516));
#27012=CARTESIAN_POINT('Ctrl Pts',(1.54264613898669,3.6756896897871,20.3381677419355));
#27013=CARTESIAN_POINT('Ctrl Pts',(-2.25406085525731,3.28780496206174,20.4970596774194));
#27014=CARTESIAN_POINT('Ctrl Pts',(-3.98466014600046,-0.113733612156729,
20.6559516129032));
#27015=CARTESIAN_POINT('Ctrl Pts',(-2.06285714434356,-3.41102216294582,
20.8148435483871));
#27016=CARTESIAN_POINT('Ctrl Pts',(1.74979322227715,-3.58171404391184,20.9737354838709));
#27017=CARTESIAN_POINT('Ctrl Pts',(3.95855555351044,-0.46935037546761,21.1326274193549));
#27018=CARTESIAN_POINT('Ctrl Pts',(2.53884345747981,3.07322723010567,21.2915193548387));
#27019=CARTESIAN_POINT('Ctrl Pts',(-1.20801252978399,3.79883634829061,21.4504112903226));
#27020=CARTESIAN_POINT('Ctrl Pts',(-3.84758526057294,1.0423721466212,21.6093032258064));
#27021=CARTESIAN_POINT('Ctrl Pts',(-2.96040057376934,-2.66954669405833,
21.7681951612904));
#27022=CARTESIAN_POINT('Ctrl Pts',(0.640333691332285,-3.93451715048184,
21.9270870967742));
#27023=CARTESIAN_POINT('Ctrl Pts',(3.6541284705207,-1.59304681672573,22.0859790322581));
#27024=CARTESIAN_POINT('Ctrl Pts',(3.31849061020388,2.20863464806944,22.2448709677419));
#27025=CARTESIAN_POINT('Ctrl Pts',(-0.058926339166703,3.98584809986529,
22.4037629032258));
#27026=CARTESIAN_POINT('Ctrl Pts',(-3.3823337336902,2.1095678543673,22.5626548387097));
#27027=CARTESIAN_POINT('Ctrl Pts',(-3.60543450198892,-1.70037073998966,
22.7215467741936));
#27028=CARTESIAN_POINT('Ctrl Pts',(-0.52374905937927,-3.95173187129016,
22.8804387096774));
#27029=CARTESIAN_POINT('Ctrl Pts',(3.03803570770629,-2.58085580280275,23.0393306451613));
#27030=CARTESIAN_POINT('Ctrl Pts',(3.81506574631169,1.15563997615671,23.1982225806452));
#27031=CARTESIAN_POINT('Ctrl Pts',(1.095229123157,3.83292171460177,23.357114516129));
#27032=CARTESIAN_POINT('Ctrl Pts',(-2.62866976993836,2.99676520389069,23.5160064516129));
#27033=CARTESIAN_POINT('Ctrl Pts',(-3.94278677992486,-0.586040912884242,
23.6748983870968));
#27034=CARTESIAN_POINT('Ctrl Pts',(-1.64345961820725,-3.63211696072943,
23.8337903225806));
#27035=CARTESIAN_POINT('Ctrl Pts',(2.163389782855,-3.34808861530533,23.9926822580645));
#27036=CARTESIAN_POINT('Ctrl Pts',(3.98513370400483,0.0032270738820094,
24.1515741935484));
#27037=CARTESIAN_POINT('Ctrl Pts',(2.15811323746268,3.35470758430291,24.3104661290323));
#27038=CARTESIAN_POINT('Ctrl Pts',(-1.65524532662936,3.62504834974875,24.4693580645161));
#27039=CARTESIAN_POINT('Ctrl Pts',(-3.1734075349997,1.59912472915632,24.5752860215054));
#27040=CARTESIAN_POINT('Ctrl Pts',(-3.33611311329483,0.488924695430968,
24.62825));
#27041=CARTESIAN_POINT('',(1.95761919937778,-2.74525502143744,0.));
#27042=CARTESIAN_POINT('Ctrl Pts',(1.95761919937776,-2.74525502143746,0.));
#27043=CARTESIAN_POINT('Ctrl Pts',(2.87119200517945,-2.09379362688536,0.0529639784946237));
#27044=CARTESIAN_POINT('Ctrl Pts',(3.98093135833217,0.181653928094203,0.158891935483871));
#27045=CARTESIAN_POINT('Ctrl Pts',(1.99999077945293,3.45131172222888,0.317783870967742));
#27046=CARTESIAN_POINT('Ctrl Pts',(-1.81592342329319,3.54735439074478,0.476675806451613));
#27047=CARTESIAN_POINT('Ctrl Pts',(-3.32105516281529,1.34233496093003,0.58788455216069));
#27048=CARTESIAN_POINT('Ctrl Pts',(-3.3766520624322,0.1136195821916,0.646129319375144));
#27049=CARTESIAN_POINT('Ctrl Pts',(-3.37589447807987,0.0021436428109594,
0.651410108094974));
#27050=CARTESIAN_POINT('Ctrl Pts',(1.73118107496478,3.54876586530513,2.39391839684799E-16));
#27051=CARTESIAN_POINT('Ctrl Pts',(1.81301063452785,3.50205269354806,2.06920727311338E-16));
#27052=CARTESIAN_POINT('Ctrl Pts',(1.89292240658196,3.4522795469799,5.6760153975772E-16));
#27053=CARTESIAN_POINT('Ctrl Pts',(1.97072352421092,3.39943606703627,2.9316826744008E-16));
#27054=CARTESIAN_POINT('Ctrl Pts',(2.07158749034463,3.33092801556019,-4.87384004076243E-17));
#27055=CARTESIAN_POINT('Ctrl Pts',(2.16890551010069,3.25726040082769,-6.1331688516479E-17));
#27056=CARTESIAN_POINT('Ctrl Pts',(2.26249391432527,3.17884397520376,-1.04083408558608E-17));
#27057=CARTESIAN_POINT('Ctrl Pts',(2.31703211703773,3.13314717171513,1.92670006623856E-17));
#27058=CARTESIAN_POINT('Ctrl Pts',(2.37030307443948,3.08583698417059,-9.57318163015451E-16));
#27059=CARTESIAN_POINT('Ctrl Pts',(2.42226407127706,3.03698980450436,-1.02695629777827E-15));
#27060=CARTESIAN_POINT('Ctrl Pts',(2.45441149625484,3.00676884764696,-1.07004028094122E-15));
#27061=CARTESIAN_POINT('Ctrl Pts',(2.48605741280453,2.97595951290433,-8.19532942944583E-16));
#27062=CARTESIAN_POINT('Ctrl Pts',(2.51719072732778,2.9445793777147,-8.39606162372775E-16));
#27063=CARTESIAN_POINT('Ctrl Pts',(2.53181221876951,2.92984196908534,-8.49033375972473E-16));
#27064=CARTESIAN_POINT('Ctrl Pts',(2.54632072268487,2.91497845934833,-6.96615474306211E-16));
#27065=CARTESIAN_POINT('Ctrl Pts',(2.56070494112922,2.90000148244637,-7.07767178198537E-16));
#27066=CARTESIAN_POINT('Ctrl Pts',(2.64790074151672,2.80921243517189,-7.75367774667319E-16));
#27067=CARTESIAN_POINT('Ctrl Pts',(2.73062866917384,2.71416182380689,-8.593918943852E-16));
#27068=CARTESIAN_POINT('Ctrl Pts',(2.80868748257388,2.61529981528879,-7.7715611723761E-16));
#27069=CARTESIAN_POINT('Ctrl Pts',(2.87698894429891,2.52879555783546,-7.05199812233468E-16));
#27070=CARTESIAN_POINT('Ctrl Pts',(2.94171511816388,2.43937213712426,-7.20848724153807E-16));
#27071=CARTESIAN_POINT('Ctrl Pts',(3.00269897791456,2.3473133317077,-6.24500451351651E-16));
#27072=CARTESIAN_POINT('Ctrl Pts',(3.02937941655548,2.30703760433796,-5.82348082000707E-16));
#27073=CARTESIAN_POINT('Ctrl Pts',(3.05534314365639,2.26625728440317,-1.08606649764317E-16));
#27074=CARTESIAN_POINT('Ctrl Pts',(3.08057418911428,2.22499554197223,-6.93889390390723E-17));
#27075=CARTESIAN_POINT('Ctrl Pts',(3.09523937783659,2.20101273710704,-4.6594198725879E-17));
#27076=CARTESIAN_POINT('Ctrl Pts',(3.10965701779078,2.17686728558595,-1.5350788780052E-16));
#27077=CARTESIAN_POINT('Ctrl Pts',(3.12382377516257,2.1525637049523,-1.66533453693773E-16));
#27078=CARTESIAN_POINT('Ctrl Pts',(3.1333468514065,2.13622652592816,-1.75289406369904E-16));
#27079=CARTESIAN_POINT('Ctrl Pts',(3.14275743380374,2.11981622896702,-6.17919290773945E-16));
#27080=CARTESIAN_POINT('Ctrl Pts',(3.15204614385832,2.10334928089744,-6.10622663543836E-16));
#27081=CARTESIAN_POINT('Ctrl Pts',(3.21133027918083,1.99825085797653,-5.64052770246931E-16));
#27082=CARTESIAN_POINT('Ctrl Pts',(3.26572921710173,1.89071971149897,-2.93721959998899E-16));
#27083=CARTESIAN_POINT('Ctrl Pts',(3.3150665440347,1.78114320161924,-3.46944695195361E-16));
#27084=CARTESIAN_POINT('Ctrl Pts',(3.36416434269629,1.67209867580975,-3.99909038813826E-16));
#27085=CARTESIAN_POINT('Ctrl Pts',(3.40824985101865,1.5610277430108,-6.74639111044964E-16));
#27086=CARTESIAN_POINT('Ctrl Pts',(3.44710068203266,1.44829560050515,-7.21644966006352E-16));
#27087=CARTESIAN_POINT('Ctrl Pts',(3.48485757303191,1.33873770674576,-7.67327256340457E-16));
#27088=CARTESIAN_POINT('Ctrl Pts',(3.51767049623361,1.22761008128266,-7.45739296926402E-16));
#27089=CARTESIAN_POINT('Ctrl Pts',(3.54528704260767,1.11524410687019,-6.10622663543836E-16));
#27090=CARTESIAN_POINT('Ctrl Pts',(3.56429882714017,1.03788911593903,-5.17605662582399E-16));
#27091=CARTESIAN_POINT('Ctrl Pts',(3.58084694549942,0.959947166702576,1.01128139593754E-16));
#27092=CARTESIAN_POINT('Ctrl Pts',(3.59483483174014,0.881527990398642,1.38777878078145E-16));
#27093=CARTESIAN_POINT('Ctrl Pts',(3.60174616248926,0.842781545425996,1.5738038819335E-16));
#27094=CARTESIAN_POINT('Ctrl Pts',(3.60803228263339,0.803918629301433,-8.2431208915498E-16));
#27095=CARTESIAN_POINT('Ctrl Pts',(3.6136804381616,0.764952740225288,-8.60422844084496E-16));
#27096=CARTESIAN_POINT('Ctrl Pts',(3.61598402562173,0.749060590478247,-8.75150533826084E-16));
#27097=CARTESIAN_POINT('Ctrl Pts',(3.6181800809526,0.733160977259198,-9.56453568707426E-16));
#27098=CARTESIAN_POINT('Ctrl Pts',(3.62026800126996,0.71725566677106,-9.43689570931383E-16));
#27099=CARTESIAN_POINT('Ctrl Pts',(3.63517124652415,0.603726074153541,-8.52582172005361E-16));
#27100=CARTESIAN_POINT('Ctrl Pts',(3.64457137343043,0.489891978911761,1.54068630345449E-16));
#27101=CARTESIAN_POINT('Ctrl Pts',(3.64826597516095,0.3760806489335,1.38777878078145E-16));
#27102=CARTESIAN_POINT('Ctrl Pts',(3.65049038519446,0.307558225463841,1.29571770019922E-16));
#27103=CARTESIAN_POINT('Ctrl Pts',(3.65064564728474,0.239043959798587,2.28153843810054E-16));
#27104=CARTESIAN_POINT('Ctrl Pts',(3.64867842117138,0.170609648189261,1.38777878078145E-16));
#27105=CARTESIAN_POINT('Ctrl Pts',(3.64536397368567,0.0553092612588858,
-9.22057312926959E-18));
#27106=CARTESIAN_POINT('Ctrl Pts',(3.63602703897368,-0.0597651999246838,
-3.71059406415836E-16));
#27107=CARTESIAN_POINT('Ctrl Pts',(3.62088618085986,-0.174255990612961,
-4.44089209850063E-16));
#27108=CARTESIAN_POINT('Ctrl Pts',(3.60564019443288,-0.289541731204713,
-5.17626084943432E-16));
#27109=CARTESIAN_POINT('Ctrl Pts',(3.58450894234823,-0.404236478340693,
2.06881119674206E-16));
#27110=CARTESIAN_POINT('Ctrl Pts',(3.55766829556208,-0.517952337059044,
1.66533453693773E-16));
#27111=CARTESIAN_POINT('Ctrl Pts',(3.55209090522836,-0.541582085487224,
1.58149353116006E-16));
#27112=CARTESIAN_POINT('Ctrl Pts',(3.54626683911464,-0.565169464342046,
2.72822796152711E-16));
#27113=CARTESIAN_POINT('Ctrl Pts',(3.54019745029697,-0.588710821151176,
2.77555756156289E-16));
#27114=CARTESIAN_POINT('Ctrl Pts',(3.53607649256559,-0.604694792398417,
2.80769313353732E-16));
#27115=CARTESIAN_POINT('Ctrl Pts',(3.53184170988113,-0.62066020100356,-1.61867697048363E-17));
#27116=CARTESIAN_POINT('Ctrl Pts',(3.52749592285427,-0.636597072708719,
-2.77555756156289E-17));
#27117=CARTESIAN_POINT('Ctrl Pts',(3.49747618222011,-0.7466854760641,-1.07670341512578E-16));
#27118=CARTESIAN_POINT('Ctrl Pts',(3.46222700262188,-0.855189606000695,
-1.99543722780696E-16));
#27119=CARTESIAN_POINT('Ctrl Pts',(3.42199607778626,-0.961778490999782,
-2.77555756156289E-16));
#27120=CARTESIAN_POINT('Ctrl Pts',(3.38156991618782,-1.0688846414842,-3.55946374337476E-16));
#27121=CARTESIAN_POINT('Ctrl Pts',(3.33611303054141,-1.17405769074672,1.35240542225809E-16));
#27122=CARTESIAN_POINT('Ctrl Pts',(3.28582849960376,-1.27693996092432,1.11022302462516E-16));
#27123=CARTESIAN_POINT('Ctrl Pts',(3.23598893769955,-1.3789118233987,8.70183704900679E-17));
#27124=CARTESIAN_POINT('Ctrl Pts',(3.18140622212873,-1.47863395215989,2.26466381867324E-16));
#27125=CARTESIAN_POINT('Ctrl Pts',(3.1222390297712,-1.57572584500942,2.22044604925031E-16));
#27126=CARTESIAN_POINT('Ctrl Pts',(3.08604888850041,-1.6351129678129,2.19339985594059E-16));
#27127=CARTESIAN_POINT('Ctrl Pts',(3.04814284654775,-1.69351537716898,-1.98475779326559E-16));
#27128=CARTESIAN_POINT('Ctrl Pts',(3.00855126708734,-1.75083831899302,-2.22044604925031E-16));
#27129=CARTESIAN_POINT('Ctrl Pts',(2.9875142347103,-1.78129693164588,-2.34567928166019E-16));
#27130=CARTESIAN_POINT('Ctrl Pts',(2.96600124729196,-1.81145066683922,-9.64459754115302E-17));
#27131=CARTESIAN_POINT('Ctrl Pts',(2.94401641708542,-1.8412845286552,-1.11022302462516E-16));
#27132=CARTESIAN_POINT('Ctrl Pts',(2.93430327275808,-1.85446546309672,-1.17462287082754E-16));
#27133=CARTESIAN_POINT('Ctrl Pts',(2.92449763119146,-1.86758436264681,1.18006511135168E-16));
#27134=CARTESIAN_POINT('Ctrl Pts',(2.91460943608169,-1.8806275411502,1.11022302462516E-16));
#27135=CARTESIAN_POINT('Ctrl Pts',(2.8471863415804,-1.96956302907997,6.34001675707856E-17));
#27136=CARTESIAN_POINT('Ctrl Pts',(2.77582498992288,-2.05512251526362,-2.18484873575661E-16));
#27137=CARTESIAN_POINT('Ctrl Pts',(2.70071126790977,-2.13697549169768,-1.66533453693773E-16));
#27138=CARTESIAN_POINT('Ctrl Pts',(2.6265626894838,-2.21777673120304,-1.1524956270538E-16));
#27139=CARTESIAN_POINT('Ctrl Pts',(2.54875698937316,-2.29496666804747,3.16111469076589E-16));
#27140=CARTESIAN_POINT('Ctrl Pts',(2.46744030034225,-2.36818969290806,1.66533453693773E-16));
#27141=CARTESIAN_POINT('Ctrl Pts',(2.38865944095536,-2.43912928592605,2.1619971139621E-17));
#27142=CARTESIAN_POINT('Ctrl Pts',(2.30658261909198,-2.50634586230322,1.27495535944492E-16));
#27143=CARTESIAN_POINT('Ctrl Pts',(2.22131994895062,-2.56947408053004,1.66533453693773E-16));
#27144=CARTESIAN_POINT('Ctrl Pts',(2.13653932671254,-2.63224539197476,2.05350663525179E-16));
#27145=CARTESIAN_POINT('Ctrl Pts',(2.04860838319626,-2.69097492590926,9.78571983200637E-17));
#27146=CARTESIAN_POINT('Ctrl Pts',(1.95761919937776,-2.74525502143746,5.55111512312578E-17));
#27147=CARTESIAN_POINT('Ctrl Pts',(0.349418900843865,3.91916189049794,24.058));
#27148=CARTESIAN_POINT('Ctrl Pts',(0.983708099956935,3.86349481221817,24.0324107126756));
#27149=CARTESIAN_POINT('Ctrl Pts',(1.60505772607221,3.66267070559658,24.0068214253513));
#27150=CARTESIAN_POINT('Ctrl Pts',(2.13605939111367,3.32170193071062,23.9812321380269));
#27151=CARTESIAN_POINT('Ctrl Pts',(3.23511152224044,2.61597446626503,23.9282681595323));
#27152=CARTESIAN_POINT('Ctrl Pts',(3.94711712557296,1.30987366083964,23.8753041810376));
#27153=CARTESIAN_POINT('Ctrl Pts',(3.94814528315368,0.00380497154103099,
23.822340202543));
#27154=CARTESIAN_POINT('Ctrl Pts',(3.94917344073441,-1.30226371775762,23.7693762240484));
#27155=CARTESIAN_POINT('Ctrl Pts',(3.23922415256329,-2.60830029092949,23.7164122455538));
#27156=CARTESIAN_POINT('Ctrl Pts',(2.14246851744994,-3.3166627231204,23.6634482670591));
#27157=CARTESIAN_POINT('Ctrl Pts',(1.04571288233662,-4.0250251553113,23.6104842885645));
#27158=CARTESIAN_POINT('Ctrl Pts',(-0.437849099718904,-4.13571344652128,
23.5575203100699));
#27159=CARTESIAN_POINT('Ctrl Pts',(-1.62766388484424,-3.59751656345146,
23.5045563315753));
#27160=CARTESIAN_POINT('Ctrl Pts',(-2.81747866996957,-3.05931968038165,
23.4515923530806));
#27161=CARTESIAN_POINT('Ctrl Pts',(-3.71354625816471,-1.87223762303205,
23.398628374586));
#27162=CARTESIAN_POINT('Ctrl Pts',(-3.90551869671661,-0.580571401587583,
23.3456643960914));
#27163=CARTESIAN_POINT('Ctrl Pts',(-3.93389711745665,-0.389630203130338,
23.3378349697575));
#27164=CARTESIAN_POINT('Ctrl Pts',(-3.94688938557907,-0.196403592096446,
23.3300055434235));
#27165=CARTESIAN_POINT('Ctrl Pts',(-3.94525314071248,-0.00295827654940184,
23.3221761170896));
#27166=CARTESIAN_POINT('Origin',(0.,0.,-1.84858989190503));
#27167=CARTESIAN_POINT('',(-1.95761919937781,-2.74525502143742,0.));
#27168=CARTESIAN_POINT('Ctrl Pts',(-1.96186193197216,-2.74910310536277,
-1.68972908581866E-15));
#27169=CARTESIAN_POINT('Ctrl Pts',(-1.11318069597017,-3.34796943221813,
0.0492202025162847));
#27170=CARTESIAN_POINT('Ctrl Pts',(1.27289724729396,-3.73216471134832,0.15142869376082));
#27171=CARTESIAN_POINT('Ctrl Pts',(3.84885445708067,-1.03979978230375,0.306625473733605));
#27172=CARTESIAN_POINT('Ctrl Pts',(2.95737874714596,2.67433718082728,0.465590339918353));
#27173=CARTESIAN_POINT('Ctrl Pts',(-0.647631800440264,3.93376542742361,
0.624555206103101));
#27174=CARTESIAN_POINT('Ctrl Pts',(-3.06550566908991,2.04752208664245,0.752221723431987));
#27175=CARTESIAN_POINT('Ctrl Pts',(-3.36890345256199,0.462673372879177,
0.826899952032626));
#27176=CARTESIAN_POINT('Ctrl Pts',(-3.36692593843476,0.00163208592380858,
0.848589891905015));
#27177=CARTESIAN_POINT('Origin',(0.,0.,0.));
#27178=CARTESIAN_POINT('Ctrl Pts',(-1.47719995289048,3.03093687853778,-0.329233991005386));
#27179=CARTESIAN_POINT('Ctrl Pts',(-2.48630564145415,2.53912496184525,-0.276245702277136));
#27180=CARTESIAN_POINT('Ctrl Pts',(-3.95706612649723,0.476768711041013,
-0.170269124820638));
#27181=CARTESIAN_POINT('Ctrl Pts',(-2.54025446427213,-3.07629710463389,
-0.0113042586358904));
#27182=CARTESIAN_POINT('Ctrl Pts',(1.21035452671364,-3.79753374264191,0.147660607548857));
#27183=CARTESIAN_POINT('Ctrl Pts',(3.84885445708067,-1.03979978230375,0.306625473733605));
#27184=CARTESIAN_POINT('Ctrl Pts',(2.95737874714596,2.67433718082728,0.465590339918353));
#27185=CARTESIAN_POINT('Ctrl Pts',(-0.647631800440264,3.93376542742361,
0.624555206103101));
#27186=CARTESIAN_POINT('Ctrl Pts',(-3.65826453346399,1.58509620284767,0.783520072287847));
#27187=CARTESIAN_POINT('Ctrl Pts',(-3.31298624479799,-2.21807698161905,
0.942484938472596));
#27188=CARTESIAN_POINT('Ctrl Pts',(0.0716483833591926,-3.98622915634864,
1.10144980465734));
#27189=CARTESIAN_POINT('Ctrl Pts',(3.39051798866077,-2.09756782602768,1.26041467084209));
#27190=CARTESIAN_POINT('Ctrl Pts',(3.59899177492058,1.71542482386315,1.41937953702684));
#27191=CARTESIAN_POINT('Ctrl Pts',(0.505790215469384,3.95468340129096,1.57834440321159));
#27192=CARTESIAN_POINT('Ctrl Pts',(-3.05141119286119,2.56598394358578,1.73730926939633));
#27193=CARTESIAN_POINT('Ctrl Pts',(-3.80929264538726,-1.17672126473752,
1.89627413558108));
#27194=CARTESIAN_POINT('Ctrl Pts',(-1.07258002819951,-3.83991470812214,
2.05523900176583));
#27195=CARTESIAN_POINT('Ctrl Pts',(2.6481020123777,-2.98042525524821,2.21420386795058));
#27196=CARTESIAN_POINT('Ctrl Pts',(3.9394520872816,0.613266379946328,2.37316873413532));
#27197=CARTESIAN_POINT('Ctrl Pts',(1.61680281711694,3.64435532093595,2.53213360032008));
#27198=CARTESIAN_POINT('Ctrl Pts',(-2.18907900650795,3.33216312280983,2.69109846650482));
#27199=CARTESIAN_POINT('Ctrl Pts',(-3.98672992391563,-0.0369098299799313,
2.85006333268957));
#27200=CARTESIAN_POINT('Ctrl Pts',(-2.12700963248002,-3.37212213291773,
3.00902819887431));
#27201=CARTESIAN_POINT('Ctrl Pts',(1.68400001564517,-3.61379602896036,3.16799306505907));
#27202=CARTESIAN_POINT('Ctrl Pts',(3.95013122707835,-0.540223147458982,
3.32695793124381));
#27203=CARTESIAN_POINT('Ctrl Pts',(2.59246639543577,3.02894300530038,3.48592279742856));
#27204=CARTESIAN_POINT('Ctrl Pts',(-1.14349143614182,3.81939852540782,3.6448876636133));
#27205=CARTESIAN_POINT('Ctrl Pts',(-3.83042595833975,1.10599038526397,3.80385252979806));
#27206=CARTESIAN_POINT('Ctrl Pts',(-3.00338040757504,-2.62203811565132,
3.9628173959828));
#27207=CARTESIAN_POINT('Ctrl Pts',(0.57892500607099,-3.94464492605495,4.12178226216755));
#27208=CARTESIAN_POINT('Ctrl Pts',(3.63013258458704,-1.64848875417016,4.2807471283523));
#27209=CARTESIAN_POINT('Ctrl Pts',(3.35110647594949,2.15996831943484,4.43971199453705));
#27210=CARTESIAN_POINT('Ctrl Pts',(-0.00217860669321579,3.9869001753454,
4.59867686072179));
#27211=CARTESIAN_POINT('Ctrl Pts',(-3.35346506555395,2.15630466503255,4.75764172690654));
#27212=CARTESIAN_POINT('Ctrl Pts',(-3.6283288127004,-1.65245507692285,4.91660659309129));
#27213=CARTESIAN_POINT('Ctrl Pts',(-0.574613628296617,-3.94527526701846,
5.07557145927603));
#27214=CARTESIAN_POINT('Ctrl Pts',(3.0062441927532,-2.61875420913902,5.2345363254608));
#27215=CARTESIAN_POINT('Ctrl Pts',(3.8292149534867,1.11017592945447,5.39350119164552));
#27216=CARTESIAN_POINT('Ctrl Pts',(1.13931660104628,3.82064594498541,5.55246605783029));
#27217=CARTESIAN_POINT('Ctrl Pts',(-2.59577512563926,3.02610793784054,5.71143092401502));
#27218=CARTESIAN_POINT('Ctrl Pts',(-3.94953846664522,-0.544539856061292,
5.87039579019978));
#27219=CARTESIAN_POINT('Ctrl Pts',(-1.68004955900417,-3.61563427819245,
6.02936065638453));
#27220=CARTESIAN_POINT('Ctrl Pts',(2.13069369871068,-3.3697955600636,6.18832552256926));
#27221=CARTESIAN_POINT('Ctrl Pts',(3.98676787287831,-0.032552759256669,
6.34729038875402));
#27222=CARTESIAN_POINT('Ctrl Pts',(2.18543605335013,3.3345534950076,6.50625525493876));
#27223=CARTESIAN_POINT('Ctrl Pts',(-1.62078473268592,3.64258625218979,6.66522012112352));
#27224=CARTESIAN_POINT('Ctrl Pts',(-3.94011990490355,0.608960498992104,
6.82418498730826));
#27225=CARTESIAN_POINT('Ctrl Pts',(-2.64484328742837,-2.98331723745481,
6.98314985349301));
#27226=CARTESIAN_POINT('Ctrl Pts',(1.07677617223565,-3.83874078693202,7.14211471967776));
#27227=CARTESIAN_POINT('Ctrl Pts',(3.81057598656871,-1.17255635469506,7.3010795858625));
#27228=CARTESIAN_POINT('Ctrl Pts',(3.04860581952888,2.56931514444696,7.46004445204726));
#27229=CARTESIAN_POINT('Ctrl Pts',(-0.510113381387115,3.95413228059959,
7.619009318232));
#27230=CARTESIAN_POINT('Ctrl Pts',(-3.60086158473341,1.71148286638841,7.77797418441675));
#27231=CARTESIAN_POINT('Ctrl Pts',(-3.38822891354565,-2.10125738160825,
7.93693905060149));
#27232=CARTESIAN_POINT('Ctrl Pts',(-0.0672816548149041,-3.98633301836102,
8.09590391678625));
#27233=CARTESIAN_POINT('Ctrl Pts',(3.31538886833258,-2.21440159096907,8.25486878297098));
#27234=CARTESIAN_POINT('Ctrl Pts',(3.65656725922866,1.58899138861319,8.41383364915575));
#27235=CARTESIAN_POINT('Ctrl Pts',(0.643261156248369,3.93466553079316,8.57279851534047));
#27236=CARTESIAN_POINT('Ctrl Pts',(-2.96016388101437,2.67073165104392,8.73176338152524));
#27237=CARTESIAN_POINT('Ctrl Pts',(-3.84797530194499,-1.04329469948394,
8.89072824770997));
#27238=CARTESIAN_POINT('Ctrl Pts',(-1.20570712414377,-3.80021684712055,
9.04969311389473));
#27239=CARTESIAN_POINT('Ctrl Pts',(2.54266018034211,-3.07087234538534,9.20865798007948));
#27240=CARTESIAN_POINT('Ctrl Pts',(3.95842601916979,0.47564819468749,9.36762284626423));
#27241=CARTESIAN_POINT('Ctrl Pts',(1.74278629094578,3.58581562527152,9.52658771244896));
#27242=CARTESIAN_POINT('Ctrl Pts',(-2.07166160205713,3.40640513751843,9.68555257863373));
#27243=CARTESIAN_POINT('Ctrl Pts',(-3.98559564477585,0.102005444431573,
9.84451744481845));
#27244=CARTESIAN_POINT('Ctrl Pts',(-2.24319907973156,-3.29597263991092,
10.0034823110032));
#27245=CARTESIAN_POINT('Ctrl Pts',(1.55707745747673,-3.67027077281332,10.1624471771879));
#27246=CARTESIAN_POINT('Ctrl Pts',(3.928912558612,-0.677512997019795,10.3214120433727));
#27247=CARTESIAN_POINT('Ctrl Pts',(2.69641733534343,2.93678588051791,10.4803769095574));
#27248=CARTESIAN_POINT('Ctrl Pts',(-1.00973405207762,3.8569177977272,10.6393417757422));
#27249=CARTESIAN_POINT('Ctrl Pts',(-3.7895693127859,1.2387663936115,10.7983066419269));
#27250=CARTESIAN_POINT('Ctrl Pts',(-3.0929058256244,-2.51581225614482,10.9572715081117));
#27251=CARTESIAN_POINT('Ctrl Pts',(0.441146911493231,-3.96241935650807,
11.1162363742964));
#27252=CARTESIAN_POINT('Ctrl Pts',(3.57049754163045,-1.77395745708877,11.2752012404812));
#27253=CARTESIAN_POINT('Ctrl Pts',(3.42432285260543,2.04190860605321,11.4341661066659));
#27254=CARTESIAN_POINT('Ctrl Pts',(0.136721492950909,3.98455580808139,11.5931309728507));
#27255=CARTESIAN_POINT('Ctrl Pts',(-3.27630628322196,2.27182633422323,11.7520958390354));
#27256=CARTESIAN_POINT('Ctrl Pts',(-3.683695752997,-1.52504536119478,11.9110607052202));
#27257=CARTESIAN_POINT('Ctrl Pts',(-0.711713421966334,-3.92286142494773,
12.0700255714049));
#27258=CARTESIAN_POINT('Ctrl Pts',(2.91318501009988,-2.72189839106446,12.2289904375897));
#27259=CARTESIAN_POINT('Ctrl Pts',(3.86556759564105,0.976096776902648,12.3879553037744));
#27260=CARTESIAN_POINT('Ctrl Pts',(1.27173165426137,3.77863419159615,12.5469201699592));
#27261=CARTESIAN_POINT('Ctrl Pts',(-2.48877340931887,3.11470458814592,12.7058850361439));
#27262=CARTESIAN_POINT('Ctrl Pts',(-3.96611198956382,-0.406612150074322,
12.8648499023287));
#27263=CARTESIAN_POINT('Ctrl Pts',(-1.80499399926681,-3.5549084962852,13.0238147685134));
#27264=CARTESIAN_POINT('Ctrl Pts',(2.01200065152342,-3.44198069904803,13.1827796346982));
#27265=CARTESIAN_POINT('Ctrl Pts',(3.98321358718988,-0.171427165804589,
13.3417445008829));
#27266=CARTESIAN_POINT('Ctrl Pts',(2.30028118194861,3.25639129072706,13.5007093670677));
#27267=CARTESIAN_POINT('Ctrl Pts',(-1.49289753065309,3.69684118097057,13.6596742332524));
#27268=CARTESIAN_POINT('Ctrl Pts',(-3.91651258901516,0.74585983564986,13.8186390994372));
#27269=CARTESIAN_POINT('Ctrl Pts',(-2.74717288447362,-2.88936306080816,
13.9776039656219));
#27270=CARTESIAN_POINT('Ctrl Pts',(0.942385426660244,-3.87392403926152,
14.1365688318067));
#27271=CARTESIAN_POINT('Ctrl Pts',(3.76741231340739,-1.30460040439068,14.2955336979914));
#27272=CARTESIAN_POINT('Ctrl Pts',(3.1362669786623,2.46154569181692,14.4544985641762));
#27273=CARTESIAN_POINT('Ctrl Pts',(-0.372046531241306,3.96950363810656,
14.6134634303609));
#27274=CARTESIAN_POINT('Ctrl Pts',(-3.53904967227374,1.83589356214594,14.7724282965457));
#27275=CARTESIAN_POINT('Ctrl Pts',(-3.45937733680892,-1.98194000815431,
14.9313931627304));
#27276=CARTESIAN_POINT('Ctrl Pts',(-0.206119829211681,-3.98156908396121,
15.0903580289152));
#27277=CARTESIAN_POINT('Ctrl Pts',(3.23622917375625,-2.32856146349605,15.2493228950999));
#27278=CARTESIAN_POINT('Ctrl Pts',(3.70970605913983,1.46063640552025,15.4082877612846));
#27279=CARTESIAN_POINT('Ctrl Pts',(0.779949646731194,3.90986653262151,15.5672526274694));
#27280=CARTESIAN_POINT('Ctrl Pts',(-2.86532184046814,2.77223889751338,15.7262174936541));
#27281=CARTESIAN_POINT('Ctrl Pts',(-3.88198649442593,-0.908602559673156,
15.8851823598389));
#27282=CARTESIAN_POINT('Ctrl Pts',(-1.33737014962086,-3.75590452983738,
16.0441472260236));
#27283=CARTESIAN_POINT('Ctrl Pts',(2.43413116992486,-3.15759136082396,16.2031120922084));
#27284=CARTESIAN_POINT('Ctrl Pts',(3.97259404474729,0.337452678146523,16.3620769583931));
#27285=CARTESIAN_POINT('Ctrl Pts',(1.86665380078734,3.52292227310739,16.5210418245779));
#27286=CARTESIAN_POINT('Ctrl Pts',(-1.95172895721992,3.47651144567355,16.6800066907626));
#27287=CARTESIAN_POINT('Ctrl Pts',(-3.97962242319515,0.240796850378547,
16.8389715569474));
#27288=CARTESIAN_POINT('Ctrl Pts',(-2.35666503270154,-3.21582146239366,
16.9979364231321));
#27289=CARTESIAN_POINT('Ctrl Pts',(1.42826443406275,-3.7222894112013,17.1569012893169));
#27290=CARTESIAN_POINT('Ctrl Pts',(3.90292376012977,-0.813980268166524,
17.3158661555016));
#27291=CARTESIAN_POINT('Ctrl Pts',(2.79709452794753,2.84106317354542,17.4748310216864));
#27292=CARTESIAN_POINT('Ctrl Pts',(-0.87475073969136,3.88975434928213,17.6337958878711));
#27293=CARTESIAN_POINT('Ctrl Pts',(-3.74411171420101,1.37003840308681,17.7927607540559));
#27294=CARTESIAN_POINT('Ctrl Pts',(-3.1786761163436,-2.40653192410502,17.9517256202406));
#27295=CARTESIAN_POINT('Ctrl Pts',(0.302833216085013,-3.97538297495793,
18.1106904864254));
#27296=CARTESIAN_POINT('Ctrl Pts',(3.5065275226793,-1.89727238082542,18.2696553526101));
#27297=CARTESIAN_POINT('Ctrl Pts',(3.49338172535042,1.92136979140851,18.4286202187948));
#27298=CARTESIAN_POINT('Ctrl Pts',(0.275455597698851,3.97737375262188,18.5875850849796));
#27299=CARTESIAN_POINT('Ctrl Pts',(-3.19516970536172,2.38458975681184,18.7465499511644));
#27300=CARTESIAN_POINT('Ctrl Pts',(-3.73459028221552,-1.3957840729596,18.9055148173491));
#27301=CARTESIAN_POINT('Ctrl Pts',(-0.847949117405149,-3.89568479841959,
19.0644796835338));
#27302=CARTESIAN_POINT('Ctrl Pts',(2.81658890100978,-2.82173788950715,19.2234445497186));
#27303=CARTESIAN_POINT('Ctrl Pts',(3.89722701433046,0.840832535700663,19.3824094159033));
#27304=CARTESIAN_POINT('Ctrl Pts',(1.40260268563389,3.73203476143841,19.5413742820881));
#27305=CARTESIAN_POINT('Ctrl Pts',(-2.3787500488546,3.19951964512964,19.7003391482728));
#27306=CARTESIAN_POINT('Ctrl Pts',(-3.97787021705804,-0.268190772315832,
19.8593040144576));
#27307=CARTESIAN_POINT('Ctrl Pts',(-1.92774697870435,-3.4898666651324,20.0182688806423));
#27308=CARTESIAN_POINT('Ctrl Pts',(1.89086481476229,-3.50998689564495,20.1772337468271));
#27309=CARTESIAN_POINT('Ctrl Pts',(3.97482324267393,-0.310093440809367,
20.3361986130118));
#27310=CARTESIAN_POINT('Ctrl Pts',(2.41233351706024,3.17427546962878,20.4951634791965));
#27311=CARTESIAN_POINT('Ctrl Pts',(-1.36319778790607,3.74660773920425,20.6541283453813));
#27312=CARTESIAN_POINT('Ctrl Pts',(-3.88815019533756,0.881853615583829,
20.813093211566));
#27313=CARTESIAN_POINT('Ctrl Pts',(-2.84616711491744,-2.79190087828212,
20.9720580777508));
#27314=CARTESIAN_POINT('Ctrl Pts',(0.806850527235046,-3.9044039261228,21.1310229439355));
#27315=CARTESIAN_POINT('Ctrl Pts',(3.71967457752779,-1.43506051902692,21.2899878101203));
#27316=CARTESIAN_POINT('Ctrl Pts',(3.22012038549849,2.35078763921597,21.448952676305));
#27317=CARTESIAN_POINT('Ctrl Pts',(-0.233528014234224,3.98005560769136,
21.6079175424898));
#27318=CARTESIAN_POINT('Ctrl Pts',(-3.47294089147738,1.95807523322667,21.7668824086745));
#27319=CARTESIAN_POINT('Ctrl Pts',(-3.52632583653101,-1.86021624962628,
21.9258472748593));
#27320=CARTESIAN_POINT('Ctrl Pts',(-0.344707483447601,-3.97197126386073,
22.0848121410441));
#27321=CARTESIAN_POINT('Ctrl Pts',(3.15313982968432,-2.43989387002868,22.2437770072288));
#27322=CARTESIAN_POINT('Ctrl Pts',(3.75834184644668,1.33050740634341,22.4027418734136));
#27323=CARTESIAN_POINT('Ctrl Pts',(0.915689325102905,3.88032175554439,22.5617067395983));
#27324=CARTESIAN_POINT('Ctrl Pts',(-2.76699741760937,2.87037799557025,22.720671605783));
#27325=CARTESIAN_POINT('Ctrl Pts',(-3.91129134187434,-0.7728027958352,22.8796364719677));
#27326=CARTESIAN_POINT('Ctrl Pts',(-1.46739644894177,-3.70704069007233,
23.0386013381526));
#27327=CARTESIAN_POINT('Ctrl Pts',(2.32262200499063,-3.24046036848089,23.1975662043372));
#27328=CARTESIAN_POINT('Ctrl Pts',(3.98198637087808,0.198816238648098,23.3565310705221));
#27329=CARTESIAN_POINT('Ctrl Pts',(1.98816433058814,3.45581133218519,23.5154959367067));
#27330=CARTESIAN_POINT('Ctrl Pts',(-1.82925354411967,3.5422830008711,23.6744608028915));
#27331=CARTESIAN_POINT('Ctrl Pts',(-3.96914826399699,0.379513463839679,
23.8334256690762));
#27332=CARTESIAN_POINT('Ctrl Pts',(-2.46663759784563,-3.13218185614485,
23.992390535261));
#27333=CARTESIAN_POINT('Ctrl Pts',(1.29650641132588,-3.76899081084458,24.1513554014457));
#27334=CARTESIAN_POINT('Ctrl Pts',(3.87454091099827,-0.951014904317504,
24.3103202676305));
#27335=CARTESIAN_POINT('Ctrl Pts',(2.88961752940844,2.74513957150359,24.4692851338152));
#27336=CARTESIAN_POINT('Ctrl Pts',(0.478408881098333,3.52136284087264,24.5752617112718));
#27337=CARTESIAN_POINT('Ctrl Pts',(-0.624728334461281,3.3133687646595,24.62825));
#27338=CARTESIAN_POINT('Ctrl Pts',(-1.56047750639987,3.20180677844002,-0.219489327336924));
#27339=CARTESIAN_POINT('Ctrl Pts',(-2.62647180561611,2.68226882971724,-0.166501038608675));
#27340=CARTESIAN_POINT('Ctrl Pts',(-4.1801468173981,0.503646678216414,-0.0605244611521764));
#27341=CARTESIAN_POINT('Ctrl Pts',(-2.683462008154,-3.24972419975438,0.0984404050325707));
#27342=CARTESIAN_POINT('Ctrl Pts',(1.27858859595154,-4.01162075153852,0.257405271217319));
#27343=CARTESIAN_POINT('Ctrl Pts',(4.06583468536472,-1.09841878093043,0.416370137402066));
#27344=CARTESIAN_POINT('Ctrl Pts',(3.12410178716573,2.82510367472183,0.575335003586814));
#27345=CARTESIAN_POINT('Ctrl Pts',(-0.684142221260432,4.15553253500754,
0.734299869771561));
#27346=CARTESIAN_POINT('Ctrl Pts',(-3.86450020240029,1.67445643711512,0.89326473595631));
#27347=CARTESIAN_POINT('Ctrl Pts',(-3.49975675527435,-2.3431216813317,1.05222960214106));
#27348=CARTESIAN_POINT('Ctrl Pts',(0.0756875806712427,-4.21095392107594,
1.2111944683258));
#27349=CARTESIAN_POINT('Ctrl Pts',(3.58165937251524,-2.21581878895911,1.37015933451055));
#27350=CARTESIAN_POINT('Ctrl Pts',(3.80188592579657,1.81213236997502,1.5291242006953));
#27351=CARTESIAN_POINT('Ctrl Pts',(0.534304277936582,4.17762976540319,1.68808906688005));
#27352=CARTESIAN_POINT('Ctrl Pts',(-3.22343533786296,2.71064199393843,1.8470539330648));
#27353=CARTESIAN_POINT('Ctrl Pts',(-4.02404256565933,-1.24305924958384,
2.00601879924955));
#27354=CARTESIAN_POINT('Ctrl Pts',(-1.1330470222017,-4.05639095560061,2.16498366543429));
#27355=CARTESIAN_POINT('Ctrl Pts',(2.79738949143739,-3.14844754849901,2.32394853161904));
#27356=CARTESIAN_POINT('Ctrl Pts',(4.1615397818786,0.647839440737169,2.48291339780379));
#27357=CARTESIAN_POINT('Ctrl Pts',(1.70795052048174,3.84980685419155,2.64187826398853));
#27358=CARTESIAN_POINT('Ctrl Pts',(-2.31248893740054,3.52001473505691,2.80084313017328));
#27359=CARTESIAN_POINT('Ctrl Pts',(-4.21148291955221,-0.0389906317936465,
2.95980799635803));
#27360=CARTESIAN_POINT('Ctrl Pts',(-2.2469203853454,-3.56222644534663,3.11877286254278));
#27361=CARTESIAN_POINT('Ctrl Pts',(1.77893597955331,-3.81752477372836,3.27773772872752));
#27362=CARTESIAN_POINT('Ctrl Pts',(4.17282096111768,-0.570678375934639,
3.43670259491227));
#27363=CARTESIAN_POINT('Ctrl Pts',(2.73861740129298,3.19970050005065,3.59566746109702));
#27364=CARTESIAN_POINT('Ctrl Pts',(-1.20795608026431,4.03471816744471,3.75463232728177));
#27365=CARTESIAN_POINT('Ctrl Pts',(-4.04636727494025,1.16834089733205,3.91359719346651));
#27366=CARTESIAN_POINT('Ctrl Pts',(-3.17269680384994,-2.76985623536663,
4.07256205965127));
#27367=CARTESIAN_POINT('Ctrl Pts',(0.611562062467236,-4.1670253683656,4.23152692583601));
#27368=CARTESIAN_POINT('Ctrl Pts',(3.83478230717035,-1.74142276094858,4.39049179202076));
#27369=CARTESIAN_POINT('Ctrl Pts',(3.5400260249384,2.28173712733952,4.54945665820551));
#27370=CARTESIAN_POINT('Ctrl Pts',(-0.00230142624457838,4.21166276895315,
4.70842152439025));
#27371=CARTESIAN_POINT('Ctrl Pts',(-3.54251758068034,2.27786693341294,4.867386390575));
#27372=CARTESIAN_POINT('Ctrl Pts',(-3.83287684714762,-1.74561268623704,
5.02635125675975));
#27373=CARTESIAN_POINT('Ctrl Pts',(-0.607007629585367,-4.16769124497425,
5.18531612294449));
#27374=CARTESIAN_POINT('Ctrl Pts',(3.17572203570494,-2.76638719772175,5.34428098912925));
#27375=CARTESIAN_POINT('Ctrl Pts',(4.04508799935564,1.17276240272716,5.50324585531399));
#27376=CARTESIAN_POINT('Ctrl Pts',(1.20354588769234,4.03603591064399,5.66221072149874));
#27377=CARTESIAN_POINT('Ctrl Pts',(-2.74211266207147,3.19670560488322,5.82117558768349));
#27378=CARTESIAN_POINT('Ctrl Pts',(-4.17219478365215,-0.575238440171331,
5.98014045386823));
#27379=CARTESIAN_POINT('Ctrl Pts',(-1.77476281483295,-3.81946665476637,
6.13910532005299));
#27380=CARTESIAN_POINT('Ctrl Pts',(2.2508121418228,-3.55976871130813,6.29807018623772));
#27381=CARTESIAN_POINT('Ctrl Pts',(4.21152300789809,-0.0343879300103317,
6.45703505242249));
#27382=CARTESIAN_POINT('Ctrl Pts',(2.30864061175677,3.52253986514459,6.61599991860723));
#27383=CARTESIAN_POINT('Ctrl Pts',(-1.71215691763581,3.84793805370841,6.77496478479197));
#27384=CARTESIAN_POINT('Ctrl Pts',(-4.16224524790261,0.643290814560192,
6.93392965097673));
#27385=CARTESIAN_POINT('Ctrl Pts',(-2.79394705497301,-3.1515025669977,7.09289451716147));
#27386=CARTESIAN_POINT('Ctrl Pts',(1.13747972501166,-4.05515085428062,7.25185938334622));
#27387=CARTESIAN_POINT('Ctrl Pts',(4.02539825555276,-1.23865954159255,7.41082424953096));
#27388=CARTESIAN_POINT('Ctrl Pts',(3.22047181083767,2.71416099216412,7.56978911571571));
#27389=CARTESIAN_POINT('Ctrl Pts',(-0.538871163521626,4.1770475751313,7.72875398190046));
#27390=CARTESIAN_POINT('Ctrl Pts',(-3.80386114665173,1.80796818356375,7.8877188480852));
#27391=CARTESIAN_POINT('Ctrl Pts',(-3.57924125016108,-2.21971634425003,
8.04668371426996));
#27392=CARTESIAN_POINT('Ctrl Pts',(-0.0710746766045851,-4.21106363833782,
8.2056485804547));
#27393=CARTESIAN_POINT('Ctrl Pts',(3.50229482737133,-2.33923908952323,8.36461344663945));
#27394=CARTESIAN_POINT('Ctrl Pts',(3.86270724386325,1.6785712150492,8.5235783128242));
#27395=CARTESIAN_POINT('Ctrl Pts',(0.679525180800456,4.15648338195204,8.68254317900894));
#27396=CARTESIAN_POINT('Ctrl Pts',(-3.12704393372178,2.82129488220555,8.8415080451937));
#27397=CARTESIAN_POINT('Ctrl Pts',(-4.06490596761654,-1.10211072502764,
9.00047291137844));
#27398=CARTESIAN_POINT('Ctrl Pts',(-1.27367919478393,-4.0144551167699,9.15943777756319));
#27399=CARTESIAN_POINT('Ctrl Pts',(2.68600334712891,-3.24399361821161,9.31840264374794));
#27400=CARTESIAN_POINT('Ctrl Pts',(4.18158337439399,0.502462992445402,9.47736750993269));
#27401=CARTESIAN_POINT('Ctrl Pts',(1.84103634728762,3.7879669670882,9.63633237611743));
#27402=CARTESIAN_POINT('Ctrl Pts',(-2.18845209448917,3.59844216375801,9.79529724230219));
#27403=CARTESIAN_POINT('Ctrl Pts',(-4.21028469511404,0.107756029408409,
9.95426210848692));
#27404=CARTESIAN_POINT('Ctrl Pts',(-2.36966004463275,-3.48178400373378,
10.1132269746717));
#27405=CARTESIAN_POINT('Ctrl Pts',(1.64485812726998,-3.87718329679412,10.2721918408564));
#27406=CARTESIAN_POINT('Ctrl Pts',(4.15040608438235,-0.71570797851312,10.4311567070412));
#27407=CARTESIAN_POINT('Ctrl Pts',(2.84842860401989,3.1023479920194,10.5901215732259));
#27408=CARTESIAN_POINT('Ctrl Pts',(-1.06665808689608,4.07435259905726,10.7490864394107));
#27409=CARTESIAN_POINT('Ctrl Pts',(-4.00320732475952,1.30860218965774,10.9080513055954));
#27410=CARTESIAN_POINT('Ctrl Pts',(-3.26726924195739,-2.657641863823,11.0670161717801));
#27411=CARTESIAN_POINT('Ctrl Pts',(0.466016689924724,-4.18580183722271,
11.2259810379649));
#27412=CARTESIAN_POINT('Ctrl Pts',(3.77178532227006,-1.87396479649261,11.3849459041496));
#27413=CARTESIAN_POINT('Ctrl Pts',(3.61736999495961,2.15702176515476,11.5439107703344));
#27414=CARTESIAN_POINT('Ctrl Pts',(0.144429204708414,4.20918623734002,11.7028756365191));
#27415=CARTESIAN_POINT('Ctrl Pts',(-3.4610089507791,2.39990116846763,11.8618405027039));
#27416=CARTESIAN_POINT('Ctrl Pts',(-3.89136511392694,-1.61102021275272,
12.0208053688886));
#27417=CARTESIAN_POINT('Ctrl Pts',(-0.751836461819641,-4.14401381639395,
12.1797702350734));
#27418=CARTESIAN_POINT('Ctrl Pts',(3.07741661604235,-2.87534616126336,12.3387351012581));
#27419=CARTESIAN_POINT('Ctrl Pts',(4.08349003170681,1.03112450108435,12.4976999674429));
#27420=CARTESIAN_POINT('Ctrl Pts',(1.34342587594075,3.99165573310602,12.6566648336276));
#27421=CARTESIAN_POINT('Ctrl Pts',(-2.62907869457274,3.29029691570976,12.8156296998124));
#27422=CARTESIAN_POINT('Ctrl Pts',(-4.18970264348228,-0.429535021835278,
12.9745945659971));
#27423=CARTESIAN_POINT('Ctrl Pts',(-1.90675103226963,-3.75531744020717,
13.1335594321819));
#27424=CARTESIAN_POINT('Ctrl Pts',(2.12542774146498,-3.63602330735055,13.2925242983666));
#27425=CARTESIAN_POINT('Ctrl Pts',(4.2077683483767,-0.181091419411761,13.4514891645514));
#27426=CARTESIAN_POINT('Ctrl Pts',(2.42996016605737,3.43997124510655,13.6104540307361));
#27427=CARTESIAN_POINT('Ctrl Pts',(-1.577060039425,3.90525161901692,13.7694188969209));
#27428=CARTESIAN_POINT('Ctrl Pts',(-4.13730706309004,0.787907888963343,
13.9283837631056));
#27429=CARTESIAN_POINT('Ctrl Pts',(-2.90204551118784,-3.05225169780932,
14.0873486292903));
#27430=CARTESIAN_POINT('Ctrl Pts',(0.995512664202879,-4.09231757213405,
14.2463134954751));
#27431=CARTESIAN_POINT('Ctrl Pts',(3.97980121844884,-1.37814761089607,14.4052783616599));
#27432=CARTESIAN_POINT('Ctrl Pts',(3.3130748919202,2.60031600701019,14.5642432278446));
#27433=CARTESIAN_POINT('Ctrl Pts',(-0.393020756736522,4.19328549714417,
14.7232080940294));
#27434=CARTESIAN_POINT('Ctrl Pts',(-3.73856457063159,1.9393925665021,14.8821729602141));
#27435=CARTESIAN_POINT('Ctrl Pts',(-3.65440068534852,-2.09367242106057,
15.0411378263989));
#27436=CARTESIAN_POINT('Ctrl Pts',(-0.217739891257386,-4.20603113582635,
15.2001026925836));
#27437=CARTESIAN_POINT('Ctrl Pts',(3.41867248324782,-2.45983475625287,15.3590675587684));
#27438=CARTESIAN_POINT('Ctrl Pts',(3.91884175823025,1.5429801844924,15.5180324249531));
#27439=CARTESIAN_POINT('Ctrl Pts',(0.823919522517587,4.13028633343982,15.6769972911379));
#27440=CARTESIAN_POINT('Ctrl Pts',(-3.02685514706235,2.92852462760477,15.8359621573226));
#27441=CARTESIAN_POINT('Ctrl Pts',(-4.10083455042517,-0.95982527880059,
15.9949270235073));
#27442=CARTESIAN_POINT('Ctrl Pts',(-1.41276475952385,-3.96764468041594,
16.1538918896921));
#27443=CARTESIAN_POINT('Ctrl Pts',(2.57135598390867,-3.3356014419895,16.3128567558768));
#27444=CARTESIAN_POINT('Ctrl Pts',(4.196550126309,0.356476665661734,16.4718216220616));
#27445=CARTESIAN_POINT('Ctrl Pts',(1.97188692205462,3.72152798490289,16.6307864882463));
#27446=CARTESIAN_POINT('Ctrl Pts',(-2.06175821382304,3.67250073431153,16.7897513544311));
#27447=CARTESIAN_POINT('Ctrl Pts',(-4.20397473152436,0.254371839027192,
16.9487162206158));
#27448=CARTESIAN_POINT('Ctrl Pts',(-2.48952267189958,-3.39711428154593,
17.1076810868006));
#27449=CARTESIAN_POINT('Ctrl Pts',(1.50878323424311,-3.93213450022406,17.2666459529853));
#27450=CARTESIAN_POINT('Ctrl Pts',(4.1229521602399,-0.859868629593263,17.4256108191701));
#27451=CARTESIAN_POINT('Ctrl Pts',(2.95478150103885,3.00122889112179,17.5845756853548));
#27452=CARTESIAN_POINT('Ctrl Pts',(-0.924065053159552,4.10904032023471,
17.7435405515396));
#27453=CARTESIAN_POINT('Ctrl Pts',(-3.95518704155557,1.44727469476127,17.9025054177243));
#27454=CARTESIAN_POINT('Ctrl Pts',(-3.35787485639895,-2.54220082301716,
18.0614702839091));
#27455=CARTESIAN_POINT('Ctrl Pts',(0.319905521907667,-4.1994962832271,18.2204351500938));
#27456=CARTESIAN_POINT('Ctrl Pts',(3.70420897591159,-2.00423163296111,18.3794000162786));
#27457=CARTESIAN_POINT('Ctrl Pts',(3.69032208064376,2.02968754169158,18.5383648824633));
#27458=CARTESIAN_POINT('Ctrl Pts',(0.290984482757316,4.20159929152924,18.6973297486481));
#27459=CARTESIAN_POINT('Ctrl Pts',(-3.37529827603299,2.51902166000967,18.8562946148328));
#27460=CARTESIAN_POINT('Ctrl Pts',(-3.94512883622391,-1.47447178385209,
19.0152594810176));
#27461=CARTESIAN_POINT('Ctrl Pts',(-0.895752482047657,-4.11530510007291,
19.1742243472023));
#27462=CARTESIAN_POINT('Ctrl Pts',(2.9753748747426,-2.98081413888224,19.333189213387));
#27463=CARTESIAN_POINT('Ctrl Pts',(4.1169342588298,0.888234701092859,19.4921540795718));
#27464=CARTESIAN_POINT('Ctrl Pts',(1.48167479769069,3.94242924726034,19.6511189457566));
#27465=CARTESIAN_POINT('Ctrl Pts',(-2.5128527369107,3.37989344485135,19.8100838119413));
#27466=CARTESIAN_POINT('Ctrl Pts',(-4.20212374428449,-0.283310100845846,
19.9690486781261));
#27467=CARTESIAN_POINT('Ctrl Pts',(-2.03642424467465,-3.68660885793949,
20.1280135443108));
#27468=CARTESIAN_POINT('Ctrl Pts',(1.9974628385994,-3.70786337197934,20.2869784104955));
#27469=CARTESIAN_POINT('Ctrl Pts',(4.1989049958817,-0.327575043797077,20.4459432766802));
#27470=CARTESIAN_POINT('Ctrl Pts',(2.54832948237039,3.35322612201562,20.6049081428651));
#27471=CARTESIAN_POINT('Ctrl Pts',(-1.44004843801888,3.95782378065465,20.7638730090497));
#27472=CARTESIAN_POINT('Ctrl Pts',(-4.10734573167046,0.931568355633416,
20.9228378752345));
#27473=CARTESIAN_POINT('Ctrl Pts',(-3.00662056859199,-2.94929505794555,
21.0818027414192));
#27474=CARTESIAN_POINT('Ctrl Pts',(0.852336947556435,-4.12451577099776,
21.240767607604));
#27475=CARTESIAN_POINT('Ctrl Pts',(3.92937225458326,-1.51596245036574,21.3997324737888));
#27476=CARTESIAN_POINT('Ctrl Pts',(3.4016555576228,2.48331393874026,21.5586973399735));
#27477=CARTESIAN_POINT('Ctrl Pts',(-0.246693220246651,4.20443233691565,
21.7176622061583));
#27478=CARTESIAN_POINT('Ctrl Pts',(-3.66872888914082,2.0684622628846,21.876627072343));
#27479=CARTESIAN_POINT('Ctrl Pts',(-3.72512342515035,-1.96508645217684,
22.0355919385278));
#27480=CARTESIAN_POINT('Ctrl Pts',(-0.364140462606384,-4.19589223597873,
22.1945568047125));
#27481=CARTESIAN_POINT('Ctrl Pts',(3.33089895455792,-2.57744355781532,22.3535216708973));
#27482=CARTESIAN_POINT('Ctrl Pts',(3.97021940141924,1.4055151272072,22.512486537082));
#27483=CARTESIAN_POINT('Ctrl Pts',(0.967311562579962,4.09907596143147,22.6714514032667));
#27484=CARTESIAN_POINT('Ctrl Pts',(-2.92298765783001,3.03219634429854,22.8304162694515));
#27485=CARTESIAN_POINT('Ctrl Pts',(-4.13179146670604,-0.816369765937287,
22.9893811356362));
#27486=CARTESIAN_POINT('Ctrl Pts',(-1.5501213272205,-3.91602612824874,23.148346001821));
#27487=CARTESIAN_POINT('Ctrl Pts',(2.45356045914115,-3.42314221273843,23.3073108680058));
#27488=CARTESIAN_POINT('Ctrl Pts',(4.20647194740789,0.210024558767638,23.4662757341905));
#27489=CARTESIAN_POINT('Ctrl Pts',(2.10024764138301,3.65063364623366,23.6252406003752));
#27490=CARTESIAN_POINT('Ctrl Pts',(-1.93237821563391,3.74198017901762,23.78420546656));
#27491=CARTESIAN_POINT('Ctrl Pts',(-4.19291008872147,0.400908639713182,
23.9431703327447));
#27492=CARTESIAN_POINT('Ctrl Pts',(-2.60569497064129,-3.30875946949763,
24.1021351989295));
#27493=CARTESIAN_POINT('Ctrl Pts',(1.36959731674678,-3.98146870411307,24.2611000651142));
#27494=CARTESIAN_POINT('Ctrl Pts',(4.09296922018457,-1.00462863103577,24.420064931299));
#27495=CARTESIAN_POINT('Ctrl Pts',(3.05252051214689,2.89989756964007,24.5790297974837));
#27496=CARTESIAN_POINT('Ctrl Pts',(0.505379313311694,3.71988063924714,24.6850063749402));
#27497=CARTESIAN_POINT('Ctrl Pts',(-0.659947566089433,3.50016083979823,
24.7379946636685));
#27498=CARTESIAN_POINT('Ctrl Pts',(-1.64375505990927,3.37267667834226,-0.109744663668463));
#27499=CARTESIAN_POINT('Ctrl Pts',(-2.76663796977808,2.82541269758923,-0.0567563749402136));
#27500=CARTESIAN_POINT('Ctrl Pts',(-4.40322750829897,0.530524645391819,
0.0492202025162849));
#27501=CARTESIAN_POINT('Ctrl Pts',(-2.82666955203587,-3.42315129487488,
0.208185068701033));
#27502=CARTESIAN_POINT('Ctrl Pts',(1.34682266518943,-4.22570776043514,0.36714993488578));
#27503=CARTESIAN_POINT('Ctrl Pts',(4.28281491364878,-1.15703777955712,0.526114801070528));
#27504=CARTESIAN_POINT('Ctrl Pts',(3.29082482718549,2.97587016861638,0.685079667255276));
#27505=CARTESIAN_POINT('Ctrl Pts',(-0.720652642080601,4.37729964259146,
0.844044533440024));
#27506=CARTESIAN_POINT('Ctrl Pts',(-4.07073587133658,1.76381667138256,1.00300939962477));
#27507=CARTESIAN_POINT('Ctrl Pts',(-3.68652726575071,-2.46816638104435,
1.16197426580952));
#27508=CARTESIAN_POINT('Ctrl Pts',(0.0797267779832985,-4.43567868580324,
1.32093913199426));
#27509=CARTESIAN_POINT('Ctrl Pts',(3.7728007563697,-2.33406975189055,1.47990399817901));
#27510=CARTESIAN_POINT('Ctrl Pts',(4.00478007667258,1.90883991608689,1.63886886436376));
#27511=CARTESIAN_POINT('Ctrl Pts',(0.562818340403771,4.40057612951542,1.79783373054851));
#27512=CARTESIAN_POINT('Ctrl Pts',(-3.39545948286473,2.85530004429109,1.95679859673326));
#27513=CARTESIAN_POINT('Ctrl Pts',(-4.23879248593139,-1.30939723443016,
2.11576346291801));
#27514=CARTESIAN_POINT('Ctrl Pts',(-1.19351401620389,-4.27286720307909,
2.27472832910275));
#27515=CARTESIAN_POINT('Ctrl Pts',(2.94667697049707,-3.31646984174982,2.4336931952875));
#27516=CARTESIAN_POINT('Ctrl Pts',(4.3836274764756,0.682412501528009,2.59265806147225));
#27517=CARTESIAN_POINT('Ctrl Pts',(1.79909822384654,4.05525838744716,2.751622927657));
#27518=CARTESIAN_POINT('Ctrl Pts',(-2.43589886829313,3.70786634730399,2.91058779384175));
#27519=CARTESIAN_POINT('Ctrl Pts',(-4.43623591518879,-0.041071433607366,
3.06955266002649));
#27520=CARTESIAN_POINT('Ctrl Pts',(-2.36683113821078,-3.75233075777553,
3.22851752621124));
#27521=CARTESIAN_POINT('Ctrl Pts',(1.87387194346144,-4.02125351849637,3.38748239239599));
#27522=CARTESIAN_POINT('Ctrl Pts',(4.39551069515703,-0.601133604410289,
3.54644725858073));
#27523=CARTESIAN_POINT('Ctrl Pts',(2.88476840715019,3.37045799480092,3.70541212476548));
#27524=CARTESIAN_POINT('Ctrl Pts',(-1.27242072438679,4.25003780948162,3.86437699095023));
#27525=CARTESIAN_POINT('Ctrl Pts',(-4.26230859154076,1.23069140940013,4.02334185713497));
#27526=CARTESIAN_POINT('Ctrl Pts',(-3.34201320012482,-2.91767435508194,
4.18230672331973));
#27527=CARTESIAN_POINT('Ctrl Pts',(0.64419911886348,-4.38940581067625,4.34127158950447));
#27528=CARTESIAN_POINT('Ctrl Pts',(4.03943202975366,-1.834356767727,4.50023645568922));
#27529=CARTESIAN_POINT('Ctrl Pts',(3.72894557392732,2.40350593524421,4.65920132187397));
#27530=CARTESIAN_POINT('Ctrl Pts',(-0.00242424579594498,4.43642536256088,
4.81816618805872));
#27531=CARTESIAN_POINT('Ctrl Pts',(-3.73157009580673,2.39942920179332,4.97713105424346));
#27532=CARTESIAN_POINT('Ctrl Pts',(-4.03742488159485,-1.83877029555123,
5.13609592042822));
#27533=CARTESIAN_POINT('Ctrl Pts',(-0.639401630874114,-4.39010722293004,
5.29506078661295));
#27534=CARTESIAN_POINT('Ctrl Pts',(3.34519987865668,-2.91402018630447,5.45402565279771));
#27535=CARTESIAN_POINT('Ctrl Pts',(4.26096104522458,1.23534887599985,5.61299051898245));
#27536=CARTESIAN_POINT('Ctrl Pts',(1.26777517433839,4.25142587630257,5.77195538516721));
#27537=CARTESIAN_POINT('Ctrl Pts',(-2.88845019850368,3.3673032719259,5.93092025135195));
#27538=CARTESIAN_POINT('Ctrl Pts',(-4.39485110065909,-0.605937024281373,
6.0898851175367));
#27539=CARTESIAN_POINT('Ctrl Pts',(-1.86947607066172,-4.02329903134028,
6.24884998372145));
#27540=CARTESIAN_POINT('Ctrl Pts',(2.37093058493492,-3.74974186255266,6.40781484990618));
#27541=CARTESIAN_POINT('Ctrl Pts',(4.43627814291787,-0.0362231007639915,
6.56677971609095));
#27542=CARTESIAN_POINT('Ctrl Pts',(2.43184517016341,3.71052623528157,6.72574458227568));
#27543=CARTESIAN_POINT('Ctrl Pts',(-1.80352910258568,4.05328985522703,6.88470944846044));
#27544=CARTESIAN_POINT('Ctrl Pts',(-4.38437059090167,0.677621130128278,
7.04367431464518));
#27545=CARTESIAN_POINT('Ctrl Pts',(-2.94305082251765,-3.31968789654059,
7.20263918082993));
#27546=CARTESIAN_POINT('Ctrl Pts',(1.19818327778767,-4.27156092162922,7.36160404701468));
#27547=CARTESIAN_POINT('Ctrl Pts',(4.2402205245368,-1.30476272849002,7.52056891319943));
#27548=CARTESIAN_POINT('Ctrl Pts',(3.39233780214647,2.85900683988128,7.67953377938417));
#27549=CARTESIAN_POINT('Ctrl Pts',(-0.567628945656141,4.39996286966301,
7.83849864556892));
#27550=CARTESIAN_POINT('Ctrl Pts',(-4.00686070857005,1.90445350073909,7.99746351175367));
#27551=CARTESIAN_POINT('Ctrl Pts',(-3.77025358677652,-2.33817530689181,
8.15642837793842));
#27552=CARTESIAN_POINT('Ctrl Pts',(-0.0748676983942658,-4.43579425831462,
8.31539324412316));
#27553=CARTESIAN_POINT('Ctrl Pts',(3.68920078641008,-2.4640765880774,8.47435811030792));
#27554=CARTESIAN_POINT('Ctrl Pts',(4.06884722849785,1.76815104148521,8.63332297649266));
#27555=CARTESIAN_POINT('Ctrl Pts',(0.715789205352545,4.37830123311092,8.79228784267741));
#27556=CARTESIAN_POINT('Ctrl Pts',(-3.29392398642918,2.97185811336718,8.95125270886215));
#27557=CARTESIAN_POINT('Ctrl Pts',(-4.28183663328808,-1.16092675057133,
9.1102175750469));
#27558=CARTESIAN_POINT('Ctrl Pts',(-1.34165126542409,-4.22869338641924,
9.26918244123165));
#27559=CARTESIAN_POINT('Ctrl Pts',(2.82934651391571,-3.41711489103788,9.42814730741641));
#27560=CARTESIAN_POINT('Ctrl Pts',(4.40474072961818,0.529277790203311,9.58711217360113));
#27561=CARTESIAN_POINT('Ctrl Pts',(1.93928640362945,3.99011830890487,9.74607703978591));
#27562=CARTESIAN_POINT('Ctrl Pts',(-2.30524258692121,3.79047918999758,9.90504190597063));
#27563=CARTESIAN_POINT('Ctrl Pts',(-4.43497374545224,0.113506614385248,
10.0640067721554));
#27564=CARTESIAN_POINT('Ctrl Pts',(-2.49612100953394,-3.66759536755666,
10.2229716383401));
#27565=CARTESIAN_POINT('Ctrl Pts',(1.73263879706324,-4.08409582077491,10.3819365045249));
#27566=CARTESIAN_POINT('Ctrl Pts',(4.3718996101527,-0.753902960006452,10.5409013707096));
#27567=CARTESIAN_POINT('Ctrl Pts',(3.00043987269634,3.26791010352089,10.6998662368944));
#27568=CARTESIAN_POINT('Ctrl Pts',(-1.12358212171453,4.29178740038732,10.8588311030791));
#27569=CARTESIAN_POINT('Ctrl Pts',(-4.21684533673315,1.37843798570399,11.0177959692639));
#27570=CARTESIAN_POINT('Ctrl Pts',(-3.44163265829037,-2.79947147150118,
11.1767608354486));
#27571=CARTESIAN_POINT('Ctrl Pts',(0.490886468356214,-4.40918431793734,
11.3357257016334));
#27572=CARTESIAN_POINT('Ctrl Pts',(3.97307310290967,-1.97397213589646,11.4946905678181));
#27573=CARTESIAN_POINT('Ctrl Pts',(3.8104171373138,2.27213492425632,11.6536554340029));
#27574=CARTESIAN_POINT('Ctrl Pts',(0.152136916465922,4.43381666659865,11.8126203001876));
#27575=CARTESIAN_POINT('Ctrl Pts',(-3.64571161833625,2.52797600271203,11.9715851663724));
#27576=CARTESIAN_POINT('Ctrl Pts',(-4.09903447485687,-1.69699506431066,
12.1305500325571));
#27577=CARTESIAN_POINT('Ctrl Pts',(-0.791959501672948,-4.36516620784018,
12.2895148987418));
#27578=CARTESIAN_POINT('Ctrl Pts',(3.24164822198482,-3.02879393146226,12.4484797649266));
#27579=CARTESIAN_POINT('Ctrl Pts',(4.30141246777259,1.08615222526604,12.6074446311113));
#27580=CARTESIAN_POINT('Ctrl Pts',(1.41512009762014,4.2046772746159,12.7664094972961));
#27581=CARTESIAN_POINT('Ctrl Pts',(-2.76938397982661,3.4658892432736,12.9253743634808));
#27582=CARTESIAN_POINT('Ctrl Pts',(-4.41329329740075,-0.452457893596237,
13.0843392296656));
#27583=CARTESIAN_POINT('Ctrl Pts',(-2.00850806527244,-3.95572638412914,
13.2433040958503));
#27584=CARTESIAN_POINT('Ctrl Pts',(2.23885483140653,-3.83006591565308,13.4022689620351));
#27585=CARTESIAN_POINT('Ctrl Pts',(4.43232310956353,-0.19075567301893,13.5612338282198));
#27586=CARTESIAN_POINT('Ctrl Pts',(2.55963915016612,3.62355119948605,13.7201986944046));
#27587=CARTESIAN_POINT('Ctrl Pts',(-1.66122254819691,4.11366205706328,13.8791635605893));
#27588=CARTESIAN_POINT('Ctrl Pts',(-4.35810153716492,0.829955942276827,
14.0381284267741));
#27589=CARTESIAN_POINT('Ctrl Pts',(-3.05691813790205,-3.21514033481048,
14.1970932929588));
#27590=CARTESIAN_POINT('Ctrl Pts',(1.04863990174551,-4.31071110500657,14.3560581591436));
#27591=CARTESIAN_POINT('Ctrl Pts',(4.19219012349031,-1.45169481740146,14.5150230253283));
#27592=CARTESIAN_POINT('Ctrl Pts',(3.48988280517811,2.73908632220345,14.6739878915131));
#27593=CARTESIAN_POINT('Ctrl Pts',(-0.413994982231739,4.41706735618179,
14.8329527576978));
#27594=CARTESIAN_POINT('Ctrl Pts',(-3.93807946898943,2.04289157085825,14.9919176238826));
#27595=CARTESIAN_POINT('Ctrl Pts',(-3.84942403388813,-2.20540483396684,
15.1508824900673));
#27596=CARTESIAN_POINT('Ctrl Pts',(-0.229359953303091,-4.4304931876915,
15.3098473562521));
#27597=CARTESIAN_POINT('Ctrl Pts',(3.60111579273939,-2.5911080490097,15.4688122224368));
#27598=CARTESIAN_POINT('Ctrl Pts',(4.12797745732068,1.62532396346455,15.6277770886216));
#27599=CARTESIAN_POINT('Ctrl Pts',(0.867889398303981,4.35070613425814,15.7867419548063));
#27600=CARTESIAN_POINT('Ctrl Pts',(-3.18838845365656,3.08481035769615,15.9457068209911));
#27601=CARTESIAN_POINT('Ctrl Pts',(-4.31968260642442,-1.01104799792802,
16.1046716871758));
#27602=CARTESIAN_POINT('Ctrl Pts',(-1.48815936942683,-4.1793848309945,16.2636365533605));
#27603=CARTESIAN_POINT('Ctrl Pts',(2.70858079789248,-3.51361152315505,16.4226014195453));
#27604=CARTESIAN_POINT('Ctrl Pts',(4.42050620787071,0.375500653176939,16.5815662857301));
#27605=CARTESIAN_POINT('Ctrl Pts',(2.07712004332191,3.92013369669841,16.7405311519148));
#27606=CARTESIAN_POINT('Ctrl Pts',(-2.17178747042617,3.8684900229495,16.8994960180995));
#27607=CARTESIAN_POINT('Ctrl Pts',(-4.42832703985357,0.267946827675841,
17.0584608842843));
#27608=CARTESIAN_POINT('Ctrl Pts',(-2.62238031109761,-3.57840710069821,
17.217425750469));
#27609=CARTESIAN_POINT('Ctrl Pts',(1.58930203442347,-4.14197958924682,17.3763906166538));
#27610=CARTESIAN_POINT('Ctrl Pts',(4.34298056035004,-0.905756991020003,
17.5353554828385));
#27611=CARTESIAN_POINT('Ctrl Pts',(3.11246847413016,3.16139460869816,17.6943203490233));
#27612=CARTESIAN_POINT('Ctrl Pts',(-0.973379366627741,4.32832629118729,
17.853285215208));
#27613=CARTESIAN_POINT('Ctrl Pts',(-4.16626236891013,1.52451098643573,18.0122500813928));
#27614=CARTESIAN_POINT('Ctrl Pts',(-3.53707359645429,-2.67786972192929,
18.1712149475776));
#27615=CARTESIAN_POINT('Ctrl Pts',(0.336977827730321,-4.42360959149628,
18.3301798137622));
#27616=CARTESIAN_POINT('Ctrl Pts',(3.90189042914389,-2.11119088509681,18.489144679947));
#27617=CARTESIAN_POINT('Ctrl Pts',(3.88726243593711,2.13800529197465,18.6481095461317));
#27618=CARTESIAN_POINT('Ctrl Pts',(0.306513367815784,4.42582483043659,18.8070744123165));
#27619=CARTESIAN_POINT('Ctrl Pts',(-3.55542684670427,2.6534535632075,18.9660392785013));
#27620=CARTESIAN_POINT('Ctrl Pts',(-4.15566739023229,-1.5531594947446,19.125004144686));
#27621=CARTESIAN_POINT('Ctrl Pts',(-0.943555846690173,-4.33492540172624,
19.2839690108708));
#27622=CARTESIAN_POINT('Ctrl Pts',(3.13416084847543,-3.13989038825732,19.4429338770555));
#27623=CARTESIAN_POINT('Ctrl Pts',(4.33664150332913,0.935636866485059,19.6018987432403));
#27624=CARTESIAN_POINT('Ctrl Pts',(1.5607469097475,4.15282373308227,19.760863609425));
#27625=CARTESIAN_POINT('Ctrl Pts',(-2.6469554249668,3.56026724457307,19.9198284756097));
#27626=CARTESIAN_POINT('Ctrl Pts',(-4.42637727151094,-0.298429429375862,
20.0787933417945));
#27627=CARTESIAN_POINT('Ctrl Pts',(-2.14510151064494,-3.88335105074656,
20.2377582079792));
#27628=CARTESIAN_POINT('Ctrl Pts',(2.10406086243651,-3.90573984831374,20.396723074164));
#27629=CARTESIAN_POINT('Ctrl Pts',(4.42298674908946,-0.345056646784782,
20.5556879403487));
#27630=CARTESIAN_POINT('Ctrl Pts',(2.68432544768054,3.53217677440245,20.7146528065335));
#27631=CARTESIAN_POINT('Ctrl Pts',(-1.51689908813168,4.16903982210505,20.8736176727182));
#27632=CARTESIAN_POINT('Ctrl Pts',(-4.32654126800335,0.981283095682997,
21.032582538903));
#27633=CARTESIAN_POINT('Ctrl Pts',(-3.16707402226655,-3.10668923760898,
21.1915474050877));
#27634=CARTESIAN_POINT('Ctrl Pts',(0.897823367877824,-4.34462761587273,
21.3505122712725));
#27635=CARTESIAN_POINT('Ctrl Pts',(4.13906993163872,-1.59686438170456,21.5094771374572));
#27636=CARTESIAN_POINT('Ctrl Pts',(3.58319072974711,2.61584023826454,21.668442003642));
#27637=CARTESIAN_POINT('Ctrl Pts',(-0.25985842625908,4.42880906613994,21.8274068698267));
#27638=CARTESIAN_POINT('Ctrl Pts',(-3.86451688680425,2.17884929254253,21.9863717360115));
#27639=CARTESIAN_POINT('Ctrl Pts',(-3.92392101376968,-2.0699566547274,22.1453366021962));
#27640=CARTESIAN_POINT('Ctrl Pts',(-0.383573441765164,-4.41981320809673,
22.304301468381));
#27641=CARTESIAN_POINT('Ctrl Pts',(3.50865807943151,-2.71499324560195,22.4632663345657));
#27642=CARTESIAN_POINT('Ctrl Pts',(4.1820969563918,1.48052284807099,22.6222312007505));
#27643=CARTESIAN_POINT('Ctrl Pts',(1.01893380005702,4.31783016731854,22.7811960669352));
#27644=CARTESIAN_POINT('Ctrl Pts',(-3.07897789805066,3.19401469302683,22.9401609331199));
#27645=CARTESIAN_POINT('Ctrl Pts',(-4.35229159153774,-0.859936736039379,
23.0991257993047));
#27646=CARTESIAN_POINT('Ctrl Pts',(-1.63284620549922,-4.12501156642513,
23.2580906654894));
#27647=CARTESIAN_POINT('Ctrl Pts',(2.58449891329166,-3.60582405699598,23.4170555316742));
#27648=CARTESIAN_POINT('Ctrl Pts',(4.43095752393771,0.221232878887186,23.5760203978589));
#27649=CARTESIAN_POINT('Ctrl Pts',(2.21233095217787,3.84545596028211,23.7349852640437));
#27650=CARTESIAN_POINT('Ctrl Pts',(-2.03550288714815,3.94167735716416,23.8939501302284));
#27651=CARTESIAN_POINT('Ctrl Pts',(-4.41667191344595,0.422303815586678,
24.0529149964132));
#27652=CARTESIAN_POINT('Ctrl Pts',(-2.74475234343696,-3.48533708285041,
24.2118798625979));
#27653=CARTESIAN_POINT('Ctrl Pts',(1.44268822216767,-4.19394659738156,24.3708447287827));
#27654=CARTESIAN_POINT('Ctrl Pts',(4.31139752937088,-1.05824235775403,24.5298095949674));
#27655=CARTESIAN_POINT('Ctrl Pts',(3.21542349488533,3.05465556777655,24.6887744611522));
#27656=CARTESIAN_POINT('Ctrl Pts',(0.532349745525053,3.91839843762163,24.7947510386087));
#27657=CARTESIAN_POINT('Ctrl Pts',(-0.695166797717585,3.68695291493697,
24.8477393273369));
#27658=CARTESIAN_POINT('Ctrl Pts',(-1.72703261341866,3.5435465782445,-1.38777878078145E-15));
#27659=CARTESIAN_POINT('Ctrl Pts',(-2.90680413394004,2.96855656546122,0.0529882887282479));
#27660=CARTESIAN_POINT('Ctrl Pts',(-4.62630819919985,0.557402612567225,
0.158964866184747));
#27661=CARTESIAN_POINT('Ctrl Pts',(-2.96987709591773,-3.59657838999538,
0.317929732369494));
#27662=CARTESIAN_POINT('Ctrl Pts',(1.41505673442732,-4.43979476933175,0.476894598554242));
#27663=CARTESIAN_POINT('Ctrl Pts',(4.49979514193284,-1.21565677818381,0.635859464738989));
#27664=CARTESIAN_POINT('Ctrl Pts',(3.45754786720525,3.12663666251093,0.794824330923737));
#27665=CARTESIAN_POINT('Ctrl Pts',(-0.757163062900767,4.59906675017539,
0.953789197108486));
#27666=CARTESIAN_POINT('Ctrl Pts',(-4.27697154027288,1.85317690565,1.11275406329323));
#27667=CARTESIAN_POINT('Ctrl Pts',(-3.87329777622707,-2.593211080757,1.27171892947798));
#27668=CARTESIAN_POINT('Ctrl Pts',(0.0837659752953463,-4.66040345053054,
1.43068379566273));
#27669=CARTESIAN_POINT('Ctrl Pts',(3.96394214022417,-2.45232071482198,1.58964866184748));
#27670=CARTESIAN_POINT('Ctrl Pts',(4.20767422754857,2.00554746219876,1.74861352803222));
#27671=CARTESIAN_POINT('Ctrl Pts',(0.591332402870964,4.62352249362764,1.90757839421698));
#27672=CARTESIAN_POINT('Ctrl Pts',(-3.5674836278665,2.99995809464374,2.06654326040171));
#27673=CARTESIAN_POINT('Ctrl Pts',(-4.45354240620347,-1.37573521927647,
2.22550812658647));
#27674=CARTESIAN_POINT('Ctrl Pts',(-1.25398101020607,-4.48934345055757,
2.38447299277121));
#27675=CARTESIAN_POINT('Ctrl Pts',(3.09596444955676,-3.48449213500062,2.54343785895597));
#27676=CARTESIAN_POINT('Ctrl Pts',(4.60571517107261,0.716985562318844,2.70240272514071));
#27677=CARTESIAN_POINT('Ctrl Pts',(1.89024592721134,4.26070992070277,2.86136759132546));
#27678=CARTESIAN_POINT('Ctrl Pts',(-2.55930879918572,3.89571795955106,3.0203324575102));
#27679=CARTESIAN_POINT('Ctrl Pts',(-4.66098891082537,-0.0431522354210798,
3.17929732369495));
#27680=CARTESIAN_POINT('Ctrl Pts',(-2.48674189107617,-3.94243507020443,
3.3382621898797));
#27681=CARTESIAN_POINT('Ctrl Pts',(1.96880790736958,-4.22498226326438,3.49722705606445));
#27682=CARTESIAN_POINT('Ctrl Pts',(4.61820042919637,-0.631588832885941,
3.65619192224919));
#27683=CARTESIAN_POINT('Ctrl Pts',(3.0309194130074,3.54121548955118,3.81515678843395));
#27684=CARTESIAN_POINT('Ctrl Pts',(-1.33688536850928,4.46535745151852,3.97412165461869));
#27685=CARTESIAN_POINT('Ctrl Pts',(-4.47824990814127,1.29304192146821,4.13308652080344));
#27686=CARTESIAN_POINT('Ctrl Pts',(-3.51132959639971,-3.06549247479725,
4.29205138698818));
#27687=CARTESIAN_POINT('Ctrl Pts',(0.676836175259727,-4.61178625298691,
4.45101625317294));
#27688=CARTESIAN_POINT('Ctrl Pts',(4.24408175233697,-1.92729077450542,4.60998111935768));
#27689=CARTESIAN_POINT('Ctrl Pts',(3.91786512291623,2.52527474314889,4.76894598554243));
#27690=CARTESIAN_POINT('Ctrl Pts',(-0.00254706534730991,4.66118795616863,
4.92791085172718));
#27691=CARTESIAN_POINT('Ctrl Pts',(-3.92062261093312,2.52099147017371,5.08687571791192));
#27692=CARTESIAN_POINT('Ctrl Pts',(-4.24197291604209,-1.93192790486543,
5.24584058409668));
#27693=CARTESIAN_POINT('Ctrl Pts',(-0.671795632162863,-4.61252320088583,
5.40480545028142));
#27694=CARTESIAN_POINT('Ctrl Pts',(3.51467772160843,-3.0616531748872,5.56377031646618));
#27695=CARTESIAN_POINT('Ctrl Pts',(4.47683409109351,1.29793534927254,5.72273518265091));
#27696=CARTESIAN_POINT('Ctrl Pts',(1.33200446098445,4.46681584196115,5.88170004883567));
#27697=CARTESIAN_POINT('Ctrl Pts',(-3.03478773493588,3.53790093896858,6.04066491502041));
#27698=CARTESIAN_POINT('Ctrl Pts',(-4.61750741766603,-0.636635608391419,
6.19962978120516));
#27699=CARTESIAN_POINT('Ctrl Pts',(-1.96418932649049,-4.22713140791419,
6.35859464738991));
#27700=CARTESIAN_POINT('Ctrl Pts',(2.49104902804703,-3.93971501379719,6.51755951357465));
#27701=CARTESIAN_POINT('Ctrl Pts',(4.66103327793766,-0.0380582715176506,
6.6765243797594));
#27702=CARTESIAN_POINT('Ctrl Pts',(2.55504972857005,3.89851260541856,6.83548924594414));
#27703=CARTESIAN_POINT('Ctrl Pts',(-1.89490128753556,4.25864165674564,6.9944541121289));
#27704=CARTESIAN_POINT('Ctrl Pts',(-4.60649593390074,0.711951445696367,
7.15341897831364));
#27705=CARTESIAN_POINT('Ctrl Pts',(-3.09215459006229,-3.48787322608348,
7.3123838444984));
#27706=CARTESIAN_POINT('Ctrl Pts',(1.25888683056368,-4.48797098897782,7.47134871068314));
#27707=CARTESIAN_POINT('Ctrl Pts',(4.45504279352084,-1.3708659153875,7.63031357686789));
#27708=CARTESIAN_POINT('Ctrl Pts',(3.56420379345526,3.00385268759844,7.78927844305264));
#27709=CARTESIAN_POINT('Ctrl Pts',(-0.596386727790659,4.62287816419472,
7.94824330923738));
#27710=CARTESIAN_POINT('Ctrl Pts',(-4.20986027048837,2.00093881791443,8.10720817542214));
#27711=CARTESIAN_POINT('Ctrl Pts',(-3.96126592339197,-2.45663426953358,
8.26617304160689));
#27712=CARTESIAN_POINT('Ctrl Pts',(-0.0786607201839425,-4.66052487829143,
8.42513790779162));
#27713=CARTESIAN_POINT('Ctrl Pts',(3.87610674544883,-2.58891408663156,8.58410277397638));
#27714=CARTESIAN_POINT('Ctrl Pts',(4.27498721313245,1.85773086792121,8.74306764016112));
#27715=CARTESIAN_POINT('Ctrl Pts',(0.752053229904626,4.60011908426979,8.90203250634587));
#27716=CARTESIAN_POINT('Ctrl Pts',(-3.46080403913657,3.12242134452881,9.06099737253062));
#27717=CARTESIAN_POINT('Ctrl Pts',(-4.49876729895963,-1.21974277611503,
9.21996223871536));
#27718=CARTESIAN_POINT('Ctrl Pts',(-1.40962333606424,-4.44293165606859,
9.37892710490011));
#27719=CARTESIAN_POINT('Ctrl Pts',(2.97268968070251,-3.59023616386415,9.53789197108486));
#27720=CARTESIAN_POINT('Ctrl Pts',(4.62789808484238,0.556092587961218,9.69685683726961));
#27721=CARTESIAN_POINT('Ctrl Pts',(2.03753645997128,4.19226965072155,9.85582170345435));
#27722=CARTESIAN_POINT('Ctrl Pts',(-2.42203307935326,3.98251621623715,10.0147865696391));
#27723=CARTESIAN_POINT('Ctrl Pts',(-4.65966279579043,0.119257199362087,
10.1737514358238));
#27724=CARTESIAN_POINT('Ctrl Pts',(-2.62258197443514,-3.85340673137953,
10.3327163020086));
#27725=CARTESIAN_POINT('Ctrl Pts',(1.82041946685649,-4.2910083447557,10.4916811681933));
#27726=CARTESIAN_POINT('Ctrl Pts',(4.59339313592305,-0.792097941499782,
10.6506460343781));
#27727=CARTESIAN_POINT('Ctrl Pts',(3.15245114137279,3.43347221502238,10.8096109005628));
#27728=CARTESIAN_POINT('Ctrl Pts',(-1.18050615653299,4.50922220171738,10.9685757667476));
#27729=CARTESIAN_POINT('Ctrl Pts',(-4.43048334870678,1.44827378175024,11.1275406329323));
#27730=CARTESIAN_POINT('Ctrl Pts',(-3.61599607462336,-2.94130107917936,
11.2865054991171));
#27731=CARTESIAN_POINT('Ctrl Pts',(0.515756246787712,-4.63256679865198,
11.4454703653018));
#27732=CARTESIAN_POINT('Ctrl Pts',(4.17436088354928,-2.07397947530031,11.6044352314866));
#27733=CARTESIAN_POINT('Ctrl Pts',(4.00346427966798,2.38724808335786,11.7634000976713));
#27734=CARTESIAN_POINT('Ctrl Pts',(0.159844628223428,4.6584470958573,11.9223649638561));
#27735=CARTESIAN_POINT('Ctrl Pts',(-3.83041428589339,2.65605083695643,12.0813298300408));
#27736=CARTESIAN_POINT('Ctrl Pts',(-4.3067038357868,-1.7829699158686,12.2402946962256));
#27737=CARTESIAN_POINT('Ctrl Pts',(-0.832082541526254,-4.58631859928641,
12.3992595624103));
#27738=CARTESIAN_POINT('Ctrl Pts',(3.40587982792729,-3.18224170166115,12.5582244285951));
#27739=CARTESIAN_POINT('Ctrl Pts',(4.51933490383836,1.14117994944773,12.7171892947798));
#27740=CARTESIAN_POINT('Ctrl Pts',(1.48681431929952,4.41769881612578,12.8761541609645));
#27741=CARTESIAN_POINT('Ctrl Pts',(-2.90968926508048,3.64148157083744,13.0351190271493));
#27742=CARTESIAN_POINT('Ctrl Pts',(-4.63688395131922,-0.475380765357195,
13.1940838933341));
#27743=CARTESIAN_POINT('Ctrl Pts',(-2.11026509827526,-4.1561353280511,13.3530487595188));
#27744=CARTESIAN_POINT('Ctrl Pts',(2.35228192134809,-4.0241085239556,13.5120136257036));
#27745=CARTESIAN_POINT('Ctrl Pts',(4.65687787075036,-0.200419926626097,
13.6709784918883));
#27746=CARTESIAN_POINT('Ctrl Pts',(2.68931813427488,3.80713115386554,13.829943358073));
#27747=CARTESIAN_POINT('Ctrl Pts',(-1.74538505696882,4.32207249510964,13.9889082242578));
#27748=CARTESIAN_POINT('Ctrl Pts',(-4.57889601123979,0.872003995590307,
14.1478730904425));
#27749=CARTESIAN_POINT('Ctrl Pts',(-3.21179076461628,-3.37802897181164,
14.3068379566273));
#27750=CARTESIAN_POINT('Ctrl Pts',(1.10176713928815,-4.5291046378791,14.465802822812));
#27751=CARTESIAN_POINT('Ctrl Pts',(4.40457902853176,-1.52524202390685,14.6247676889968));
#27752=CARTESIAN_POINT('Ctrl Pts',(3.66669071843603,2.87785663739672,14.7837325551815));
#27753=CARTESIAN_POINT('Ctrl Pts',(-0.434969207726955,4.6408492152194,14.9426974213663));
#27754=CARTESIAN_POINT('Ctrl Pts',(-4.13759436734728,2.14639057521441,15.101662287551));
#27755=CARTESIAN_POINT('Ctrl Pts',(-4.04444738242773,-2.3171372468731,15.2606271537358));
#27756=CARTESIAN_POINT('Ctrl Pts',(-0.240980015348797,-4.65495523955664,
15.4195920199205));
#27757=CARTESIAN_POINT('Ctrl Pts',(3.78355910223096,-2.72238134176653,15.5785568861053));
#27758=CARTESIAN_POINT('Ctrl Pts',(4.33711315641111,1.7076677424367,15.73752175229));
#27759=CARTESIAN_POINT('Ctrl Pts',(0.911859274090375,4.57112593507645,15.8964866184748));
#27760=CARTESIAN_POINT('Ctrl Pts',(-3.34992176025076,3.24109608778754,16.0554514846595));
#27761=CARTESIAN_POINT('Ctrl Pts',(-4.53853066242366,-1.06227071705545,
16.2144163508443));
#27762=CARTESIAN_POINT('Ctrl Pts',(-1.56355397932982,-4.39112498157307,
16.373381217029));
#27763=CARTESIAN_POINT('Ctrl Pts',(2.8458056118763,-3.69162160432059,16.5323460832138));
#27764=CARTESIAN_POINT('Ctrl Pts',(4.64446228943243,0.394524640692141,16.6913109493985));
#27765=CARTESIAN_POINT('Ctrl Pts',(2.18235316458919,4.11873940849393,16.8502758155833));
#27766=CARTESIAN_POINT('Ctrl Pts',(-2.2818167270293,4.06447931158747,17.009240681768));
#27767=CARTESIAN_POINT('Ctrl Pts',(-4.65267934818278,0.281521816324489,
17.1682055479527));
#27768=CARTESIAN_POINT('Ctrl Pts',(-2.75523795029565,-3.75969991985049,
17.3271704141375));
#27769=CARTESIAN_POINT('Ctrl Pts',(1.66982083460383,-4.35182467826958,17.4861352803222));
#27770=CARTESIAN_POINT('Ctrl Pts',(4.56300896046017,-0.95164535244674,17.645100146507));
#27771=CARTESIAN_POINT('Ctrl Pts',(3.27015544722148,3.32156032627453,17.8040650126917));
#27772=CARTESIAN_POINT('Ctrl Pts',(-1.02269368009593,4.54761226213988,17.9630298788765));
#27773=CARTESIAN_POINT('Ctrl Pts',(-4.37733769626469,1.6017472781102,18.1219947450612));
#27774=CARTESIAN_POINT('Ctrl Pts',(-3.71627233650965,-2.81353862084143,
18.280959611246));
#27775=CARTESIAN_POINT('Ctrl Pts',(0.354050133552978,-4.64772289976546,
18.4399244774307));
#27776=CARTESIAN_POINT('Ctrl Pts',(4.09957188237618,-2.21815013723249,18.5988893436155));
#27777=CARTESIAN_POINT('Ctrl Pts',(4.08420279123045,2.24632304225772,18.7578542098002));
#27778=CARTESIAN_POINT('Ctrl Pts',(0.322042252874243,4.65005036934395,18.916819075985));
#27779=CARTESIAN_POINT('Ctrl Pts',(-3.73555541737554,2.78788546640533,19.0757839421697));
#27780=CARTESIAN_POINT('Ctrl Pts',(-4.36620594424068,-1.63184720563709,
19.2347488083544));
#27781=CARTESIAN_POINT('Ctrl Pts',(-0.991359211332678,-4.55454570337957,
19.3937136745392));
#27782=CARTESIAN_POINT('Ctrl Pts',(3.29294682220825,-3.29896663763241,19.5526785407239));
#27783=CARTESIAN_POINT('Ctrl Pts',(4.55634874782847,0.983039031877256,19.7116434069087));
#27784=CARTESIAN_POINT('Ctrl Pts',(1.63981902180431,4.3632182189042,19.8706082730935));
#27785=CARTESIAN_POINT('Ctrl Pts',(-2.7810581130229,3.74064104429479,20.0295731392782));
#27786=CARTESIAN_POINT('Ctrl Pts',(-4.65063079873739,-0.313548757905883,
20.188538005463));
#27787=CARTESIAN_POINT('Ctrl Pts',(-2.25377877661524,-4.08009324355364,
20.3475028716477));
#27788=CARTESIAN_POINT('Ctrl Pts',(2.21065888627362,-4.10361632464813,20.5064677378324));
#27789=CARTESIAN_POINT('Ctrl Pts',(4.64706850229723,-0.362538249772487,
20.6654326040172));
#27790=CARTESIAN_POINT('Ctrl Pts',(2.82032141299069,3.71112742678928,20.824397470202));
#27791=CARTESIAN_POINT('Ctrl Pts',(-1.59374973824449,4.38025586355546,20.9833623363867));
#27792=CARTESIAN_POINT('Ctrl Pts',(-4.54573680433624,1.03099783573258,21.1423272025715));
#27793=CARTESIAN_POINT('Ctrl Pts',(-3.32752747594111,-3.2640834172724,21.3012920687562));
#27794=CARTESIAN_POINT('Ctrl Pts',(0.943309788199209,-4.5647394607477,21.4602569349409));
#27795=CARTESIAN_POINT('Ctrl Pts',(4.34876760869419,-1.67776631304337,21.6192218011257));
#27796=CARTESIAN_POINT('Ctrl Pts',(3.76472590187142,2.74836653778883,21.7781866673104));
#27797=CARTESIAN_POINT('Ctrl Pts',(-0.273023632271506,4.65318579536423,
21.9371515334952));
#27798=CARTESIAN_POINT('Ctrl Pts',(-4.06030488446768,2.28923632220046,22.0961163996799));
#27799=CARTESIAN_POINT('Ctrl Pts',(-4.12271860238902,-2.17482685727795,
22.2550812658647));
#27800=CARTESIAN_POINT('Ctrl Pts',(-0.403006420923942,-4.64373418021473,
22.4140461320495));
#27801=CARTESIAN_POINT('Ctrl Pts',(3.68641720430509,-2.85254293338859,22.5730109982341));
#27802=CARTESIAN_POINT('Ctrl Pts',(4.39397451136436,1.55553056893478,22.7319758644189));
#27803=CARTESIAN_POINT('Ctrl Pts',(1.07055603753408,4.53658437320562,22.8909407306037));
#27804=CARTESIAN_POINT('Ctrl Pts',(-3.2349681382713,3.35583304175512,23.0499055967884));
#27805=CARTESIAN_POINT('Ctrl Pts',(-4.57279171636944,-0.903503706141469,
23.2088704629732));
#27806=CARTESIAN_POINT('Ctrl Pts',(-1.71557108377795,-4.33399700460152,
23.3678353291579));
#27807=CARTESIAN_POINT('Ctrl Pts',(2.71543736744218,-3.78850590125353,23.5268001953427));
#27808=CARTESIAN_POINT('Ctrl Pts',(4.65544310046753,0.232441199006727,23.6857650615274));
#27809=CARTESIAN_POINT('Ctrl Pts',(2.32441426297274,4.04027827433057,23.8447299277122));
#27810=CARTESIAN_POINT('Ctrl Pts',(-2.13862755866238,4.14137453531068,24.0036947938969));
#27811=CARTESIAN_POINT('Ctrl Pts',(-4.64043373817043,0.443698991460186,
24.1626596600816));
#27812=CARTESIAN_POINT('Ctrl Pts',(-2.88380971623262,-3.66191469620319,
24.3216245262664));
#27813=CARTESIAN_POINT('Ctrl Pts',(1.51577912758857,-4.40642449065004,24.4805893924511));
#27814=CARTESIAN_POINT('Ctrl Pts',(4.52982583855719,-1.1118560844723,24.6395542586359));
#27815=CARTESIAN_POINT('Ctrl Pts',(3.37832647762378,3.20941356591303,24.7985191248206));
#27816=CARTESIAN_POINT('Ctrl Pts',(0.559320177738415,4.11691623599613,24.9044957022771));
#27817=CARTESIAN_POINT('Ctrl Pts',(-0.730386029345736,3.8737449900757,24.9574839910054));
#27818=CARTESIAN_POINT('Ctrl Pts',(-3.94350653563855,-0.00347714007584369,
23.1778238829104));
#27819=CARTESIAN_POINT('Ctrl Pts',(-3.94586355936157,-0.259474013504655,
23.1881727429313));
#27820=CARTESIAN_POINT('Ctrl Pts',(-3.92307523690983,-0.515053183369563,
23.1985216029522));
#27821=CARTESIAN_POINT('Ctrl Pts',(-3.87361768125451,-0.765363131235343,
23.2088704629732));
#27822=CARTESIAN_POINT('Ctrl Pts',(-3.62038483883896,-2.0470014722948,23.2618587517014));
#27823=CARTESIAN_POINT('Ctrl Pts',(-2.66797796130846,-3.19049923844816,
23.3148470404297));
#27824=CARTESIAN_POINT('Ctrl Pts',(-1.45327311400651,-3.67133293763351,
23.3678353291579));
#27825=CARTESIAN_POINT('Ctrl Pts',(-0.238568266704596,-4.15216663681884,
23.4208236178862));
#27826=CARTESIAN_POINT('Ctrl Pts',(1.23843455036875,-3.9703362690362,23.4738119066144));
#27827=CARTESIAN_POINT('Ctrl Pts',(2.30027024774299,-3.20926323510153,23.5268001953427));
#27828=CARTESIAN_POINT('Ctrl Pts',(3.36210594511727,-2.44819020116684,23.5797884840709));
#27829=CARTESIAN_POINT('Ctrl Pts',(4.00877452279241,-1.10787450108007,23.6327767727992));
#27830=CARTESIAN_POINT('Ctrl Pts',(3.94360400538084,0.196922861517294,23.6857650615274));
#27831=CARTESIAN_POINT('Ctrl Pts',(3.87843348796927,1.50172022411466,23.7387533502557));
#27832=CARTESIAN_POINT('Ctrl Pts',(3.10142387547099,2.77099924922264,23.7917416389839));
#27833=CARTESIAN_POINT('Ctrl Pts',(1.96907876561599,3.42248813860663,23.8447299277122));
#27834=CARTESIAN_POINT('Ctrl Pts',(0.836733655761017,4.07397702799061,23.8977182164404));
#27835=CARTESIAN_POINT('Ctrl Pts',(-0.650946951450773,4.10767578165063,
23.9507065051686));
#27836=CARTESIAN_POINT('Ctrl Pts',(-1.81175495164127,3.50824590117222,24.0036947938969));
#27837=CARTESIAN_POINT('Ctrl Pts',(-2.20830746798924,3.30347006620307,24.0217965292646));
#27838=CARTESIAN_POINT('Ctrl Pts',(-2.56671309215799,3.02480645592577,24.0398982646323));
#27839=CARTESIAN_POINT('Ctrl Pts',(-2.87170785494343,2.69478584831398,24.058));
#27840=CARTESIAN_POINT('Ctrl Pts',(-1.96186193197213,-2.74910310536279,
1.04083408558608E-17));
#27841=CARTESIAN_POINT('Ctrl Pts',(-2.03089214936932,-2.70842374984998,
4.0844089957036E-17));
#27842=CARTESIAN_POINT('Ctrl Pts',(-2.0982520786512,-2.66519645821488,9.07751022854637E-17));
#27843=CARTESIAN_POINT('Ctrl Pts',(-2.16378064478676,-2.619448737651,1.42247325030098E-16));
#27844=CARTESIAN_POINT('Ctrl Pts',(-2.25130095090051,-2.55834783549675,
1.98311708005797E-16));
#27845=CARTESIAN_POINT('Ctrl Pts',(-2.33555581159229,-2.49275291176235,
1.14301651927622E-16));
#27846=CARTESIAN_POINT('Ctrl Pts',(-2.41645347142118,-2.4230636931251,1.90819582357449E-16));
#27847=CARTESIAN_POINT('Ctrl Pts',(-2.46698855966785,-2.37953028534638,
2.38618744594068E-16));
#27848=CARTESIAN_POINT('Ctrl Pts',(-2.51621317497323,-2.33439817262585,
-8.87118969308996E-17));
#27849=CARTESIAN_POINT('Ctrl Pts',(-2.56410004332752,-2.28775595645186,
-9.0205620750794E-17));
#27850=CARTESIAN_POINT('Ctrl Pts',(-2.58450501257648,-2.26788134323446,
-9.08421081566083E-17));
#27851=CARTESIAN_POINT('Ctrl Pts',(-2.60466703883067,-2.24773246660606,
1.20223089018126E-16));
#27852=CARTESIAN_POINT('Ctrl Pts',(-2.62458377340069,-2.22731585490721,
1.31838984174237E-16));
#27853=CARTESIAN_POINT('Ctrl Pts',(-2.6428539078105,-2.20858717031188,1.42494544454281E-16));
#27854=CARTESIAN_POINT('Ctrl Pts',(-2.66092072754138,-2.18962968712113,
4.62480998826576E-16));
#27855=CARTESIAN_POINT('Ctrl Pts',(-2.67876242915531,-2.17047018454057,
4.44089209850063E-16));
#27856=CARTESIAN_POINT('Ctrl Pts',(-2.75353668750271,-2.09017304546908,
3.67009545019966E-16));
#27857=CARTESIAN_POINT('Ctrl Pts',(-2.82442308955658,-2.00626812836577,
4.38199731939201E-16));
#27858=CARTESIAN_POINT('Ctrl Pts',(-2.89132427090349,-1.91917015947591,
2.28983498828939E-16));
#27859=CARTESIAN_POINT('Ctrl Pts',(-2.9553640840902,-1.83579737674842,2.87154585004375E-17));
#27860=CARTESIAN_POINT('Ctrl Pts',(-3.01575243661163,-1.74949800545801,
1.64657856526806E-16));
#27861=CARTESIAN_POINT('Ctrl Pts',(-3.07237914628982,-1.6606009570442,2.22044604925031E-16));
#27862=CARTESIAN_POINT('Ctrl Pts',(-3.09715333177403,-1.62170849836315,
2.47151307349255E-16));
#27863=CARTESIAN_POINT('Ctrl Pts',(-3.12120717339458,-1.58231843772374,
3.74830717982145E-16));
#27864=CARTESIAN_POINT('Ctrl Pts',(-3.14452974084395,-1.54245667505035,
4.16333634234434E-16));
#27865=CARTESIAN_POINT('Ctrl Pts',(-3.1552141693008,-1.52419538574881,4.35346761344512E-16));
#27866=CARTESIAN_POINT('Ctrl Pts',(-3.1657451101877,-1.50583508811633,6.65859873947159E-18));
#27867=CARTESIAN_POINT('Ctrl Pts',(-3.17612143314624,-1.48737821330264,
4.16333634234434E-17));
#27868=CARTESIAN_POINT('Ctrl Pts',(-3.1851701035806,-1.47128289918176,7.21331002193362E-17));
#27869=CARTESIAN_POINT('Ctrl Pts',(-3.19410146294443,-1.45511349134961,
1.2766348924177E-16));
#27870=CARTESIAN_POINT('Ctrl Pts',(-3.20290718418031,-1.4388859283946,1.2490009027033E-16));
#27871=CARTESIAN_POINT('Ctrl Pts',(-3.25753999780039,-1.33820622270319,
1.07755298047126E-16));
#27872=CARTESIAN_POINT('Ctrl Pts',(-3.30741231186542,-1.23516335787123,
5.68363615759287E-16));
#27873=CARTESIAN_POINT('Ctrl Pts',(-3.35241796906181,-1.13019103593447,
4.71844785465692E-16));
#27874=CARTESIAN_POINT('Ctrl Pts',(-3.39804200535616,-1.0237763911033,3.73999783509847E-16));
#27875=CARTESIAN_POINT('Ctrl Pts',(-3.43866526602443,-0.915378183946712,
-6.22512805566231E-17));
#27876=CARTESIAN_POINT('Ctrl Pts',(-3.47413966247048,-0.805410191460158,
-1.66533453693773E-16));
#27877=CARTESIAN_POINT('Ctrl Pts',(-3.50939387582959,-0.696124750178875,
-2.70168366465852E-16));
#27878=CARTESIAN_POINT('Ctrl Pts',(-3.53956336356882,-0.585288114116654,
-7.73645964354313E-17));
#27879=CARTESIAN_POINT('Ctrl Pts',(-3.56445901023683,-0.473280938901883,
-1.38777878078145E-16));
#27880=CARTESIAN_POINT('Ctrl Pts',(-3.58104437402115,-0.39866228078212,
-1.79691120092537E-16));
#27881=CARTESIAN_POINT('Ctrl Pts',(-3.59528821670414,-0.323523611696084,
-9.85603223433227E-18));
#27882=CARTESIAN_POINT('Ctrl Pts',(-3.60712230450606,-0.24797391740747,
-2.77555756156289E-17));
#27883=CARTESIAN_POINT('Ctrl Pts',(-3.61048639425725,-0.226497318913744,
-3.28438994009322E-17));
#27884=CARTESIAN_POINT('Ctrl Pts',(-3.613655686349,-0.204987494839638,2.70286722177284E-16));
#27885=CARTESIAN_POINT('Ctrl Pts',(-3.61662845468875,-0.183446929103701,
2.77555756156289E-16));
#27886=CARTESIAN_POINT('Ctrl Pts',(-3.61934694140478,-0.163748878291719,
2.84203018926811E-16));
#27887=CARTESIAN_POINT('Ctrl Pts',(-3.62190130092961,-0.144022588989176,
-9.4234710418247E-17));
#27888=CARTESIAN_POINT('Ctrl Pts',(-3.62428757941211,-0.124293547804644,
-8.32667268468867E-17));
#27889=CARTESIAN_POINT('Ctrl Pts',(-3.63845233765523,-0.007183537050793,
-1.81616534692129E-17));
#27890=CARTESIAN_POINT('Ctrl Pts',(-3.64672404198312,0.110194833970378,
2.72159498670366E-16));
#27891=CARTESIAN_POINT('Ctrl Pts',(-3.64895596115005,0.227419084314086,
2.4980018054066E-16));
#27892=CARTESIAN_POINT('Ctrl Pts',(-3.6502760977502,0.296754939123098,2.36575080521473E-16));
#27893=CARTESIAN_POINT('Ctrl Pts',(-3.64948239134564,0.366037414325706,
-3.91023963353986E-16));
#27894=CARTESIAN_POINT('Ctrl Pts',(-3.64653656430167,0.435182446792325,
-3.33066907387547E-16));
#27895=CARTESIAN_POINT('Ctrl Pts',(-3.64171075252927,0.548454851010284,
-2.38122486414389E-16));
#27896=CARTESIAN_POINT('Ctrl Pts',(-3.63111244226456,0.661358405661847,
1.01745842338307E-16));
#27897=CARTESIAN_POINT('Ctrl Pts',(-3.61501201454962,0.773605457518614,
8.32667268468867E-17));
#27898=CARTESIAN_POINT('Ctrl Pts',(-3.5986111375463,0.887947146080084,6.44427734916789E-17));
#27899=CARTESIAN_POINT('Ctrl Pts',(-3.57650072189919,1.00160829055033,1.76269981291295E-16));
#27900=CARTESIAN_POINT('Ctrl Pts',(-3.5489124899874,1.11428362811214,1.66533453693773E-16));
#27901=CARTESIAN_POINT('Ctrl Pts',(-3.53981806230419,1.1514269184982,1.63323819005896E-16));
#27902=CARTESIAN_POINT('Ctrl Pts',(-3.53012795001213,1.18846302772386,5.91487372108521E-17));
#27903=CARTESIAN_POINT('Ctrl Pts',(-3.51984924725713,1.22538078979166,5.55111512312578E-17));
#27904=CARTESIAN_POINT('Ctrl Pts',(-3.51512490385872,1.24234909694735,5.38392276706252E-17));
#27905=CARTESIAN_POINT('Ctrl Pts',(-3.51027554782375,1.25929445386572,-8.56270895207211E-17));
#27906=CARTESIAN_POINT('Ctrl Pts',(-3.5053071420154,1.27619828084334,-8.32667268468867E-17));
#27907=CARTESIAN_POINT('Ctrl Pts',(-3.4726474677456,1.38731510670219,-6.77509499438615E-17));
#27908=CARTESIAN_POINT('Ctrl Pts',(-3.43480620738079,1.4967920748245,-3.16991689118145E-16));
#27909=CARTESIAN_POINT('Ctrl Pts',(-3.3920889732967,1.60433756714027,-2.77555756156289E-16));
#27910=CARTESIAN_POINT('Ctrl Pts',(-3.34803513046651,1.71524812390167,-2.36885885322814E-16));
#27911=CARTESIAN_POINT('Ctrl Pts',(-3.29879531544834,1.82410515487266,-4.90905898233538E-17));
#27912=CARTESIAN_POINT('Ctrl Pts',(-3.2446494755425,1.93058787890887,-2.77555756156289E-17));
#27913=CARTESIAN_POINT('Ctrl Pts',(-3.19007975249465,2.03790420773747,-6.25353928999361E-18));
#27914=CARTESIAN_POINT('Ctrl Pts',(-3.13052656738101,2.14280969706861,3.27691398306138E-16));
#27915=CARTESIAN_POINT('Ctrl Pts',(-3.06622468325314,2.24496360523417,3.33066907387547E-16));
#27916=CARTESIAN_POINT('Ctrl Pts',(-3.02442954901331,2.31136191319685,3.36560897131582E-16));
#27917=CARTESIAN_POINT('Ctrl Pts',(-2.98062715064349,2.37659746123392,-1.92345692100733E-16));
#27918=CARTESIAN_POINT('Ctrl Pts',(-2.93487136195522,2.44057147262401,-2.22044604925031E-16));
#27919=CARTESIAN_POINT('Ctrl Pts',(-2.91011088425382,2.47519063509293,-2.38115998071626E-16));
#27920=CARTESIAN_POINT('Ctrl Pts',(-2.88477824351069,2.50944029002795,-9.06967170124101E-17));
#27921=CARTESIAN_POINT('Ctrl Pts',(-2.85888104291211,2.54330410738954,-1.11022302462516E-16));
#27922=CARTESIAN_POINT('Ctrl Pts',(-2.84939469288667,2.55570869233558,-1.1846772565866E-16));
#27923=CARTESIAN_POINT('Ctrl Pts',(-2.83983467756884,2.56805870725536,-6.92597506618051E-18));
#27924=CARTESIAN_POINT('Ctrl Pts',(-2.83020669950388,2.58034686246535,0.));
#27925=CARTESIAN_POINT('Ctrl Pts',(-2.75399123609851,2.67762039564213,5.48262984856848E-17));
#27926=CARTESIAN_POINT('Ctrl Pts',(-2.67342730379929,2.77114184208896,-1.37750122974287E-16));
#27927=CARTESIAN_POINT('Ctrl Pts',(-2.58880471591903,2.86057864451344,-1.11022302462516E-16));
#27928=CARTESIAN_POINT('Ctrl Pts',(-2.5041872730583,2.95001000921607,-8.42961069915503E-17));
#27929=CARTESIAN_POINT('Ctrl Pts',(-2.41551123635495,3.03535802102991,-2.67279349305171E-16));
#27930=CARTESIAN_POINT('Ctrl Pts',(-2.3230183042847,3.11627005080055,-3.33066907387547E-16));
#27931=CARTESIAN_POINT('Ctrl Pts',(-2.23098883090374,3.19677665085427,-3.98524820655353E-16));
#27932=CARTESIAN_POINT('Ctrl Pts',(-2.13518016460462,3.27289238327565,-7.81735663884996E-17));
#27933=CARTESIAN_POINT('Ctrl Pts',(-2.0357894675403,3.34423830723631,-2.22044604925031E-16));
#27934=CARTESIAN_POINT('Ctrl Pts',(-1.93639877047599,3.41558423119697,-3.65915643461563E-16));
#27935=CARTESIAN_POINT('Ctrl Pts',(-1.83342562767619,3.48216116641753,-4.77297284244418E-18));
#27936=CARTESIAN_POINT('Ctrl Pts',(-1.72703261341869,3.54354657824449,0.));
#27937=CARTESIAN_POINT('Origin',(0.,0.,0.));
#27938=CARTESIAN_POINT('Origin',(-1.73205080756888,-3.,-8.));
#27939=CARTESIAN_POINT('',(-1.73205080756888,-3.,-8.));
#27940=CARTESIAN_POINT('',(1.73205080756888,-3.,-8.));
#27941=CARTESIAN_POINT('',(-0.86602540378444,-3.,-8.));
#27942=CARTESIAN_POINT('',(-1.73205080756888,-3.,-4.));
#27943=CARTESIAN_POINT('',(-1.73205080756888,-3.,-8.));
#27944=CARTESIAN_POINT('',(1.73205080756888,-3.,-4.));
#27945=CARTESIAN_POINT('',(-1.73205080756888,-3.,-4.));
#27946=CARTESIAN_POINT('',(1.73205080756888,-3.,-8.));
#27947=CARTESIAN_POINT('Origin',(-3.46410161513775,4.24230095489963E-16,
-8.));
#27948=CARTESIAN_POINT('',(-3.46410161513775,4.24230095489963E-16,-8.));
#27949=CARTESIAN_POINT('',(-3.03108891324554,-0.749999999999999,-8.));
#27950=CARTESIAN_POINT('',(-3.46410161513775,5.55111512312578E-16,-4.));
#27951=CARTESIAN_POINT('',(-3.46410161513775,4.24230095489963E-16,-8.));
#27952=CARTESIAN_POINT('',(-3.46410161513775,4.24230095489963E-16,-4.));
#27953=CARTESIAN_POINT('Origin',(-1.73205080756888,3.,-8.));
#27954=CARTESIAN_POINT('',(-1.73205080756888,3.,-8.));
#27955=CARTESIAN_POINT('',(-2.1650635094611,2.25,-8.));
#27956=CARTESIAN_POINT('',(-1.73205080756888,3.,-4.));
#27957=CARTESIAN_POINT('',(-1.73205080756888,3.,-8.));
#27958=CARTESIAN_POINT('',(-1.73205080756888,3.,-4.));
#27959=CARTESIAN_POINT('Origin',(1.73205080756888,3.,-8.));
#27960=CARTESIAN_POINT('',(1.73205080756888,3.,-8.));
#27961=CARTESIAN_POINT('',(0.866025403784439,3.,-8.));
#27962=CARTESIAN_POINT('',(1.73205080756888,3.,-4.));
#27963=CARTESIAN_POINT('',(1.73205080756888,3.,-8.));
#27964=CARTESIAN_POINT('',(1.73205080756888,3.,-4.));
#27965=CARTESIAN_POINT('Origin',(3.46410161513775,0.,-8.));
#27966=CARTESIAN_POINT('',(3.46410161513775,0.,-8.));
#27967=CARTESIAN_POINT('',(3.03108891324554,0.75,-8.));
#27968=CARTESIAN_POINT('',(3.46410161513775,0.,-4.));
#27969=CARTESIAN_POINT('',(3.46410161513775,0.,-8.));
#27970=CARTESIAN_POINT('',(3.46410161513775,0.,-4.));
#27971=CARTESIAN_POINT('Origin',(1.73205080756888,-3.,-8.));
#27972=CARTESIAN_POINT('',(2.1650635094611,-2.25,-8.));
#27973=CARTESIAN_POINT('',(1.73205080756888,-3.,-4.));
#27974=CARTESIAN_POINT('Origin',(0.,5.55111512312578E-16,-4.));
#27975=CARTESIAN_POINT('Origin',(0.,0.,0.));
#27976=CARTESIAN_POINT('',(-6.5,-7.9602041944578E-16,0.));
#27977=CARTESIAN_POINT('Origin',(0.,0.,0.));
#27978=CARTESIAN_POINT('Origin',(0.,0.,-8.));
#27979=CARTESIAN_POINT('',(-6.5,-7.9602041944578E-16,-8.));
#27980=CARTESIAN_POINT('',(-6.5,-7.9602041944578E-16,-8.));
#27981=CARTESIAN_POINT('Origin',(0.,0.,-8.));
#27982=CARTESIAN_POINT('Origin',(0.,0.,-8.));
#27983=CARTESIAN_POINT('Origin',(0.,0.,25.));
#63721=UNCERTAINTY_MEASURE_WITH_UNIT(LENGTH_MEASURE(0.01),#63756,
'DISTANCE_ACCURACY_VALUE',
'Maximum model space distance between geometric entities at asserted c
onnectivities');
#63735=UNCERTAINTY_MEASURE_WITH_UNIT(LENGTH_MEASURE(0.01),#63756,
'DISTANCE_ACCURACY_VALUE',
'Maximum model space distance between geometric entities at asserted c
onnectivities');
#63741=(
GEOMETRIC_REPRESENTATION_CONTEXT(3)
GLOBAL_UNCERTAINTY_ASSIGNED_CONTEXT((#63721))
GLOBAL_UNIT_ASSIGNED_CONTEXT((#63756,#63758,#63759))
REPRESENTATION_CONTEXT('','3D')
);
#63755=(
GEOMETRIC_REPRESENTATION_CONTEXT(3)
GLOBAL_UNCERTAINTY_ASSIGNED_CONTEXT((#63735))
GLOBAL_UNIT_ASSIGNED_CONTEXT((#63756,#63758,#63759))
REPRESENTATION_CONTEXT('','3D')
);
#63756=(
LENGTH_UNIT()
NAMED_UNIT(*)
SI_UNIT(.MILLI.,.METRE.)
);
#63758=(
NAMED_UNIT(*)
PLANE_ANGLE_UNIT()
SI_UNIT($,.RADIAN.)
);
#63759=(
NAMED_UNIT(*)
SI_UNIT($,.STERADIAN.)
SOLID_ANGLE_UNIT()
);
#63765=SHAPE_DEFINITION_REPRESENTATION(#63784,#63863);
#63784=PRODUCT_DEFINITION_SHAPE('',$,#63883);
#63863=SHAPE_REPRESENTATION('',(#14621),#63741);
#63877=PRODUCT_DEFINITION_CONTEXT('part definition',#63936,'design');
#63883=PRODUCT_DEFINITION('Socket head cap screw M8x25',
'Socket head cap screw M8x25',#63902,#63877);
#63902=PRODUCT_DEFINITION_FORMATION('',$,#63943);
#63936=APPLICATION_CONTEXT(
'Core Data for Automotive Mechanical Design Process');
#63937=PRODUCT_CONTEXT('part definition',#63936,'mechanical');
#63943=PRODUCT('Socket head cap screw M8x25',
'Socket head cap screw M8x25',$,(#63937));
#63960=PRESENTATION_STYLE_ASSIGNMENT((#63967));
#63967=SURFACE_STYLE_USAGE(.BOTH.,#63974);
#63974=SURFACE_SIDE_STYLE('',(#63981));
#63981=SURFACE_STYLE_FILL_AREA(#63988);
#63988=FILL_AREA_STYLE('Dark gray',(#63995));
#63995=FILL_AREA_STYLE_COLOUR('Dark gray',#64002);
#64002=COLOUR_RGB('Dark gray',0.250980392156863,0.282352941176471,0.32156862745098);
ENDSEC;
END-ISO-10303-21;
